ISO-10303-21;
HEADER;
FILE_DESCRIPTION (('STEP AP214'),
    '1' );
FILE_NAME ('spur gear_iso_ISO - Spur gear 2M 34T 20PA 18FW ---S34A75H50L30.0N.step',
    '2026-10-08T11:45:07',
    ( '' ),
    ( '' ),
    'SwSTEP 2.0',
    'SolidWorks 2026',
    '' );
FILE_SCHEMA (( 'AUTOMOTIVE_DESIGN' ));
ENDSEC;

DATA;
#7=DIRECTION ( 'NONE',  ( 0.000000000000000000, 0.000000000000000000, 1.000000000000000000 ) ) ;
#20=EDGE_CURVE ( 'NONE', #11424, #24676, #28236, .T. ) ;
#26=ORIENTED_EDGE ( 'NONE', *, *, #36883, .F. ) ;
#27=DIRECTION ( 'NONE',  ( 0.000000000000000000, 0.000000000000000000, 1.000000000000000000 ) ) ;
#43=ORIENTED_EDGE ( 'NONE', *, *, #17545, .T. ) ;
#46=DIRECTION ( 'NONE',  ( 0.000000000000000000, 0.000000000000000000, 1.000000000000000000 ) ) ;
#51=VERTEX_POINT ( 'NONE', #28063 ) ;
#52=EDGE_CURVE ( 'NONE', #2224, #13079, #24812, .T. ) ;
#63=ORIENTED_EDGE ( 'NONE', *, *, #22832, .T. ) ;
#79=ORIENTED_EDGE ( 'NONE', *, *, #11091, .T. ) ;
#89=ORIENTED_EDGE ( 'NONE', *, *, #24562, .T. ) ;
#90=ORIENTED_EDGE ( 'NONE', *, *, #30632, .T. ) ;
#91=LINE ( 'NONE', #6449, #40012 ) ;
#101=EDGE_LOOP ( 'NONE', ( #3389, #16998, #1175, #14979 ) ) ;
#103=ORIENTED_EDGE ( 'NONE', *, *, #29129, .T. ) ;
#126=ADVANCED_FACE ( 'NONE', ( #11053 ), #35784, .T. ) ;
#131=ADVANCED_FACE ( 'NONE', ( #11260 ), #25041, .T. ) ;
#148=FACE_OUTER_BOUND ( 'NONE', #24269, .T. ) ;
#153=ORIENTED_EDGE ( 'NONE', *, *, #32598, .F. ) ;
#190=CARTESIAN_POINT ( 'NONE',  ( 17.99999999999999645, -31.80866420683992857, 2.997093558041182160 ) ) ;
#212=AXIS2_PLACEMENT_3D ( 'NONE', #31464, #8530, #17983 ) ;
#216=DIRECTION ( 'NONE',  ( -1.000000000000000000, 0.000000000000000000, 0.000000000000000000 ) ) ;
#218=LINE ( 'NONE', #26245, #34087 ) ;
#224=CARTESIAN_POINT ( 'NONE',  ( 17.99999999999999645, -23.87611429743648017, -20.54551452399645939 ) ) ;
#233=CARTESIAN_POINT ( 'NONE',  ( 0.000000000000000000, 12.42760411676038146, 33.78690065568429191 ) ) ;
#243=EDGE_CURVE ( 'NONE', #7044, #26460, #16384, .T. ) ;
#247=ORIENTED_EDGE ( 'NONE', *, *, #11286, .T. ) ;
#248=EDGE_CURVE ( 'NONE', #1617, #22493, #17123, .T. ) ;
#294=VECTOR ( 'NONE', #25496, 1000.000000000000000 ) ;
#310=AXIS2_PLACEMENT_3D ( 'NONE', #8177, #1395, #28267 ) ;
#319=EDGE_CURVE ( 'NONE', #36754, #15839, #12891, .T. ) ;
#321=ORIENTED_EDGE ( 'NONE', *, *, #37167, .T. ) ;
#326=EDGE_CURVE ( 'NONE', #40378, #9051, #40786, .T. ) ;
#327=DIRECTION ( 'NONE',  ( 0.000000000000000000, 0.7980172272802363853, 0.6026346363792605132 ) ) ;
#353=LINE ( 'NONE', #36584, #16374 ) ;
#356=EDGE_CURVE ( 'NONE', #26178, #21757, #8740, .T. ) ;
#365=EDGE_LOOP ( 'NONE', ( #40363, #21648, #12484, #22363 ) ) ;
#370=ORIENTED_EDGE ( 'NONE', *, *, #15483, .F. ) ;
#374=DIRECTION ( 'NONE',  ( 0.000000000000000000, 0.000000000000000000, -1.000000000000000000 ) ) ;
#378=AXIS2_PLACEMENT_3D ( 'NONE', #10736, #14239, #7672 ) ;
#383=AXIS2_PLACEMENT_3D ( 'NONE', #12644, #12853, #30723 ) ;
#392=CARTESIAN_POINT ( 'NONE',  ( 17.99999999999999645, 0.000000000000000000, 0.000000000000000000 ) ) ;
#395=ORIENTED_EDGE ( 'NONE', *, *, #18780, .F. ) ;
#408=CARTESIAN_POINT ( 'NONE',  ( 0.000000000000000000, 31.80866420683990725, 16.59709355804141495 ) ) ;
#419=DIRECTION ( 'NONE',  ( 0.000000000000000000, 0.000000000000000000, 1.000000000000000000 ) ) ;
#420=ORIENTED_EDGE ( 'NONE', *, *, #41596, .F. ) ;
#430=DIRECTION ( 'NONE',  ( -1.000000000000000000, -0.000000000000000000, 0.000000000000000000 ) ) ;
#431=AXIS2_PLACEMENT_3D ( 'NONE', #12045, #31659, #11830 ) ;
#451=ORIENTED_EDGE ( 'NONE', *, *, #9647, .F. ) ;
#452=CARTESIAN_POINT ( 'NONE',  ( 17.99999999999999645, 0.000000000000000000, 0.000000000000000000 ) ) ;
#455=ORIENTED_EDGE ( 'NONE', *, *, #22771, .T. ) ;
#462=CIRCLE ( 'NONE', #22115, 13.60000000000000142 ) ;
#471=ORIENTED_EDGE ( 'NONE', *, *, #11051, .F. ) ;
#474=ORIENTED_EDGE ( 'NONE', *, *, #37927, .T. ) ;
#475=DIRECTION ( 'NONE',  ( -1.000000000000000000, -0.000000000000000000, 0.000000000000000000 ) ) ;
#502=AXIS2_PLACEMENT_3D ( 'NONE', #28642, #35156, #28215 ) ;
#526=DIRECTION ( 'NONE',  ( 0.000000000000000000, 0.000000000000000000, 1.000000000000000000 ) ) ;
#544=DIRECTION ( 'NONE',  ( -1.000000000000000000, 0.000000000000000000, -0.000000000000000000 ) ) ;
#547=FACE_BOUND ( 'NONE', #22047, .T. ) ;
#551=EDGE_CURVE ( 'NONE', #38409, #5751, #33026, .T. ) ;
#564=EDGE_CURVE ( 'NONE', #21757, #23443, #22642, .T. ) ;
#587=DIRECTION ( 'NONE',  ( -1.000000000000000000, 0.000000000000000000, 0.000000000000000000 ) ) ;
#588=EDGE_CURVE ( 'NONE', #36837, #2925, #6541, .T. ) ;
#593=AXIS2_PLACEMENT_3D ( 'NONE', #42590, #9443, #2867 ) ;
#594=EDGE_LOOP ( 'NONE', ( #9108, #20591, #34334, #3466 ) ) ;
#606=VERTEX_POINT ( 'NONE', #25767 ) ;
#619=FACE_OUTER_BOUND ( 'NONE', #3367, .T. ) ;
#633=CARTESIAN_POINT ( 'NONE',  ( 17.99999999999999645, 0.000000000000000000, 0.000000000000000000 ) ) ;
#635=ORIENTED_EDGE ( 'NONE', *, *, #17742, .T. ) ;
#637=VERTEX_POINT ( 'NONE', #6729 ) ;
#639=CIRCLE ( 'NONE', #2719, 36.00000000000000000 ) ;
#641=FACE_OUTER_BOUND ( 'NONE', #29128, .T. ) ;
#645=DIRECTION ( 'NONE',  ( -1.000000000000000000, 0.000000000000000000, -0.000000000000000000 ) ) ;
#648=ORIENTED_EDGE ( 'NONE', *, *, #24910, .T. ) ;
#652=CARTESIAN_POINT ( 'NONE',  ( 17.99999999999999645, -2.007101075700182591, 31.43498920425968279 ) ) ;
#660=ORIENTED_EDGE ( 'NONE', *, *, #6365, .T. ) ;
#673=AXIS2_PLACEMENT_3D ( 'NONE', #23183, #40131, #40354 ) ;
#682=ORIENTED_EDGE ( 'NONE', *, *, #5364, .T. ) ;
#686=EDGE_CURVE ( 'NONE', #51, #7956, #33742, .T. ) ;
#700=DIRECTION ( 'NONE',  ( 0.000000000000000000, 0.000000000000000000, 1.000000000000000000 ) ) ;
#720=FACE_OUTER_BOUND ( 'NONE', #18484, .T. ) ;
#723=ORIENTED_EDGE ( 'NONE', *, *, #248, .T. ) ;
#731=ORIENTED_EDGE ( 'NONE', *, *, #31759, .T. ) ;
#732=VECTOR ( 'NONE', #15027, 1000.000000000000000 ) ;
#737=EDGE_CURVE ( 'NONE', #1458, #13372, #15945, .T. ) ;
#738=DIRECTION ( 'NONE',  ( 0.000000000000000000, 0.000000000000000000, -1.000000000000000000 ) ) ;
#761=FACE_OUTER_BOUND ( 'NONE', #34017, .T. ) ;
#763=ORIENTED_EDGE ( 'NONE', *, *, #22251, .F. ) ;
#785=CARTESIAN_POINT ( 'NONE',  ( 17.99999999999999645, 0.000000000000000000, 0.000000000000000000 ) ) ;
#799=EDGE_LOOP ( 'NONE', ( #7058, #14371, #34397, #3950 ) ) ;
#809=CIRCLE ( 'NONE', #33583, 31.49899999999999878 ) ;
#811=DIRECTION ( 'NONE',  ( -1.000000000000000000, -0.000000000000000000, -0.000000000000000000 ) ) ;
#822=CARTESIAN_POINT ( 'NONE',  ( 17.99999999999999645, 0.000000000000000000, 0.000000000000000000 ) ) ;
#851=ORIENTED_EDGE ( 'NONE', *, *, #31292, .F. ) ;
#870=ORIENTED_EDGE ( 'NONE', *, *, #13246, .F. ) ;
#884=CIRCLE ( 'NONE', #32268, 13.59999999999999964 ) ;
#885=EDGE_CURVE ( 'NONE', #23736, #7766, #38626, .T. ) ;
#895=CARTESIAN_POINT ( 'NONE',  ( 17.99999999999999645, -28.62203781742993414, -14.19692359621484989 ) ) ;
#905=ORIENTED_EDGE ( 'NONE', *, *, #39410, .T. ) ;
#912=ORIENTED_EDGE ( 'NONE', *, *, #3824, .F. ) ;
#929=CARTESIAN_POINT ( 'NONE',  ( 0.000000000000000000, 0.000000000000000000, 0.000000000000000000 ) ) ;
#930=ORIENTED_EDGE ( 'NONE', *, *, #21468, .T. ) ;
#937=SURFACE_STYLE_USAGE ( .BOTH. , #27168 ) ;
#948=DIRECTION ( 'NONE',  ( 0.000000000000000000, 0.1837495178165638177, 0.9829730996839030066 ) ) ;
#963=EDGE_CURVE ( 'NONE', #39350, #15922, #24979, .T. ) ;
#965=AXIS2_PLACEMENT_3D ( 'NONE', #8712, #15089, #35532 ) ;
#987=AXIS2_PLACEMENT_3D ( 'NONE', #7218, #20574, #3932 ) ;
#988=EDGE_CURVE ( 'NONE', #38106, #24796, #34858, .T. ) ;
#990=VERTEX_POINT ( 'NONE', #24646 ) ;
#1008=ORIENTED_EDGE ( 'NONE', *, *, #6860, .T. ) ;
#1015=DIRECTION ( 'NONE',  ( -1.000000000000000000, 0.000000000000000000, 0.000000000000000000 ) ) ;
#1017=EDGE_CURVE ( 'NONE', #26550, #30103, #18543, .T. ) ;
#1028=CIRCLE ( 'NONE', #32411, 31.49899999999999878 ) ;
#1046=AXIS2_PLACEMENT_3D ( 'NONE', #16688, #39312, #36058 ) ;
#1053=EDGE_CURVE ( 'NONE', #10216, #990, #8208, .T. ) ;
#1057=AXIS2_PLACEMENT_3D ( 'NONE', #31225, #645, #40360 ) ;
#1059=VERTEX_POINT ( 'NONE', #1467 ) ;
#1060=CARTESIAN_POINT ( 'NONE',  ( 17.99999999999999645, 19.69434969228107946, -24.58291258574028504 ) ) ;
#1073=DIRECTION ( 'NONE',  ( 0.000000000000000000, 0.5264321628773506179, 0.8502171357296174348 ) ) ;
#1078=DIRECTION ( 'NONE',  ( -1.000000000000000000, 0.000000000000000000, -0.000000000000000000 ) ) ;
#1079=LINE ( 'NONE', #1308, #38060 ) ;
#1087=FACE_OUTER_BOUND ( 'NONE', #9984, .T. ) ;
#1104=AXIS2_PLACEMENT_3D ( 'NONE', #21842, #32253, #22048 ) ;
#1117=ORIENTED_EDGE ( 'NONE', *, *, #14504, .F. ) ;
#1127=CARTESIAN_POINT ( 'NONE',  ( 17.99999999999999645, 0.000000000000000000, 0.000000000000000000 ) ) ;
#1128=VECTOR ( 'NONE', #24223, 1000.000000000000000 ) ;
#1139=DIRECTION ( 'NONE',  ( -1.000000000000000000, -0.000000000000000000, -0.000000000000000000 ) ) ;
#1170=EDGE_CURVE ( 'NONE', #1826, #25635, #19389, .T. ) ;
#1173=ORIENTED_EDGE ( 'NONE', *, *, #21059, .F. ) ;
#1174=CARTESIAN_POINT ( 'NONE',  ( 17.99999999999999645, -31.48608500567869584, -0.9019157472707834966 ) ) ;
#1175=ORIENTED_EDGE ( 'NONE', *, *, #11123, .T. ) ;
#1189=EDGE_CURVE ( 'NONE', #27145, #20374, #25648, .T. ) ;
#1224=AXIS2_PLACEMENT_3D ( 'NONE', #2448, #15398, #16029 ) ;
#1230=CARTESIAN_POINT ( 'NONE',  ( 17.99999999999999645, -5.822172717930484964, 31.41458249383138934 ) ) ;
#1239=CARTESIAN_POINT ( 'NONE',  ( 8.999999999999998224, -12.42760411676061949, 33.78690065568420664 ) ) ;
#1266=AXIS2_PLACEMENT_3D ( 'NONE', #33038, #13435, #39354 ) ;
#1274=CIRCLE ( 'NONE', #42337, 31.49900000000000588 ) ;
#1296=ORIENTED_EDGE ( 'NONE', *, *, #34658, .F. ) ;
#1297=LINE ( 'NONE', #14644, #18318 ) ;
#1298=CYLINDRICAL_SURFACE ( 'NONE', #14562, 36.00000000000000000 ) ;
#1301=ORIENTED_EDGE ( 'NONE', *, *, #551, .T. ) ;
#1302=DIRECTION ( 'NONE',  ( 0.000000000000000000, 0.1837495178165707566, -0.9829730996839017854 ) ) ;
#1308=CARTESIAN_POINT ( 'NONE',  ( 8.999999999999998224, 31.94619804602764290, 16.59639811537368814 ) ) ;
#1311=ADVANCED_FACE ( 'NONE', ( #30890 ), #10828, .T. ) ;
#1314=CARTESIAN_POINT ( 'NONE',  ( 17.99999999999999645, -13.22719389141998825, 28.58720592780592185 ) ) ;
#1320=LINE ( 'NONE', #38190, #25849 ) ;
#1322=ORIENTED_EDGE ( 'NONE', *, *, #8182, .F. ) ;
#1327=CARTESIAN_POINT ( 'NONE',  ( 17.99999999999999645, -25.46650492921910924, 19.29328419707777087 ) ) ;
#1328=DIRECTION ( 'NONE',  ( 1.000000000000000000, -0.000000000000000000, -0.000000000000000000 ) ) ;
#1330=ORIENTED_EDGE ( 'NONE', *, *, #27210, .T. ) ;
#1337=LINE ( 'NONE', #28630, #17622 ) ;
#1349=ORIENTED_EDGE ( 'NONE', *, *, #33619, .F. ) ;
#1363=ORIENTED_EDGE ( 'NONE', *, *, #1409, .F. ) ;
#1367=CARTESIAN_POINT ( 'NONE',  ( 0.000000000000000000, 0.000000000000000000, 0.000000000000000000 ) ) ;
#1368=DIRECTION ( 'NONE',  ( 0.000000000000000000, 0.000000000000000000, 1.000000000000000000 ) ) ;
#1379=CARTESIAN_POINT ( 'NONE',  ( -10.00000000000000000, 0.000000000000000000, 0.000000000000000000 ) ) ;
#1389=ORIENTED_EDGE ( 'NONE', *, *, #13360, .T. ) ;
#1395=DIRECTION ( 'NONE',  ( 1.000000000000000000, 0.000000000000000000, 0.000000000000000000 ) ) ;
#1401=VERTEX_POINT ( 'NONE', #40030 ) ;
#1409=EDGE_CURVE ( 'NONE', #30643, #17666, #40880, .T. ) ;
#1428=CARTESIAN_POINT ( 'NONE',  ( 17.99999999999999645, -29.68570942776479527, 10.53307442156924267 ) ) ;
#1429=ADVANCED_FACE ( 'NONE', ( #35226 ), #28513, .T. ) ;
#1431=EDGE_LOOP ( 'NONE', ( #35385, #15024, #20016, #15168 ) ) ;
#1434=CARTESIAN_POINT ( 'NONE',  ( 17.99999999999999645, -31.48608500567871005, 0.9019157472703476230 ) ) ;
#1438=CYLINDRICAL_SURFACE ( 'NONE', #16743, 36.00000000000000000 ) ;
#1444=CARTESIAN_POINT ( 'NONE',  ( 17.99999999999999645, -16.86122981692000167, -27.13802899033310112 ) ) ;
#1458=VERTEX_POINT ( 'NONE', #41111 ) ;
#1459=DIRECTION ( 'NONE',  ( 0.000000000000000000, 0.000000000000000000, -1.000000000000000000 ) ) ;
#1467=CARTESIAN_POINT ( 'NONE',  ( 0.000000000000000000, -34.45183346761142928, 10.44371441202643247 ) ) ;
#1468=VECTOR ( 'NONE', #2507, 1000.000000000000000 ) ;
#1469=EDGE_CURVE ( 'NONE', #15044, #4662, #21969, .T. ) ;
#1496=CARTESIAN_POINT ( 'NONE',  ( 17.99999999999999645, 31.11570115861495367, 4.898994019976747438 ) ) ;
#1505=CARTESIAN_POINT ( 'NONE',  ( 17.99999999999999645, -0.04937522221144796664, 31.94951095880159997 ) ) ;
#1507=VERTEX_POINT ( 'NONE', #21334 ) ;
#1508=CARTESIAN_POINT ( 'NONE',  ( 17.99999999999999645, -14.84191762912296930, -27.78316904333141224 ) ) ;
#1514=FACE_OUTER_BOUND ( 'NONE', #30875, .T. ) ;
#1549=CARTESIAN_POINT ( 'NONE',  ( 17.99999999999999645, -31.81777574834303124, 10.70123563439434733 ) ) ;
#1571=ORIENTED_EDGE ( 'NONE', *, *, #22036, .T. ) ;
#1577=ORIENTED_EDGE ( 'NONE', *, *, #5048, .F. ) ;
#1581=CARTESIAN_POINT ( 'NONE',  ( 17.99999999999999645, -0.04937522221144796664, 31.94951095880159997 ) ) ;
#1608=CYLINDRICAL_SURFACE ( 'NONE', #41636, 36.00000000000000000 ) ;
#1617=VERTEX_POINT ( 'NONE', #16258 ) ;
#1634=AXIS2_PLACEMENT_3D ( 'NONE', #30829, #3526, #20184 ) ;
#1658=CARTESIAN_POINT ( 'NONE',  ( 17.99999999999999645, 27.24480646643607074, 15.80846360676594564 ) ) ;
#1661=CARTESIAN_POINT ( 'NONE',  ( 9.000000000000000000, -18.42432724429453827, -30.92804820216021611 ) ) ;
#1662=ORIENTED_EDGE ( 'NONE', *, *, #26038, .F. ) ;
#1671=DIRECTION ( 'NONE',  ( 0.000000000000000000, -6.887872625202028030E-15, 1.000000000000000000 ) ) ;
#1674=DIRECTION ( 'NONE',  ( -1.000000000000000000, -0.000000000000000000, -0.000000000000000000 ) ) ;
#1681=DIRECTION ( 'NONE',  ( 0.000000000000000000, 0.000000000000000000, 1.000000000000000000 ) ) ;
#1688=PRODUCT_DEFINITION_FORMATION_WITH_SPECIFIED_SOURCE ( 'ANY', '', #42610, .NOT_KNOWN. ) ;
#1695=ORIENTED_EDGE ( 'NONE', *, *, #28401, .T. ) ;
#1697=AXIS2_PLACEMENT_3D ( 'NONE', #25090, #12178, #11967 ) ;
#1701=EDGE_LOOP ( 'NONE', ( #4047, #40782, #39916, #41488 ) ) ;
#1703=VECTOR ( 'NONE', #42041, 1000.000000000000000 ) ;
#1718=ORIENTED_EDGE ( 'NONE', *, *, #8640, .F. ) ;
#1721=ORIENTED_EDGE ( 'NONE', *, *, #16760, .T. ) ;
#1722=DIRECTION ( 'NONE',  ( -1.000000000000000000, 0.000000000000000000, 0.000000000000000000 ) ) ;
#1727=AXIS2_PLACEMENT_3D ( 'NONE', #22337, #26009, #32324 ) ;
#1737=DIRECTION ( 'NONE',  ( 0.000000000000000000, 0.000000000000000000, 1.000000000000000000 ) ) ;
#1740=AXIS2_PLACEMENT_3D ( 'NONE', #15647, #2288, #29380 ) ;
#1749=EDGE_CURVE ( 'NONE', #5647, #37373, #5403, .T. ) ;
#1768=DIRECTION ( 'NONE',  ( -1.000000000000000000, -0.000000000000000000, 0.000000000000000000 ) ) ;
#1792=DIRECTION ( 'NONE',  ( -1.000000000000000000, -0.000000000000000000, -0.000000000000000000 ) ) ;
#1798=DIRECTION ( 'NONE',  ( -1.000000000000000000, 0.000000000000000000, 0.000000000000000000 ) ) ;
#1801=DIRECTION ( 'NONE',  ( -1.000000000000000000, -0.000000000000000000, 0.000000000000000000 ) ) ;
#1803=ORIENTED_EDGE ( 'NONE', *, *, #38011, .T. ) ;
#1805=AXIS2_PLACEMENT_3D ( 'NONE', #6929, #17448, #20081 ) ;
#1810=DIRECTION ( 'NONE',  ( 0.000000000000000000, 0.000000000000000000, -1.000000000000000000 ) ) ;
#1816=CYLINDRICAL_SURFACE ( 'NONE', #15838, 31.49899999999999878 ) ;
#1826=VERTEX_POINT ( 'NONE', #26708 ) ;
#1828=DIRECTION ( 'NONE',  ( -1.000000000000000000, -0.000000000000000000, -0.000000000000000000 ) ) ;
#1839=VERTEX_POINT ( 'NONE', #30200 ) ;
#1860=CARTESIAN_POINT ( 'NONE',  ( 17.99999999999999645, 0.000000000000000000, 0.000000000000000000 ) ) ;
#1864=CYLINDRICAL_SURFACE ( 'NONE', #10730, 36.00000000000000000 ) ;
#1868=AXIS2_PLACEMENT_3D ( 'NONE', #20455, #33716, #13903 ) ;
#1878=ORIENTED_EDGE ( 'NONE', *, *, #22280, .T. ) ;
#1893=EDGE_CURVE ( 'NONE', #15044, #36592, #15853, .T. ) ;
#1896=EDGE_LOOP ( 'NONE', ( #11436, #40390, #32204, #905 ) ) ;
#1902=ADVANCED_FACE ( 'NONE', ( #18230 ), #11652, .T. ) ;
#1904=CARTESIAN_POINT ( 'NONE',  ( 17.99999999999999645, 2.007101075699966763, 31.43498920425970411 ) ) ;
#1911=ADVANCED_FACE ( 'NONE', ( #37800 ), #11005, .T. ) ;
#1917=LINE ( 'NONE', #18341, #1703 ) ;
#1921=ORIENTED_EDGE ( 'NONE', *, *, #11316, .T. ) ;
#1922=VECTOR ( 'NONE', #17544, 1000.000000000000000 ) ;
#1933=DIRECTION ( 'NONE',  ( -1.000000000000000000, -0.000000000000000000, -0.000000000000000000 ) ) ;
#1937=DIRECTION ( 'NONE',  ( 0.000000000000000000, 0.000000000000000000, 1.000000000000000000 ) ) ;
#1939=CIRCLE ( 'NONE', #17377, 13.59999999999999787 ) ;
#1957=VERTEX_POINT ( 'NONE', #34531 ) ;
#1962=VERTEX_POINT ( 'NONE', #8353 ) ;
#1967=DIRECTION ( 'NONE',  ( 0.000000000000000000, 0.8951632913550604531, 0.4457383557765420834 ) ) ;
#1969=ORIENTED_EDGE ( 'NONE', *, *, #3743, .T. ) ;
#1971=CARTESIAN_POINT ( 'NONE',  ( 17.99999999999999645, -27.24480646643597126, -15.80846360676612861 ) ) ;
#1973=VERTEX_POINT ( 'NONE', #28021 ) ;
#1978=DIRECTION ( 'NONE',  ( 1.000000000000000000, 0.000000000000000000, 0.000000000000000000 ) ) ;
#1986=FACE_OUTER_BOUND ( 'NONE', #6911, .T. ) ;
#1996=ORIENTED_EDGE ( 'NONE', *, *, #34716, .F. ) ;
#2003=DIRECTION ( 'NONE',  ( 0.000000000000000000, -0.8951632913550663373, 0.4457383557765300930 ) ) ;
#2007=ADVANCED_FACE ( 'NONE', ( #34968, #2009 ), #24763, .F. ) ;
#2008=DIRECTION ( 'NONE',  ( -1.000000000000000000, -0.000000000000000000, -0.000000000000000000 ) ) ;
#2009=FACE_OUTER_BOUND ( 'NONE', #34245, .T. ) ;
#2013=VERTEX_POINT ( 'NONE', #26233 ) ;
#2021=EDGE_CURVE ( 'NONE', #31789, #27337, #36232, .T. ) ;
#2024=DIRECTION ( 'NONE',  ( 0.000000000000000000, -0.9957341762950354669, 0.09226835946329131621 ) ) ;
#2028=AXIS2_PLACEMENT_3D ( 'NONE', #36456, #40160, #7 ) ;
#2051=ADVANCED_FACE ( 'NONE', ( #19277 ), #2637, .T. ) ;
#2079=ORIENTED_EDGE ( 'NONE', *, *, #3317, .T. ) ;
#2088=CARTESIAN_POINT ( 'NONE',  ( 17.99999999999999645, 26.29521155129848964, 17.34211205339357065 ) ) ;
#2093=EDGE_LOOP ( 'NONE', ( #14400, #9830, #23029, #24213 ) ) ;
#2131=VECTOR ( 'NONE', #10668, 1000.000000000000000 ) ;
#2150=CARTESIAN_POINT ( 'NONE',  ( 17.99999999999999645, 0.000000000000000000, 0.000000000000000000 ) ) ;
#2153=CARTESIAN_POINT ( 'NONE',  ( 17.99999999999999645, 34.45183346761150744, -10.44371441202619444 ) ) ;
#2156=DIRECTION ( 'NONE',  ( 0.000000000000000000, -0.9618256431728159361, -0.2736629900720938813 ) ) ;
#2171=DIRECTION ( 'NONE',  ( -1.000000000000000000, 0.000000000000000000, 0.000000000000000000 ) ) ;
#2174=EDGE_CURVE ( 'NONE', #34774, #41169, #4771, .T. ) ;
#2176=ADVANCED_FACE ( 'NONE', ( #10499 ), #26873, .T. ) ;
#2177=CIRCLE ( 'NONE', #34964, 31.49900000000000233 ) ;
#2187=DIRECTION ( 'NONE',  ( -1.000000000000000000, -0.000000000000000000, 0.000000000000000000 ) ) ;
#2194=CIRCLE ( 'NONE', #35651, 13.59999999999999964 ) ;
#2200=CYLINDRICAL_SURFACE ( 'NONE', #37712, 13.59999999999999964 ) ;
#2202=DIRECTION ( 'NONE',  ( -1.000000000000000000, 0.000000000000000000, 0.000000000000000000 ) ) ;
#2209=EDGE_CURVE ( 'NONE', #39386, #13089, #10105, .T. ) ;
#2214=ORIENTED_EDGE ( 'NONE', *, *, #39218, .T. ) ;
#2219=CARTESIAN_POINT ( 'NONE',  ( 17.99999999999999645, -19.69434969228090893, 24.58291258574042004 ) ) ;
#2222=EDGE_CURVE ( 'NONE', #637, #10990, #3491, .T. ) ;
#2224=VERTEX_POINT ( 'NONE', #40149 ) ;
#2232=VERTEX_POINT ( 'NONE', #13366 ) ;
#2233=DIRECTION ( 'NONE',  ( -1.000000000000000000, 0.000000000000000000, 0.000000000000000000 ) ) ;
#2243=CARTESIAN_POINT ( 'NONE',  ( 17.99999999999999645, -24.70533337038242649, 26.18485254986684296 ) ) ;
#2245=CARTESIAN_POINT ( 'NONE',  ( 17.99999999999999645, 16.86122981692056655, -27.13802899033274940 ) ) ;
#2250=DIRECTION ( 'NONE',  ( -1.000000000000000000, 0.000000000000000000, -0.000000000000000000 ) ) ;
#2257=EDGE_CURVE ( 'NONE', #35838, #26002, #34649, .T. ) ;
#2268=CARTESIAN_POINT ( 'NONE',  ( -10.00000000000000000, 0.000000000000000000, 0.000000000000000000 ) ) ;
#2288=DIRECTION ( 'NONE',  ( -1.000000000000000000, -0.000000000000000000, -0.000000000000000000 ) ) ;
#2289=ORIENTED_EDGE ( 'NONE', *, *, #37302, .F. ) ;
#2290=CARTESIAN_POINT ( 'NONE',  ( 9.000000000000000000, -6.007673836297746206, -35.49518073030003507 ) ) ;
#2301=CARTESIAN_POINT ( 'NONE',  ( 0.000000000000000000, 0.000000000000000000, 0.000000000000000000 ) ) ;
#2311=ORIENTED_EDGE ( 'NONE', *, *, #27025, .F. ) ;
#2315=CARTESIAN_POINT ( 'NONE',  ( 8.999999999999998224, -28.35267316522799419, 22.18391138608698299 ) ) ;
#2320=ORIENTED_EDGE ( 'NONE', *, *, #7928, .T. ) ;
#2333=CARTESIAN_POINT ( 'NONE',  ( 0.000000000000000000, -29.03409033315573851, -12.21509719675420946 ) ) ;
#2335=DIRECTION ( 'NONE',  ( -1.000000000000000000, -0.000000000000000000, 0.000000000000000000 ) ) ;
#2348=ORIENTED_EDGE ( 'NONE', *, *, #14413, .F. ) ;
#2358=ORIENTED_EDGE ( 'NONE', *, *, #10200, .F. ) ;
#2364=AXIS2_PLACEMENT_3D ( 'NONE', #36310, #38734, #6007 ) ;
#2369=DIRECTION ( 'NONE',  ( 0.000000000000000000, 0.000000000000000000, 1.000000000000000000 ) ) ;
#2374=ORIENTED_EDGE ( 'NONE', *, *, #16195, .F. ) ;
#2377=EDGE_LOOP ( 'NONE', ( #38231, #17944, #6084, #2912 ) ) ;
#2380=CARTESIAN_POINT ( 'NONE',  ( 17.99999999999999645, 30.74337109795219547, -8.695908345466218492 ) ) ;
#2418=AXIS2_PLACEMENT_3D ( 'NONE', #9197, #9403, #38866 ) ;
#2423=VECTOR ( 'NONE', #3623, 1000.000000000000000 ) ;
#2426=DIRECTION ( 'NONE',  ( -1.000000000000000000, 0.000000000000000000, 0.000000000000000000 ) ) ;
#2433=ORIENTED_EDGE ( 'NONE', *, *, #41200, .T. ) ;
#2435=CARTESIAN_POINT ( 'NONE',  ( 0.000000000000000000, 24.70533337038260768, -26.18485254986667243 ) ) ;
#2447=CIRCLE ( 'NONE', #29651, 13.59999999999999964 ) ;
#2448=CARTESIAN_POINT ( 'NONE',  ( 17.99999999999999645, 21.56073507908678977, -23.57770962728541875 ) ) ;
#2449=DIRECTION ( 'NONE',  ( 0.000000000000000000, 0.9957341762950348008, -0.09226835946329869920 ) ) ;
#2455=VECTOR ( 'NONE', #11395, 1000.000000000000000 ) ;
#2462=ORIENTED_EDGE ( 'NONE', *, *, #11129, .T. ) ;
#2463=CARTESIAN_POINT ( 'NONE',  ( 0.000000000000000000, 18.25486108452625089, 25.66996392254279868 ) ) ;
#2486=CIRCLE ( 'NONE', #34555, 13.60000000000000142 ) ;
#2507=DIRECTION ( 'NONE',  ( 1.000000000000000000, -0.000000000000000000, 0.000000000000000000 ) ) ;
#2522=DIRECTION ( 'NONE',  ( -1.000000000000000000, 0.000000000000000000, 0.000000000000000000 ) ) ;
#2523=DIRECTION ( 'NONE',  ( 0.000000000000000000, 0.9618256431728199329, -0.2736629900720799480 ) ) ;
#2529=DIRECTION ( 'NONE',  ( -1.000000000000000000, -0.000000000000000000, 0.000000000000000000 ) ) ;
#2534=EDGE_CURVE ( 'NONE', #13079, #18333, #22034, .T. ) ;
#2541=ORIENTED_EDGE ( 'NONE', *, *, #32242, .T. ) ;
#2558=EDGE_CURVE ( 'NONE', #32077, #37206, #42892, .T. ) ;
#2563=EDGE_LOOP ( 'NONE', ( #37489, #5883, #11625, #20473 ) ) ;
#2571=EDGE_LOOP ( 'NONE', ( #11773, #3935, #14039, #27082 ) ) ;
#2589=CIRCLE ( 'NONE', #3988, 31.49900000000000233 ) ;
#2593=AXIS2_PLACEMENT_3D ( 'NONE', #4389, #34942, #14474 ) ;
#2608=DIRECTION ( 'NONE',  ( -1.000000000000000000, 0.000000000000000000, 0.000000000000000000 ) ) ;
#2609=AXIS2_PLACEMENT_3D ( 'NONE', #37508, #17926, #14407 ) ;
#2613=DIRECTION ( 'NONE',  ( 0.000000000000000000, 0.000000000000000000, 1.000000000000000000 ) ) ;
#2637=CYLINDRICAL_SURFACE ( 'NONE', #16500, 36.00000000000000000 ) ;
#2644=AXIS2_PLACEMENT_3D ( 'NONE', #16680, #42385, #39105 ) ;
#2652=ORIENTED_EDGE ( 'NONE', *, *, #6192, .T. ) ;
#2653=CARTESIAN_POINT ( 'NONE',  ( 0.000000000000000000, 0.000000000000000000, 0.000000000000000000 ) ) ;
#2655=EDGE_CURVE ( 'NONE', #26427, #7766, #40912, .T. ) ;
#2658=DIRECTION ( 'NONE',  ( -1.000000000000000000, -0.000000000000000000, -0.000000000000000000 ) ) ;
#2661=ORIENTED_EDGE ( 'NONE', *, *, #8849, .T. ) ;
#2719=AXIS2_PLACEMENT_3D ( 'NONE', #20295, #30300, #20509 ) ;
#2723=CARTESIAN_POINT ( 'NONE',  ( 17.99999999999999645, -22.66088087769164972, -21.87856208362581256 ) ) ;
#2730=ORIENTED_EDGE ( 'NONE', *, *, #30580, .F. ) ;
#2734=CARTESIAN_POINT ( 'NONE',  ( 0.000000000000000000, -18.25486108452643208, 25.66996392254267079 ) ) ;
#2764=ORIENTED_EDGE ( 'NONE', *, *, #7843, .F. ) ;
#2773=CARTESIAN_POINT ( 'NONE',  ( 9.000000000000000000, 34.45183346761135113, 10.44371441202667761 ) ) ;
#2782=CARTESIAN_POINT ( 'NONE',  ( 0.000000000000000000, 0.000000000000000000, 0.000000000000000000 ) ) ;
#2784=CARTESIAN_POINT ( 'NONE',  ( 17.99999999999999645, 23.87611429743691360, -20.54551452399595135 ) ) ;
#2785=AXIS2_PLACEMENT_3D ( 'NONE', #22316, #32940, #3016 ) ;
#2793=EDGE_LOOP ( 'NONE', ( #39259, #22003, #16775, #1803 ) ) ;
#2811=DIRECTION ( 'NONE',  ( -1.000000000000000000, 0.000000000000000000, 0.000000000000000000 ) ) ;
#2819=ORIENTED_EDGE ( 'NONE', *, *, #10470, .T. ) ;
#2821=DIRECTION ( 'NONE',  ( -1.000000000000000000, -0.000000000000000000, 0.000000000000000000 ) ) ;
#2854=ORIENTED_EDGE ( 'NONE', *, *, #26962, .F. ) ;
#2867=DIRECTION ( 'NONE',  ( 0.000000000000000000, 0.7980172272802408262, -0.6026346363792547400 ) ) ;
#2884=DIRECTION ( 'NONE',  ( -1.000000000000000000, -0.000000000000000000, 0.000000000000000000 ) ) ;
#2906=EDGE_LOOP ( 'NONE', ( #9783, #11514, #36033, #10931 ) ) ;
#2912=ORIENTED_EDGE ( 'NONE', *, *, #9169, .T. ) ;
#2917=CARTESIAN_POINT ( 'NONE',  ( 0.000000000000000000, 31.11570115861495367, 4.898994019976747438 ) ) ;
#2918=DIRECTION ( 'NONE',  ( -1.000000000000000000, 0.000000000000000000, 0.000000000000000000 ) ) ;
#2925=VERTEX_POINT ( 'NONE', #36087 ) ;
#2927=DIRECTION ( 'NONE',  ( -1.000000000000000000, 0.000000000000000000, -0.000000000000000000 ) ) ;
#2928=VECTOR ( 'NONE', #11986, 1000.000000000000000 ) ;
#2937=UNCERTAINTY_MEASURE_WITH_UNIT (LENGTH_MEASURE( 1.000000000000000082E-05 ), #7508, 'distance_accuracy_value', 'NONE');
#2940=DIRECTION ( 'NONE',  ( 1.000000000000000000, -0.000000000000000000, -0.000000000000000000 ) ) ;
#2969=DIRECTION ( 'NONE',  ( -1.000000000000000000, 0.000000000000000000, 0.000000000000000000 ) ) ;
#2979=APPLICATION_CONTEXT ( 'automotive_design' ) ;
#2983=DIRECTION ( 'NONE',  ( -1.000000000000000000, 0.000000000000000000, 0.000000000000000000 ) ) ;
#2986=AXIS2_PLACEMENT_3D ( 'NONE', #17045, #20117, #13980 ) ;
#2993=CYLINDRICAL_SURFACE ( 'NONE', #22758, 13.60000000000000142 ) ;
#3016=DIRECTION ( 'NONE',  ( 0.000000000000000000, 0.000000000000000000, 1.000000000000000000 ) ) ;
#3018=ORIENTED_EDGE ( 'NONE', *, *, #7101, .F. ) ;
#3021=CIRCLE ( 'NONE', #21210, 13.59999999999999964 ) ;
#3027=PRODUCT_DEFINITION ( 'UNKNOWN', '', #1688, #36991 ) ;
#3031=AXIS2_PLACEMENT_3D ( 'NONE', #30092, #22936, #6495 ) ;
#3033=VECTOR ( 'NONE', #34781, 1000.000000000000000 ) ;
#3039=DIRECTION ( 'NONE',  ( -1.000000000000000000, 0.000000000000000000, 0.000000000000000000 ) ) ;
#3068=VECTOR ( 'NONE', #11070, 1000.000000000000000 ) ;
#3071=DIRECTION ( 'NONE',  ( -1.000000000000000000, -0.000000000000000000, 0.000000000000000000 ) ) ;
#3073=ORIENTED_EDGE ( 'NONE', *, *, #16811, .F. ) ;
#3075=VERTEX_POINT ( 'NONE', #10561 ) ;
#3084=EDGE_CURVE ( 'NONE', #11761, #34450, #26130, .T. ) ;
#3093=VERTEX_POINT ( 'NONE', #34116 ) ;
#3095=ORIENTED_EDGE ( 'NONE', *, *, #13067, .T. ) ;
#3100=LINE ( 'NONE', #19538, #37682 ) ;
#3103=VECTOR ( 'NONE', #9563, 1000.000000000000000 ) ;
#3109=ORIENTED_EDGE ( 'NONE', *, *, #32690, .T. ) ;
#3113=VECTOR ( 'NONE', #19786, 1000.000000000000000 ) ;
#3118=CARTESIAN_POINT ( 'NONE',  ( 17.99999999999999645, 0.000000000000000000, 0.000000000000000000 ) ) ;
#3129=CIRCLE ( 'NONE', #5257, 13.60000000000000320 ) ;
#3186=ORIENTED_EDGE ( 'NONE', *, *, #42578, .F. ) ;
#3188=DIRECTION ( 'NONE',  ( 0.000000000000000000, 0.6736956436465532105, 0.7390089172206626422 ) ) ;
#3201=CIRCLE ( 'NONE', #22097, 36.00000000000000000 ) ;
#3207=EDGE_CURVE ( 'NONE', #42394, #35006, #40858, .T. ) ;
#3208=ORIENTED_EDGE ( 'NONE', *, *, #25808, .F. ) ;
#3236=VERTEX_POINT ( 'NONE', #34767 ) ;
#3259=EDGE_CURVE ( 'NONE', #26405, #39386, #36552, .T. ) ;
#3261=EDGE_LOOP ( 'NONE', ( #474, #40185, #26790, #9231 ) ) ;
#3271=EDGE_CURVE ( 'NONE', #1962, #5566, #4874, .T. ) ;
#3278=DIRECTION ( 'NONE',  ( -1.000000000000000000, 0.000000000000000000, -0.000000000000000000 ) ) ;
#3279=CARTESIAN_POINT ( 'NONE',  ( 17.99999999999999645, -21.56073507908629594, -23.57770962728587705 ) ) ;
#3283=ORIENTED_EDGE ( 'NONE', *, *, #33246, .F. ) ;
#3296=ORIENTED_EDGE ( 'NONE', *, *, #6501, .F. ) ;
#3304=FACE_OUTER_BOUND ( 'NONE', #5848, .T. ) ;
#3307=CARTESIAN_POINT ( 'NONE',  ( 17.99999999999999645, 26.29521155129873833, -17.34211205339320117 ) ) ;
#3316=DIRECTION ( 'NONE',  ( 0.000000000000000000, 0.000000000000000000, 1.000000000000000000 ) ) ;
#3317=EDGE_CURVE ( 'NONE', #2232, #40785, #4511, .T. ) ;
#3330=DIRECTION ( 'NONE',  ( -1.000000000000000000, -0.000000000000000000, -0.000000000000000000 ) ) ;
#3331=VERTEX_POINT ( 'NONE', #31935 ) ;
#3336=DIRECTION ( 'NONE',  ( 0.000000000000000000, 0.6736956436465584286, -0.7390089172206579793 ) ) ;
#3339=ORIENTED_EDGE ( 'NONE', *, *, #32072, .F. ) ;
#3340=CARTESIAN_POINT ( 'NONE',  ( 17.99999999999999645, 27.24480646643607074, 15.80846360676594564 ) ) ;
#3342=FILL_AREA_STYLE ('',( #15222 ) ) ;
#3366=CARTESIAN_POINT ( 'NONE',  ( 17.99999999999999645, -31.81777574834303124, 10.70123563439434733 ) ) ;
#3367=EDGE_LOOP ( 'NONE', ( #15088, #41066, #31064, #1389 ) ) ;
#3389=ORIENTED_EDGE ( 'NONE', *, *, #33819, .F. ) ;
#3391=CARTESIAN_POINT ( 'NONE',  ( 17.99999999999999645, 0.000000000000000000, 0.000000000000000000 ) ) ;
#3394=CARTESIAN_POINT ( 'NONE',  ( 0.000000000000000000, -16.86122981692037825, 27.13802899033285954 ) ) ;
#3406=DIRECTION ( 'NONE',  ( 0.000000000000000000, 0.000000000000000000, -1.000000000000000000 ) ) ;
#3411=EDGE_LOOP ( 'NONE', ( #37180, #20080, #41185, #14364 ) ) ;
#3413=CARTESIAN_POINT ( 'NONE',  ( 0.000000000000000000, 29.09613215194482549, 21.19941258140333673 ) ) ;
#3416=CARTESIAN_POINT ( 'NONE',  ( 0.000000000000000000, -26.29521155129861398, 17.34211205339337880 ) ) ;
#3418=CIRCLE ( 'NONE', #13214, 36.00000000000000000 ) ;
#3420=EDGE_LOOP ( 'NONE', ( #6082, #14662, #24472, #30443 ) ) ;
#3423=DIRECTION ( 'NONE',  ( 0.000000000000000000, 0.000000000000000000, 1.000000000000000000 ) ) ;
#3430=VERTEX_POINT ( 'NONE', #39512 ) ;
#3435=DIRECTION ( 'NONE',  ( -1.000000000000000000, -0.000000000000000000, -0.000000000000000000 ) ) ;
#3437=CARTESIAN_POINT ( 'NONE',  ( 17.99999999999999645, 29.09613215194512748, -21.19941258140292462 ) ) ;
#3440=VERTEX_POINT ( 'NONE', #29093 ) ;
#3451=EDGE_CURVE ( 'NONE', #29515, #32794, #15034, .T. ) ;
#3454=CARTESIAN_POINT ( 'NONE',  ( 17.99999999999999645, -21.48775762007876367, 23.64423737150130478 ) ) ;
#3466=ORIENTED_EDGE ( 'NONE', *, *, #6025, .F. ) ;
#3469=VECTOR ( 'NONE', #12213, 1000.000000000000000 ) ;
#3480=CARTESIAN_POINT ( 'NONE',  ( 0.000000000000000000, 7.220349212960450735, 35.26849241522667455 ) ) ;
#3490=CARTESIAN_POINT ( 'NONE',  ( 17.99999999999999645, -18.42432724429453472, -30.92804820216021255 ) ) ;
#3491=LINE ( 'NONE', #21402, #7303 ) ;
#3493=AXIS2_PLACEMENT_3D ( 'NONE', #25301, #31177, #14386 ) ;
#3495=VERTEX_POINT ( 'NONE', #9852 ) ;
#3510=LINE ( 'NONE', #224, #38080 ) ;
#3522=ORIENTED_EDGE ( 'NONE', *, *, #28811, .F. ) ;
#3526=DIRECTION ( 'NONE',  ( 1.000000000000000000, 0.000000000000000000, 0.000000000000000000 ) ) ;
#3536=CARTESIAN_POINT ( 'NONE',  ( 17.99999999999999645, -31.11570115861498920, 4.898994019976531611 ) ) ;
#3538=ORIENTED_EDGE ( 'NONE', *, *, #6523, .T. ) ;
#3556=DIRECTION ( 'NONE',  ( 0.000000000000000000, 0.000000000000000000, 1.000000000000000000 ) ) ;
#3560=ORIENTED_EDGE ( 'NONE', *, *, #22818, .T. ) ;
#3572=CYLINDRICAL_SURFACE ( 'NONE', #16556, 13.59999999999999964 ) ;
#3582=EDGE_CURVE ( 'NONE', #10692, #43124, #6632, .T. ) ;
#3595=DIRECTION ( 'NONE',  ( -1.000000000000000000, 0.000000000000000000, 0.000000000000000000 ) ) ;
#3613=EDGE_CURVE ( 'NONE', #7922, #13471, #24024, .T. ) ;
#3623=DIRECTION ( 'NONE',  ( -1.000000000000000000, -0.000000000000000000, 0.000000000000000000 ) ) ;
#3627=CARTESIAN_POINT ( 'NONE',  ( 17.99999999999999645, -11.49545354908957862, 29.80986809967256335 ) ) ;
#3628=ORIENTED_EDGE ( 'NONE', *, *, #14851, .T. ) ;
#3635=CARTESIAN_POINT ( 'NONE',  ( 8.999999999999998224, 13.57797752207971520, -33.34124362422459598 ) ) ;
#3679=ADVANCED_FACE ( 'NONE', ( #27110 ), #37112, .T. ) ;
#3684=AXIS2_PLACEMENT_3D ( 'NONE', #39624, #23104, #30483 ) ;
#3707=DIRECTION ( 'NONE',  ( 0.000000000000000000, 0.3612416661871537538, -0.9324722294043554793 ) ) ;
#3708=LINE ( 'NONE', #20575, #27261 ) ;
#3710=LINE ( 'NONE', #29307, #4105 ) ;
#3718=ORIENTED_EDGE ( 'NONE', *, *, #26997, .F. ) ;
#3739=DIRECTION ( 'NONE',  ( -1.000000000000000000, 0.000000000000000000, 0.000000000000000000 ) ) ;
#3743=EDGE_CURVE ( 'NONE', #25070, #38187, #21024, .T. ) ;
#3749=CYLINDRICAL_SURFACE ( 'NONE', #21754, 13.59999999999999787 ) ;
#3755=( LENGTH_UNIT ( ) NAMED_UNIT ( * ) SI_UNIT ( .MILLI., .METRE. ) );
#3762=CIRCLE ( 'NONE', #34438, 13.60000000000000320 ) ;
#3766=ORIENTED_EDGE ( 'NONE', *, *, #23093, .F. ) ;
#3784=ADVANCED_FACE ( 'NONE', ( #8315 ), #11606, .T. ) ;
#3787=AXIS2_PLACEMENT_3D ( 'NONE', #42274, #12429, #29872 ) ;
#3788=CYLINDRICAL_SURFACE ( 'NONE', #29908, 13.60000000000000142 ) ;
#3789=ORIENTED_EDGE ( 'NONE', *, *, #34107, .F. ) ;
#3796=VERTEX_POINT ( 'NONE', #34276 ) ;
#3809=AXIS2_PLACEMENT_3D ( 'NONE', #452, #6795, #3707 ) ;
#3815=CIRCLE ( 'NONE', #12224, 31.49899999999999878 ) ;
#3824=EDGE_CURVE ( 'NONE', #34733, #1839, #21880, .T. ) ;
#3838=FACE_OUTER_BOUND ( 'NONE', #13768, .T. ) ;
#3844=LINE ( 'NONE', #3635, #12298 ) ;
#3850=AXIS2_PLACEMENT_3D ( 'NONE', #40923, #11282, #31135 ) ;
#3852=CARTESIAN_POINT ( 'NONE',  ( 0.000000000000000000, 0.000000000000000000, 0.000000000000000000 ) ) ;
#3853=VERTEX_POINT ( 'NONE', #35132 ) ;
#3857=AXIS2_PLACEMENT_3D ( 'NONE', #10349, #14506, #34538 ) ;
#3858=FACE_OUTER_BOUND ( 'NONE', #37039, .T. ) ;
#3859=DIRECTION ( 'NONE',  ( -1.000000000000000000, 0.000000000000000000, 0.000000000000000000 ) ) ;
#3887=CIRCLE ( 'NONE', #17187, 36.00000000000000000 ) ;
#3907=DIRECTION ( 'NONE',  ( -1.000000000000000000, 0.000000000000000000, -0.000000000000000000 ) ) ;
#3911=VERTEX_POINT ( 'NONE', #12671 ) ;
#3917=AXIS2_PLACEMENT_3D ( 'NONE', #38975, #8254, #35285 ) ;
#3919=ORIENTED_EDGE ( 'NONE', *, *, #2209, .F. ) ;
#3921=CARTESIAN_POINT ( 'NONE',  ( 0.000000000000000000, -9.484061862024134371, 30.03730300138978038 ) ) ;
#3932=DIRECTION ( 'NONE',  ( 0.000000000000000000, 0.000000000000000000, 1.000000000000000000 ) ) ;
#3934=CYLINDRICAL_SURFACE ( 'NONE', #23792, 13.59999999999999787 ) ;
#3935=ORIENTED_EDGE ( 'NONE', *, *, #31959, .T. ) ;
#3946=DIRECTION ( 'NONE',  ( -1.000000000000000000, -0.000000000000000000, 0.000000000000000000 ) ) ;
#3949=AXIS2_PLACEMENT_3D ( 'NONE', #9626, #26214, #23383 ) ;
#3950=ORIENTED_EDGE ( 'NONE', *, *, #26322, .T. ) ;
#3960=DIRECTION ( 'NONE',  ( 0.000000000000000000, 0.000000000000000000, 1.000000000000000000 ) ) ;
#3973=DIRECTION ( 'NONE',  ( 0.000000000000000000, 0.5264321628773507289, 0.8502171357296173237 ) ) ;
#3976=LINE ( 'NONE', #26921, #37032 ) ;
#3984=ORIENTED_EDGE ( 'NONE', *, *, #4138, .T. ) ;
#3988=AXIS2_PLACEMENT_3D ( 'NONE', #17432, #4277, #17649 ) ;
#3995=EDGE_CURVE ( 'NONE', #39242, #38361, #26188, .T. ) ;
#4009=EDGE_CURVE ( 'NONE', #15839, #35006, #34521, .T. ) ;
#4010=AXIS2_PLACEMENT_3D ( 'NONE', #40396, #10087, #13393 ) ;
#4016=DIRECTION ( 'NONE',  ( 0.000000000000000000, 0.000000000000000000, 1.000000000000000000 ) ) ;
#4025=LINE ( 'NONE', #30885, #40445 ) ;
#4027=VERTEX_POINT ( 'NONE', #8959 ) ;
#4037=CARTESIAN_POINT ( 'NONE',  ( 17.99999999999999645, -25.46650492921910924, 19.29328419707777087 ) ) ;
#4041=DIRECTION ( 'NONE',  ( -1.000000000000000000, -0.000000000000000000, -0.000000000000000000 ) ) ;
#4043=EDGE_LOOP ( 'NONE', ( #5060, #25425, #21799, #9186 ) ) ;
#4047=ORIENTED_EDGE ( 'NONE', *, *, #37792, .F. ) ;
#4067=CARTESIAN_POINT ( 'NONE',  ( 0.000000000000000000, 0.000000000000000000, 0.000000000000000000 ) ) ;
#4079=DIRECTION ( 'NONE',  ( -1.000000000000000000, 0.000000000000000000, 0.000000000000000000 ) ) ;
#4096=ORIENTED_EDGE ( 'NONE', *, *, #243, .F. ) ;
#4105=VECTOR ( 'NONE', #16882, 1000.000000000000000 ) ;
#4121=DIRECTION ( 'NONE',  ( -1.000000000000000000, 0.000000000000000000, 0.000000000000000000 ) ) ;
#4122=AXIS2_PLACEMENT_3D ( 'NONE', #13531, #13110, #26407 ) ;
#4125=LINE ( 'NONE', #17055, #17625 ) ;
#4138=EDGE_CURVE ( 'NONE', #3093, #26484, #28110, .T. ) ;
#4146=FACE_OUTER_BOUND ( 'NONE', #19482, .T. ) ;
#4152=ORIENTED_EDGE ( 'NONE', *, *, #37137, .F. ) ;
#4155=ORIENTED_EDGE ( 'NONE', *, *, #32346, .F. ) ;
#4166=VECTOR ( 'NONE', #34515, 1000.000000000000000 ) ;
#4167=CARTESIAN_POINT ( 'NONE',  ( 0.000000000000000000, 0.000000000000000000, 0.000000000000000000 ) ) ;
#4182=FACE_OUTER_BOUND ( 'NONE', #13823, .T. ) ;
#4191=ADVANCED_FACE ( 'NONE', ( #148 ), #7148, .T. ) ;
#4200=AXIS2_PLACEMENT_3D ( 'NONE', #6087, #42074, #2156 ) ;
#4218=( NAMED_UNIT ( * ) PLANE_ANGLE_UNIT ( ) SI_UNIT ( $, .RADIAN. ) );
#4224=VERTEX_POINT ( 'NONE', #8996 ) ;
#4229=CIRCLE ( 'NONE', #28657, 36.00000000000000000 ) ;
#4232=DIRECTION ( 'NONE',  ( -1.000000000000000000, -0.000000000000000000, -0.000000000000000000 ) ) ;
#4234=ORIENTED_EDGE ( 'NONE', *, *, #18836, .F. ) ;
#4275=DIRECTION ( 'NONE',  ( -1.000000000000000000, 0.000000000000000000, 0.000000000000000000 ) ) ;
#4277=DIRECTION ( 'NONE',  ( -1.000000000000000000, 0.000000000000000000, 0.000000000000000000 ) ) ;
#4287=DIRECTION ( 'NONE',  ( -1.000000000000000000, -0.000000000000000000, 0.000000000000000000 ) ) ;
#4291=CYLINDRICAL_SURFACE ( 'NONE', #21145, 13.59999999999999964 ) ;
#4300=CARTESIAN_POINT ( 'NONE',  ( -10.00000000000000000, 0.000000000000000000, 0.000000000000000000 ) ) ;
#4305=DIRECTION ( 'NONE',  ( 1.000000000000000000, 0.000000000000000000, 0.000000000000000000 ) ) ;
#4309=DIRECTION ( 'NONE',  ( -1.000000000000000000, -0.000000000000000000, 0.000000000000000000 ) ) ;
#4310=EDGE_CURVE ( 'NONE', #1973, #6784, #27464, .T. ) ;
#4312=ORIENTED_EDGE ( 'NONE', *, *, #3743, .F. ) ;
#4320=ORIENTED_EDGE ( 'NONE', *, *, #4379, .T. ) ;
#4333=CYLINDRICAL_SURFACE ( 'NONE', #29572, 36.00000000000000000 ) ;
#4339=ORIENTED_EDGE ( 'NONE', *, *, #21426, .F. ) ;
#4343=CARTESIAN_POINT ( 'NONE',  ( 17.99999999999999645, 0.000000000000000000, 0.000000000000000000 ) ) ;
#4346=VECTOR ( 'NONE', #15678, 1000.000000000000000 ) ;
#4349=DIRECTION ( 'NONE',  ( 0.000000000000000000, 0.000000000000000000, 1.000000000000000000 ) ) ;
#4365=CARTESIAN_POINT ( 'NONE',  ( 9.000000000000000000, -0.6168405712484084091, -35.99471499692226928 ) ) ;
#4379=EDGE_CURVE ( 'NONE', #9315, #19383, #17461, .T. ) ;
#4381=CARTESIAN_POINT ( 'NONE',  ( 17.99999999999999645, -11.58753559615507100, 29.77419532459258278 ) ) ;
#4389=CARTESIAN_POINT ( 'NONE',  ( 17.99999999999999645, -11.58753559615507100, 29.77419532459258278 ) ) ;
#4399=DIRECTION ( 'NONE',  ( 0.000000000000000000, 0.000000000000000000, 1.000000000000000000 ) ) ;
#4430=CARTESIAN_POINT ( 'NONE',  ( 0.000000000000000000, 19.47322409167269441, 30.27859877001407796 ) ) ;
#4435=CARTESIAN_POINT ( 'NONE',  ( 8.999999999999998224, -19.47322409167291113, 30.27859877001393230 ) ) ;
#4440=DIRECTION ( 'NONE',  ( 0.000000000000000000, 0.000000000000000000, -1.000000000000000000 ) ) ;
#4444=VERTEX_POINT ( 'NONE', #6944 ) ;
#4464=CARTESIAN_POINT ( 'NONE',  ( -10.00000000000000000, 0.000000000000000000, 36.00000000000000000 ) ) ;
#4487=EDGE_CURVE ( 'NONE', #40347, #17666, #17901, .T. ) ;
#4511=CIRCLE ( 'NONE', #13583, 31.49900000000000233 ) ;
#4514=ORIENTED_EDGE ( 'NONE', *, *, #7794, .F. ) ;
#4519=CARTESIAN_POINT ( 'NONE',  ( 17.99999999999999645, -22.66088087769196235, 21.87856208362548571 ) ) ;
#4521=AXIS2_PLACEMENT_3D ( 'NONE', #41107, #37840, #27629 ) ;
#4523=CARTESIAN_POINT ( 'NONE',  ( 9.000000000000000000, 35.78425302087538995, 3.935382540232920334 ) ) ;
#4524=ORIENTED_EDGE ( 'NONE', *, *, #5048, .T. ) ;
#4527=ORIENTED_EDGE ( 'NONE', *, *, #13395, .T. ) ;
#4534=CYLINDRICAL_SURFACE ( 'NONE', #8547, 13.60000000000000142 ) ;
#4539=ORIENTED_EDGE ( 'NONE', *, *, #32834, .F. ) ;
#4554=EDGE_CURVE ( 'NONE', #42747, #28980, #32795, .T. ) ;
#4556=ORIENTED_EDGE ( 'NONE', *, *, #33158, .T. ) ;
#4560=AXIS2_PLACEMENT_3D ( 'NONE', #27887, #38103, #11744 ) ;
#4575=EDGE_LOOP ( 'NONE', ( #14731, #14161, #28611, #40835 ) ) ;
#4576=CARTESIAN_POINT ( 'NONE',  ( 0.000000000000000000, 0.000000000000000000, 0.000000000000000000 ) ) ;
#4579=CARTESIAN_POINT ( 'NONE',  ( 50.00005079999999680, 1.836970198721029589E-15, -15.00000000000000000 ) ) ;
#4611=ORIENTED_EDGE ( 'NONE', *, *, #34107, .T. ) ;
#4613=ORIENTED_EDGE ( 'NONE', *, *, #10470, .F. ) ;
#4614=FACE_OUTER_BOUND ( 'NONE', #42571, .T. ) ;
#4622=AXIS2_PLACEMENT_3D ( 'NONE', #20731, #3435, #43151 ) ;
#4637=VERTEX_POINT ( 'NONE', #16103 ) ;
#4642=DIRECTION ( 'NONE',  ( 0.000000000000000000, 0.000000000000000000, 1.000000000000000000 ) ) ;
#4662=VERTEX_POINT ( 'NONE', #12403 ) ;
#4685=ORIENTED_EDGE ( 'NONE', *, *, #30864, .F. ) ;
#4692=ORIENTED_EDGE ( 'NONE', *, *, #32430, .F. ) ;
#4696=AXIS2_PLACEMENT_3D ( 'NONE', #11904, #12114, #7953 ) ;
#4697=EDGE_CURVE ( 'NONE', #1617, #35040, #10500, .T. ) ;
#4701=EDGE_CURVE ( 'NONE', #12909, #33268, #21703, .T. ) ;
#4702=EDGE_CURVE ( 'NONE', #23443, #35253, #14011, .T. ) ;
#4704=DIRECTION ( 'NONE',  ( -1.000000000000000000, -0.000000000000000000, -0.000000000000000000 ) ) ;
#4711=VECTOR ( 'NONE', #38762, 1000.000000000000000 ) ;
#4714=VERTEX_POINT ( 'NONE', #13047 ) ;
#4718=DIRECTION ( 'NONE',  ( -1.000000000000000000, -0.000000000000000000, 0.000000000000000000 ) ) ;
#4723=CYLINDRICAL_SURFACE ( 'NONE', #15374, 13.59999999999999964 ) ;
#4728=AXIS2_PLACEMENT_3D ( 'NONE', #3279, #13579, #17078 ) ;
#4744=ORIENTED_EDGE ( 'NONE', *, *, #40432, .F. ) ;
#4754=CYLINDRICAL_SURFACE ( 'NONE', #21625, 36.00000000000000000 ) ;
#4761=DIRECTION ( 'NONE',  ( -1.000000000000000000, 0.000000000000000000, 0.000000000000000000 ) ) ;
#4762=EDGE_LOOP ( 'NONE', ( #26073, #32079, #20063, #25247 ) ) ;
#4768=AXIS2_PLACEMENT_3D ( 'NONE', #14274, #21717, #17573 ) ;
#4771=LINE ( 'NONE', #8033, #35182 ) ;
#4774=DIRECTION ( 'NONE',  ( 0.000000000000000000, 0.000000000000000000, 1.000000000000000000 ) ) ;
#4787=AXIS2_PLACEMENT_3D ( 'NONE', #41426, #24918, #17711 ) ;
#4792=CARTESIAN_POINT ( 'NONE',  ( 0.000000000000000000, -35.89808275599447285, 2.706964063997105541 ) ) ;
#4797=ORIENTED_EDGE ( 'NONE', *, *, #39627, .T. ) ;
#4798=DIRECTION ( 'NONE',  ( 0.000000000000000000, 0.7980172272802362743, 0.6026346363792606242 ) ) ;
#4800=ORIENTED_EDGE ( 'NONE', *, *, #23694, .F. ) ;
#4803=CARTESIAN_POINT ( 'NONE',  ( 17.99999999999999645, 13.57797752207971520, -33.34124362422460308 ) ) ;
#4807=VERTEX_POINT ( 'NONE', #43112 ) ;
#4830=ORIENTED_EDGE ( 'NONE', *, *, #39351, .T. ) ;
#4844=AXIS2_PLACEMENT_3D ( 'NONE', #2245, #6186, #32373 ) ;
#4853=CARTESIAN_POINT ( 'NONE',  ( 17.99999999999999645, -32.49609705003693705, -15.49205204337308217 ) ) ;
#4864=DIRECTION ( 'NONE',  ( -1.000000000000000000, -0.000000000000000000, -0.000000000000000000 ) ) ;
#4865=DIRECTION ( 'NONE',  ( -0.000000000000000000, 0.000000000000000000, 1.000000000000000000 ) ) ;
#4874=LINE ( 'NONE', #41071, #42127 ) ;
#4920=DIRECTION ( 'NONE',  ( 1.000000000000000000, 0.000000000000000000, 0.000000000000000000 ) ) ;
#4922=EDGE_CURVE ( 'NONE', #16072, #3331, #16800, .T. ) ;
#4925=CIRCLE ( 'NONE', #41825, 36.00000000000000000 ) ;
#4956=CARTESIAN_POINT ( 'NONE',  ( 17.99999999999999645, 6.007673836298523362, -35.49518073029991427 ) ) ;
#4966=AXIS2_PLACEMENT_3D ( 'NONE', #14316, #24376, #7750 ) ;
#4968=CARTESIAN_POINT ( 'NONE',  ( 0.000000000000000000, 29.03409033315599075, -12.21509719675360373 ) ) ;
#4972=CARTESIAN_POINT ( 'NONE',  ( 17.99999999999999645, 31.80866420683995699, -2.997093558040963224 ) ) ;
#4975=VERTEX_POINT ( 'NONE', #8204 ) ;
#5000=EDGE_CURVE ( 'NONE', #41773, #9315, #20318, .T. ) ;
#5002=LINE ( 'NONE', #28146, #3469 ) ;
#5017=DIRECTION ( 'NONE',  ( -1.000000000000000000, 0.000000000000000000, 0.000000000000000000 ) ) ;
#5018=CARTESIAN_POINT ( 'NONE',  ( 17.99999999999999645, 0.000000000000000000, 0.000000000000000000 ) ) ;
#5033=CARTESIAN_POINT ( 'NONE',  ( 0.000000000000000000, 30.71634675606066267, -8.790889055186230649 ) ) ;
#5039=ORIENTED_EDGE ( 'NONE', *, *, #35442, .T. ) ;
#5044=EDGE_CURVE ( 'NONE', #28643, #12333, #31336, .T. ) ;
#5048=EDGE_CURVE ( 'NONE', #35040, #20538, #14769, .T. ) ;
#5050=ORIENTED_EDGE ( 'NONE', *, *, #16705, .F. ) ;
#5060=ORIENTED_EDGE ( 'NONE', *, *, #7410, .T. ) ;
#5067=DIRECTION ( 'NONE',  ( 0.000000000000000000, 0.000000000000000000, 1.000000000000000000 ) ) ;
#5076=DIRECTION ( 'NONE',  ( -1.000000000000000000, 0.000000000000000000, 0.000000000000000000 ) ) ;
#5090=ORIENTED_EDGE ( 'NONE', *, *, #14851, .F. ) ;
#5104=CIRCLE ( 'NONE', #39926, 13.59999999999999964 ) ;
#5114=ORIENTED_EDGE ( 'NONE', *, *, #16195, .T. ) ;
#5128=DIRECTION ( 'NONE',  ( 1.000000000000000000, -0.000000000000000000, 0.000000000000000000 ) ) ;
#5135=VECTOR ( 'NONE', #2426, 1000.000000000000000 ) ;
#5153=CYLINDRICAL_SURFACE ( 'NONE', #4560, 36.00000000000000000 ) ;
#5156=CLOSED_SHELL ( 'NONE', ( #11390, #17769, #21411, #31700, #36108, #22905, #2007, #37370, #40041, #30386, #39837, #29411, #12008, #42611, #38116, #7814, #20253, #29250, #5489, #19636, #41260, #15535, #23935, #41545, #22012, #37144, #13377, #20211, #22616, #31401, #29732, #21008, #21220, #4191, #2051, #6737, #42483, #13350, #33730, #36344, #11227, #42732, #32296, #41762, #14615, #14448, #38735, #17674, #8738, #19714, #28870, #19536, #3679, #31342, #21773, #31146, #5969, #24793, #13025, #8925, #43066, #19175, #33510, #7074, #126, #12207, #8002, #30302, #22157, #21191, #13109, #3784, #34152, #32513, #2176, #37703, #6145, #24192, #35136, #28420, #20462, #13511, #31773, #9200, #9381, #41475, #10259, #19463, #42244, #40388, #34545, #17373, #28529, #16196, #32885, #22733, #38217, #32371, #20389, #29793, #15482, #1311, #1902, #43133, #23457, #27821, #13000, #13216, #30911, #39086, #1911, #24553, #15555, #24320, #131, #10903, #18397, #15608, #19480, #16225, #1429, #24976, #11923, #11975, #36442, #12709, #10713, #34595, #38250, #22215, #36527, #37608, #36612, #29899, #15656, #20085, #35002, #6419, #25106, #22282, #10729, #37500, #41173, #32010, #41330 ) ) ;
#5192=AXIS2_PLACEMENT_3D ( 'NONE', #38593, #25344, #32074 ) ;
#5197=ORIENTED_EDGE ( 'NONE', *, *, #26203, .F. ) ;
#5199=CIRCLE ( 'NONE', #28889, 13.59999999999999964 ) ;
#5210=CARTESIAN_POINT ( 'NONE',  ( 17.99999999999999645, -14.84191762912334767, 27.78316904333121684 ) ) ;
#5220=VECTOR ( 'NONE', #9196, 1000.000000000000000 ) ;
#5222=ORIENTED_EDGE ( 'NONE', *, *, #28811, .T. ) ;
#5230=FACE_OUTER_BOUND ( 'NONE', #2906, .T. ) ;
#5233=DIRECTION ( 'NONE',  ( -1.000000000000000000, 0.000000000000000000, -0.000000000000000000 ) ) ;
#5235=ORIENTED_EDGE ( 'NONE', *, *, #35877, .F. ) ;
#5249=DIRECTION ( 'NONE',  ( -1.000000000000000000, -0.000000000000000000, -0.000000000000000000 ) ) ;
#5253=EDGE_LOOP ( 'NONE', ( #7674, #38000, #38428, #36957 ) ) ;
#5257=AXIS2_PLACEMENT_3D ( 'NONE', #37535, #34258, #17725 ) ;
#5258=CIRCLE ( 'NONE', #29657, 13.60000000000000142 ) ;
#5269=CARTESIAN_POINT ( 'NONE',  ( 17.99999999999999645, 14.84191762912315049, 27.78316904333131276 ) ) ;
#5271=ORIENTED_EDGE ( 'NONE', *, *, #4009, .T. ) ;
#5272=EDGE_CURVE ( 'NONE', #29573, #9315, #9128, .T. ) ;
#5274=DIRECTION ( 'NONE',  ( -1.000000000000000000, -0.000000000000000000, -0.000000000000000000 ) ) ;
#5283=CIRCLE ( 'NONE', #9447, 36.00000000000000000 ) ;
#5290=( GEOMETRIC_REPRESENTATION_CONTEXT ( 3 ) GLOBAL_UNCERTAINTY_ASSIGNED_CONTEXT ( ( #2937 ) ) GLOBAL_UNIT_ASSIGNED_CONTEXT ( ( #7508, #4218, #37169 ) ) REPRESENTATION_CONTEXT ( 'NONE', 'WORKASPACE' ) );
#5294=CARTESIAN_POINT ( 'NONE',  ( -10.00000000000000000, 0.000000000000000000, 0.000000000000000000 ) ) ;
#5295=DIRECTION ( 'NONE',  ( 0.000000000000000000, 0.000000000000000000, 1.000000000000000000 ) ) ;
#5306=ORIENTED_EDGE ( 'NONE', *, *, #35678, .T. ) ;
#5335=VERTEX_POINT ( 'NONE', #3340 ) ;
#5346=ORIENTED_EDGE ( 'NONE', *, *, #25625, .T. ) ;
#5352=DIRECTION ( 'NONE',  ( 0.000000000000000000, 0.000000000000000000, 1.000000000000000000 ) ) ;
#5356=AXIS2_PLACEMENT_3D ( 'NONE', #32571, #22160, #9435 ) ;
#5364=EDGE_CURVE ( 'NONE', #14556, #31789, #13822, .T. ) ;
#5368=EDGE_CURVE ( 'NONE', #10216, #28707, #33897, .T. ) ;
#5384=LINE ( 'NONE', #2088, #40751 ) ;
#5395=AXIS2_PLACEMENT_3D ( 'NONE', #10962, #21235, #21464 ) ;
#5403=CIRCLE ( 'NONE', #6754, 13.60000000000000142 ) ;
#5405=CARTESIAN_POINT ( 'NONE',  ( 9.000000000000000000, -29.09613215194497826, 21.19941258140312002 ) ) ;
#5424=ORIENTED_EDGE ( 'NONE', *, *, #26015, .F. ) ;
#5425=CIRCLE ( 'NONE', #20105, 31.49899999999999878 ) ;
#5436=FACE_OUTER_BOUND ( 'NONE', #5253, .T. ) ;
#5459=ORIENTED_EDGE ( 'NONE', *, *, #16655, .F. ) ;
#5489=ADVANCED_FACE ( 'NONE', ( #24109 ), #24995, .T. ) ;
#5496=CARTESIAN_POINT ( 'NONE',  ( 17.99999999999999645, -29.09613215194498181, 21.19941258140312357 ) ) ;
#5507=AXIS2_PLACEMENT_3D ( 'NONE', #30612, #30391, #26685 ) ;
#5548=ORIENTED_EDGE ( 'NONE', *, *, #4554, .T. ) ;
#5561=AXIS2_PLACEMENT_3D ( 'NONE', #41749, #12529, #9230 ) ;
#5566=VERTEX_POINT ( 'NONE', #18669 ) ;
#5582=DIRECTION ( 'NONE',  ( 0.000000000000000000, 0.000000000000000000, 1.000000000000000000 ) ) ;
#5602=CARTESIAN_POINT ( 'NONE',  ( 0.000000000000000000, 0.000000000000000000, 0.000000000000000000 ) ) ;
#5608=CYLINDRICAL_SURFACE ( 'NONE', #18137, 31.49899999999999878 ) ;
#5647=VERTEX_POINT ( 'NONE', #8783 ) ;
#5654=DIRECTION ( 'NONE',  ( 0.000000000000000000, -0.3612416661871405976, -0.9324722294043605864 ) ) ;
#5655=EDGE_LOOP ( 'NONE', ( #37834, #24385, #24160, #33284 ) ) ;
#5658=EDGE_CURVE ( 'NONE', #33813, #21218, #13102, .T. ) ;
#5660=CARTESIAN_POINT ( 'NONE',  ( 0.000000000000000000, 0.000000000000000000, 0.000000000000000000 ) ) ;
#5662=CARTESIAN_POINT ( 'NONE',  ( 0.000000000000000000, -31.81777574834308098, 2.898764365605205562 ) ) ;
#5679=AXIS2_PLACEMENT_3D ( 'NONE', #16396, #39257, #28498 ) ;
#5683=DIRECTION ( 'NONE',  ( 0.000000000000000000, 0.000000000000000000, -1.000000000000000000 ) ) ;
#5688=EDGE_LOOP ( 'NONE', ( #6430, #7483, #28678, #24186 ) ) ;
#5692=DIRECTION ( 'NONE',  ( -1.000000000000000000, 0.000000000000000000, 0.000000000000000000 ) ) ;
#5701=AXIS2_PLACEMENT_3D ( 'NONE', #26543, #36544, #29835 ) ;
#5706=EDGE_CURVE ( 'NONE', #37148, #27491, #8195, .T. ) ;
#5711=CIRCLE ( 'NONE', #21817, 36.00000000000000000 ) ;
#5712=CARTESIAN_POINT ( 'NONE',  ( 0.000000000000000000, -22.66088087769196235, 21.87856208362548571 ) ) ;
#5729=VECTOR ( 'NONE', #32575, 1000.000000000000000 ) ;
#5734=CIRCLE ( 'NONE', #30145, 36.00000000000000000 ) ;
#5736=EDGE_CURVE ( 'NONE', #13228, #40785, #13367, .T. ) ;
#5749=FACE_OUTER_BOUND ( 'NONE', #18210, .T. ) ;
#5751=VERTEX_POINT ( 'NONE', #13806 ) ;
#5758=CARTESIAN_POINT ( 'NONE',  ( 17.99999999999999645, -34.45183346761128718, -10.44371441202691742 ) ) ;
#5776=CARTESIAN_POINT ( 'NONE',  ( 8.999999999999998224, 32.49609705003704363, 15.49205204337285835 ) ) ;
#5792=DIRECTION ( 'NONE',  ( 0.000000000000000000, 0.3612416661871538093, -0.9324722294043554793 ) ) ;
#5797=MECHANICAL_DESIGN_GEOMETRIC_PRESENTATION_REPRESENTATION('',(#10670),#35049);
#5814=DIRECTION ( 'NONE',  ( 0.000000000000000000, 0.000000000000000000, 1.000000000000000000 ) ) ;
#5816=AXIS2_PLACEMENT_3D ( 'NONE', #1379, #7714, #25004 ) ;
#5834=CIRCLE ( 'NONE', #41358, 31.49899999999999878 ) ;
#5840=CIRCLE ( 'NONE', #1634, 13.59999999999999787 ) ;
#5847=DIRECTION ( 'NONE',  ( 0.000000000000000000, 0.000000000000000000, 1.000000000000000000 ) ) ;
#5848=EDGE_LOOP ( 'NONE', ( #31544, #20693, #103, #43110 ) ) ;
#5860=CYLINDRICAL_SURFACE ( 'NONE', #35806, 31.49899999999999878 ) ;
#5883=ORIENTED_EDGE ( 'NONE', *, *, #34794, .T. ) ;
#5897=CARTESIAN_POINT ( 'NONE',  ( 17.99999999999999645, 21.56073507908645936, 23.57770962728572428 ) ) ;
#5898=DIRECTION ( 'NONE',  ( 0.000000000000000000, -0.1837495178165569620, -0.9829730996839042279 ) ) ;
#5904=CARTESIAN_POINT ( 'NONE',  ( 17.99999999999999645, -9.484061862024134371, 30.03730300138978038 ) ) ;
#5917=CARTESIAN_POINT ( 'NONE',  ( 0.000000000000000000, 0.000000000000000000, 0.000000000000000000 ) ) ;
#5930=DIRECTION ( 'NONE',  ( -1.000000000000000000, 0.000000000000000000, -0.000000000000000000 ) ) ;
#5950=CARTESIAN_POINT ( 'NONE',  ( 17.99999999999999645, -6.007673836298256020, 35.49518073029995691 ) ) ;
#5961=EDGE_CURVE ( 'NONE', #15922, #21082, #1320, .T. ) ;
#5969=ADVANCED_FACE ( 'NONE', ( #15102 ), #25977, .T. ) ;
#5989=DIRECTION ( 'NONE',  ( -1.000000000000000000, -0.000000000000000000, -0.000000000000000000 ) ) ;
#6000=LINE ( 'NONE', #19354, #10165 ) ;
#6007=DIRECTION ( 'NONE',  ( 0.000000000000000000, 0.000000000000000000, 1.000000000000000000 ) ) ;
#6016=LINE ( 'NONE', #13023, #11246 ) ;
#6017=FACE_OUTER_BOUND ( 'NONE', #29939, .T. ) ;
#6025=EDGE_CURVE ( 'NONE', #27337, #1059, #4925, .T. ) ;
#6030=DIRECTION ( 'NONE',  ( 0.000000000000000000, -6.982962677686266711E-15, 1.000000000000000000 ) ) ;
#6046=DIRECTION ( 'NONE',  ( -1.000000000000000000, 0.000000000000000000, 0.000000000000000000 ) ) ;
#6055=DIRECTION ( 'NONE',  ( 0.000000000000000000, -0.8951632913550570114, -0.4457383557765489668 ) ) ;
#6067=VECTOR ( 'NONE', #37399, 1000.000000000000000 ) ;
#6082=ORIENTED_EDGE ( 'NONE', *, *, #31959, .F. ) ;
#6084=ORIENTED_EDGE ( 'NONE', *, *, #40844, .T. ) ;
#6087=CARTESIAN_POINT ( 'NONE',  ( 17.99999999999999645, 0.000000000000000000, 0.000000000000000000 ) ) ;
#6095=AXIS2_PLACEMENT_3D ( 'NONE', #4343, #36872, #20338 ) ;
#6102=CYLINDRICAL_SURFACE ( 'NONE', #34159, 13.59999999999999964 ) ;
#6138=DIRECTION ( 'NONE',  ( 1.000000000000000000, 0.000000000000000000, 0.000000000000000000 ) ) ;
#6145=ADVANCED_FACE ( 'NONE', ( #10011 ), #6102, .T. ) ;
#6147=DIRECTION ( 'NONE',  ( -1.000000000000000000, -0.000000000000000000, 0.000000000000000000 ) ) ;
#6163=ORIENTED_EDGE ( 'NONE', *, *, #319, .T. ) ;
#6169=VERTEX_POINT ( 'NONE', #39883 ) ;
#6172=CARTESIAN_POINT ( 'NONE',  ( 17.99999999999999645, 0.000000000000000000, 0.000000000000000000 ) ) ;
#6175=VECTOR ( 'NONE', #4287, 1000.000000000000000 ) ;
#6180=CARTESIAN_POINT ( 'NONE',  ( 0.000000000000000000, -29.09613215194468694, -21.19941258140352858 ) ) ;
#6186=DIRECTION ( 'NONE',  ( -1.000000000000000000, -0.000000000000000000, 0.000000000000000000 ) ) ;
#6187=ORIENTED_EDGE ( 'NONE', *, *, #7719, .F. ) ;
#6192=EDGE_CURVE ( 'NONE', #38171, #51, #33574, .T. ) ;
#6206=CIRCLE ( 'NONE', #20176, 31.49899999999999523 ) ;
#6231=CARTESIAN_POINT ( 'NONE',  ( 17.99999999999999645, -31.48608500567871005, 0.9019157472703476230 ) ) ;
#6236=ORIENTED_EDGE ( 'NONE', *, *, #26203, .T. ) ;
#6238=CIRCLE ( 'NONE', #4844, 13.59999999999999787 ) ;
#6241=EDGE_CURVE ( 'NONE', #18067, #30185, #19874, .T. ) ;
#6250=DIRECTION ( 'NONE',  ( -1.000000000000000000, 0.000000000000000000, -0.000000000000000000 ) ) ;
#6266=ORIENTED_EDGE ( 'NONE', *, *, #8276, .T. ) ;
#6275=EDGE_CURVE ( 'NONE', #37206, #17989, #18928, .T. ) ;
#6278=CYLINDRICAL_SURFACE ( 'NONE', #42763, 31.49899999999999878 ) ;
#6284=AXIS2_PLACEMENT_3D ( 'NONE', #42309, #8728, #2369 ) ;
#6285=CARTESIAN_POINT ( 'NONE',  ( 17.99999999999999645, -29.68570942776464960, -10.53307442156965656 ) ) ;
#6292=ORIENTED_EDGE ( 'NONE', *, *, #20083, .T. ) ;
#6293=CARTESIAN_POINT ( 'NONE',  ( 8.999999999999998224, 32.49609705003727100, -15.49205204337239827 ) ) ;
#6294=AXIS2_PLACEMENT_3D ( 'NONE', #24809, #37628, #7748 ) ;
#6306=EDGE_LOOP ( 'NONE', ( #20074, #8360, #26279, #12684 ) ) ;
#6308=CARTESIAN_POINT ( 'NONE',  ( 17.99999999999999645, 29.68570942776486987, -10.53307442156903662 ) ) ;
#6314=EDGE_CURVE ( 'NONE', #4637, #18138, #11931, .T. ) ;
#6323=CARTESIAN_POINT ( 'NONE',  ( 0.000000000000000000, 0.000000000000000000, 0.000000000000000000 ) ) ;
#6325=AXIS2_PLACEMENT_3D ( 'NONE', #17243, #41382, #11106 ) ;
#6341=CARTESIAN_POINT ( 'NONE',  ( 17.99999999999999645, 22.66088087769211157, -21.87856208362532939 ) ) ;
#6346=DIRECTION ( 'NONE',  ( 0.000000000000000000, 0.000000000000000000, -1.000000000000000000 ) ) ;
#6358=ORIENTED_EDGE ( 'NONE', *, *, #39652, .T. ) ;
#6365=EDGE_CURVE ( 'NONE', #7922, #11917, #40531, .T. ) ;
#6375=CYLINDRICAL_SURFACE ( 'NONE', #36366, 15.00000000000000000 ) ;
#6403=VERTEX_POINT ( 'NONE', #37059 ) ;
#6409=DIRECTION ( 'NONE',  ( -1.000000000000000000, 0.000000000000000000, 0.000000000000000000 ) ) ;
#6412=CARTESIAN_POINT ( 'NONE',  ( 0.000000000000000000, -35.78425302087541127, 3.935382540232673865 ) ) ;
#6419=ADVANCED_FACE ( 'NONE', ( #37916 ), #36300, .T. ) ;
#6430=ORIENTED_EDGE ( 'NONE', *, *, #38552, .T. ) ;
#6436=LINE ( 'NONE', #3366, #3113 ) ;
#6437=ORIENTED_EDGE ( 'NONE', *, *, #41282, .T. ) ;
#6449=CARTESIAN_POINT ( 'NONE',  ( 17.99999999999999645, 31.81777574834305966, 10.70123563439457293 ) ) ;
#6456=DIRECTION ( 'NONE',  ( 0.000000000000000000, -0.3612416661871404866, -0.9324722294043605864 ) ) ;
#6477=AXIS2_PLACEMENT_3D ( 'NONE', #32874, #40038, #327 ) ;
#6479=DIRECTION ( 'NONE',  ( -1.000000000000000000, 0.000000000000000000, 0.000000000000000000 ) ) ;
#6480=DIRECTION ( 'NONE',  ( -1.000000000000000000, 0.000000000000000000, 0.000000000000000000 ) ) ;
#6495=DIRECTION ( 'NONE',  ( 0.000000000000000000, -0.7980172272802321665, -0.6026346363792660643 ) ) ;
#6501=EDGE_CURVE ( 'NONE', #16404, #24756, #26958, .T. ) ;
#6523=EDGE_CURVE ( 'NONE', #35253, #41289, #42837, .T. ) ;
#6536=CYLINDRICAL_SURFACE ( 'NONE', #34750, 13.60000000000000142 ) ;
#6541=CIRCLE ( 'NONE', #5192, 13.60000000000000142 ) ;
#6549=EDGE_CURVE ( 'NONE', #1059, #4637, #19346, .T. ) ;
#6552=AXIS2_PLACEMENT_3D ( 'NONE', #20051, #13265, #17638 ) ;
#6554=CARTESIAN_POINT ( 'NONE',  ( 17.99999999999999645, -25.52601536738579213, -19.21447964122724272 ) ) ;
#6558=DIRECTION ( 'NONE',  ( -1.000000000000000000, 0.000000000000000000, -0.000000000000000000 ) ) ;
#6588=ORIENTED_EDGE ( 'NONE', *, *, #23595, .F. ) ;
#6599=VERTEX_POINT ( 'NONE', #24116 ) ;
#6622=DIRECTION ( 'NONE',  ( 0.000000000000000000, 0.000000000000000000, 1.000000000000000000 ) ) ;
#6631=CARTESIAN_POINT ( 'NONE',  ( 0.000000000000000000, -19.69434969228090893, 24.58291258574042004 ) ) ;
#6632=CIRCLE ( 'NONE', #3809, 31.49899999999999523 ) ;
#6640=EDGE_CURVE ( 'NONE', #1957, #35650, #24184, .T. ) ;
#6643=CARTESIAN_POINT ( 'NONE',  ( 17.99999999999999645, 0.000000000000000000, 0.000000000000000000 ) ) ;
#6651=CARTESIAN_POINT ( 'NONE',  ( 17.99999999999999645, 0.000000000000000000, 0.000000000000000000 ) ) ;
#6653=ORIENTED_EDGE ( 'NONE', *, *, #11316, .F. ) ;
#6664=ORIENTED_EDGE ( 'NONE', *, *, #26349, .F. ) ;
#6667=FACE_OUTER_BOUND ( 'NONE', #34063, .T. ) ;
#6688=EDGE_LOOP ( 'NONE', ( #27743, #22177, #33528, #21853 ) ) ;
#6694=VERTEX_POINT ( 'NONE', #7061 ) ;
#6704=DIRECTION ( 'NONE',  ( -1.000000000000000000, 0.000000000000000000, -0.000000000000000000 ) ) ;
#6706=CARTESIAN_POINT ( 'NONE',  ( 17.99999999999999645, -27.24480646643597126, -15.80846360676612861 ) ) ;
#6708=VECTOR ( 'NONE', #17021, 1000.000000000000000 ) ;
#6709=DIRECTION ( 'NONE',  ( 0.000000000000000000, 0.000000000000000000, 1.000000000000000000 ) ) ;
#6729=CARTESIAN_POINT ( 'NONE',  ( 17.99999999999999645, 7.220349212960956997, -35.26849241522656797 ) ) ;
#6732=CARTESIAN_POINT ( 'NONE',  ( 0.000000000000000000, 19.47322409167312429, -30.27859877001379374 ) ) ;
#6736=CARTESIAN_POINT ( 'NONE',  ( 17.99999999999999645, -3.803237743091689715, -31.26855263151018960 ) ) ;
#6737=ADVANCED_FACE ( 'NONE', ( #11880 ), #17795, .T. ) ;
#6754=AXIS2_PLACEMENT_3D ( 'NONE', #30845, #34106, #33251 ) ;
#6769=EDGE_LOOP ( 'NONE', ( #17557, #40124, #36540, #28473 ) ) ;
#6784=VERTEX_POINT ( 'NONE', #34543 ) ;
#6788=EDGE_CURVE ( 'NONE', #4027, #12125, #24672, .T. ) ;
#6792=VERTEX_POINT ( 'NONE', #21727 ) ;
#6795=DIRECTION ( 'NONE',  ( -1.000000000000000000, 0.000000000000000000, -0.000000000000000000 ) ) ;
#6797=AXIS2_PLACEMENT_3D ( 'NONE', #12535, #29119, #42392 ) ;
#6807=VERTEX_POINT ( 'NONE', #28247 ) ;
#6817=FACE_OUTER_BOUND ( 'NONE', #22890, .T. ) ;
#6831=ORIENTED_EDGE ( 'NONE', *, *, #11091, .F. ) ;
#6836=LINE ( 'NONE', #20194, #28722 ) ;
#6843=AXIS2_PLACEMENT_3D ( 'NONE', #9619, #5692, #19678 ) ;
#6860=EDGE_CURVE ( 'NONE', #40285, #19624, #23981, .T. ) ;
#6865=CARTESIAN_POINT ( 'NONE',  ( 17.99999999999999645, 29.09613215194482905, 21.19941258140334028 ) ) ;
#6907=EDGE_CURVE ( 'NONE', #42608, #27860, #26025, .T. ) ;
#6908=EDGE_CURVE ( 'NONE', #10741, #15182, #10710, .T. ) ;
#6911=EDGE_LOOP ( 'NONE', ( #42117, #8591, #19085, #19729 ) ) ;
#6912=ORIENTED_EDGE ( 'NONE', *, *, #33271, .T. ) ;
#6920=CARTESIAN_POINT ( 'NONE',  ( 17.99999999999999645, 31.81777574834305966, -2.898764365605425830 ) ) ;
#6928=EDGE_CURVE ( 'NONE', #21082, #26674, #32291, .T. ) ;
#6929=CARTESIAN_POINT ( 'NONE',  ( 17.99999999999999645, -5.822172717930031993, -31.41458249383147106 ) ) ;
#6934=CARTESIAN_POINT ( 'NONE',  ( 17.99999999999999645, -31.81777574834303124, -2.898764365605651427 ) ) ;
#6941=DIRECTION ( 'NONE',  ( -1.000000000000000000, 0.000000000000000000, 0.000000000000000000 ) ) ;
#6944=CARTESIAN_POINT ( 'NONE',  ( 17.99999999999999645, 26.29521155129873833, -17.34211205339320117 ) ) ;
#6946=CIRCLE ( 'NONE', #36904, 31.49900000000000233 ) ;
#6969=EDGE_LOOP ( 'NONE', ( #40720, #11249, #43014, #20666 ) ) ;
#6980=ORIENTED_EDGE ( 'NONE', *, *, #17101, .F. ) ;
#6981=CYLINDRICAL_SURFACE ( 'NONE', #6095, 31.49899999999999878 ) ;
#6984=CARTESIAN_POINT ( 'NONE',  ( 17.99999999999999645, 11.49545354908936545, 29.80986809967263085 ) ) ;
#6986=ORIENTED_EDGE ( 'NONE', *, *, #16651, .F. ) ;
#6994=DIRECTION ( 'NONE',  ( 0.000000000000000000, -0.7980172272802321665, -0.6026346363792660643 ) ) ;
#6998=DIRECTION ( 'NONE',  ( 0.000000000000000000, 0.000000000000000000, 1.000000000000000000 ) ) ;
#7011=AXIS2_PLACEMENT_3D ( 'NONE', #23975, #27024, #3423 ) ;
#7021=VERTEX_POINT ( 'NONE', #22563 ) ;
#7044=VERTEX_POINT ( 'NONE', #13813 ) ;
#7045=DIRECTION ( 'NONE',  ( -1.000000000000000000, 0.000000000000000000, -0.000000000000000000 ) ) ;
#7058=ORIENTED_EDGE ( 'NONE', *, *, #29466, .F. ) ;
#7059=DIRECTION ( 'NONE',  ( -1.000000000000000000, -0.000000000000000000, 0.000000000000000000 ) ) ;
#7061=CARTESIAN_POINT ( 'NONE',  ( 17.99999999999999645, -35.89808275599443732, -2.706964063997608694 ) ) ;
#7064=EDGE_CURVE ( 'NONE', #11917, #17450, #27114, .T. ) ;
#7074=ADVANCED_FACE ( 'NONE', ( #16880 ), #3934, .T. ) ;
#7078=AXIS2_PLACEMENT_3D ( 'NONE', #20404, #11004, #27578 ) ;
#7079=CARTESIAN_POINT ( 'NONE',  ( 0.000000000000000000, 0.000000000000000000, 0.000000000000000000 ) ) ;
#7088=DIRECTION ( 'NONE',  ( 0.000000000000000000, -0.7980172272802321665, -0.6026346363792661753 ) ) ;
#7101=EDGE_CURVE ( 'NONE', #19749, #29952, #3708, .T. ) ;
#7109=EDGE_LOOP ( 'NONE', ( #41018, #21984, #19106, #8766 ) ) ;
#7121=DIRECTION ( 'NONE',  ( 1.000000000000000000, 0.000000000000000000, 0.000000000000000000 ) ) ;
#7133=CARTESIAN_POINT ( 'NONE',  ( 17.99999999999999645, -21.48775762007842260, -23.64423737150161031 ) ) ;
#7139=CARTESIAN_POINT ( 'NONE',  ( 0.000000000000000000, 35.78425302087543969, -3.935382540232422510 ) ) ;
#7145=EDGE_LOOP ( 'NONE', ( #35469, #3560, #17875, #32543 ) ) ;
#7147=ORIENTED_EDGE ( 'NONE', *, *, #26349, .T. ) ;
#7148=CYLINDRICAL_SURFACE ( 'NONE', #4622, 36.00000000000000000 ) ;
#7151=DIRECTION ( 'NONE',  ( 0.000000000000000000, -6.887872625202028030E-15, 1.000000000000000000 ) ) ;
#7154=LINE ( 'NONE', #4523, #13033 ) ;
#7174=CARTESIAN_POINT ( 'NONE',  ( 0.000000000000000000, 0.000000000000000000, 0.000000000000000000 ) ) ;
#7176=ORIENTED_EDGE ( 'NONE', *, *, #8988, .T. ) ;
#7199=EDGE_CURVE ( 'NONE', #42739, #26154, #19350, .T. ) ;
#7200=DIRECTION ( 'NONE',  ( 0.000000000000000000, -0.9618256431728219313, 0.2736629900720728981 ) ) ;
#7205=FACE_OUTER_BOUND ( 'NONE', #20226, .T. ) ;
#7218=CARTESIAN_POINT ( 'NONE',  ( 17.99999999999999645, 21.48775762007893420, -23.64423737150114135 ) ) ;
#7226=AXIS2_PLACEMENT_3D ( 'NONE', #10959, #24290, #29794 ) ;
#7234=CARTESIAN_POINT ( 'NONE',  ( 17.99999999999999645, -28.57802095670076881, -14.28532136906702732 ) ) ;
#7265=ORIENTED_EDGE ( 'NONE', *, *, #356, .F. ) ;
#7287=EDGE_CURVE ( 'NONE', #5566, #26405, #42579, .T. ) ;
#7295=AXIS2_PLACEMENT_3D ( 'NONE', #9526, #2522, #29187 ) ;
#7299=AXIS2_PLACEMENT_3D ( 'NONE', #16572, #2969, #9766 ) ;
#7303=VECTOR ( 'NONE', #3278, 1000.000000000000000 ) ;
#7311=DIRECTION ( 'NONE',  ( -1.000000000000000000, 0.000000000000000000, 0.000000000000000000 ) ) ;
#7323=DIRECTION ( 'NONE',  ( 0.000000000000000000, 0.000000000000000000, -1.000000000000000000 ) ) ;
#7344=CARTESIAN_POINT ( 'NONE',  ( 17.99999999999999645, -30.78424799127072120, 6.672111855473074726 ) ) ;
#7352=DIRECTION ( 'NONE',  ( -1.000000000000000000, 0.000000000000000000, -0.000000000000000000 ) ) ;
#7359=ORIENTED_EDGE ( 'NONE', *, *, #2534, .T. ) ;
#7363=EDGE_LOOP ( 'NONE', ( #42998, #4797, #35638, #24445 ) ) ;
#7364=AXIS2_PLACEMENT_3D ( 'NONE', #42941, #29894, #9999 ) ;
#7375=AXIS2_PLACEMENT_3D ( 'NONE', #24591, #3859, #17245 ) ;
#7376=CARTESIAN_POINT ( 'NONE',  ( 9.000000000000000000, -7.220349212960696761, 35.26849241522661771 ) ) ;
#7399=EDGE_CURVE ( 'NONE', #33710, #23971, #16780, .T. ) ;
#7410=EDGE_CURVE ( 'NONE', #24289, #38409, #13124, .T. ) ;
#7419=AXIS2_PLACEMENT_3D ( 'NONE', #13868, #20864, #20208 ) ;
#7433=CARTESIAN_POINT ( 'NONE',  ( 0.000000000000000000, 21.56073507908645936, 23.57770962728572428 ) ) ;
#7435=CARTESIAN_POINT ( 'NONE',  ( 17.99999999999999645, 11.58753559615485251, 29.77419532459266449 ) ) ;
#7436=DIRECTION ( 'NONE',  ( 1.000000000000000000, 0.000000000000000000, -0.000000000000000000 ) ) ;
#7445=VECTOR ( 'NONE', #12127, 1000.000000000000000 ) ;
#7476=EDGE_CURVE ( 'NONE', #28925, #7021, #22358, .T. ) ;
#7483=ORIENTED_EDGE ( 'NONE', *, *, #21302, .T. ) ;
#7494=CIRCLE ( 'NONE', #9590, 31.49899999999999523 ) ;
#7498=AXIS2_PLACEMENT_3D ( 'NONE', #23065, #30223, #40230 ) ;
#7505=ORIENTED_EDGE ( 'NONE', *, *, #26558, .F. ) ;
#7508=( LENGTH_UNIT ( ) NAMED_UNIT ( * ) SI_UNIT ( .MILLI., .METRE. ) );
#7529=AXIS2_PLACEMENT_3D ( 'NONE', #9899, #17364, #13419 ) ;
#7532=FACE_OUTER_BOUND ( 'NONE', #14000, .T. ) ;
#7540=ORIENTED_EDGE ( 'NONE', *, *, #11703, .F. ) ;
#7549=EDGE_CURVE ( 'NONE', #2925, #21218, #40765, .T. ) ;
#7572=CARTESIAN_POINT ( 'NONE',  ( 17.99999999999999645, -7.749090474611287860, -30.53094492177221397 ) ) ;
#7581=ORIENTED_EDGE ( 'NONE', *, *, #7101, .T. ) ;
#7592=ORIENTED_EDGE ( 'NONE', *, *, #29530, .T. ) ;
#7600=ORIENTED_EDGE ( 'NONE', *, *, #33271, .F. ) ;
#7620=ORIENTED_EDGE ( 'NONE', *, *, #10110, .F. ) ;
#7634=ORIENTED_EDGE ( 'NONE', *, *, #39351, .F. ) ;
#7638=FACE_OUTER_BOUND ( 'NONE', #36973, .T. ) ;
#7656=CARTESIAN_POINT ( 'NONE',  ( 0.000000000000000000, -31.11570115861491814, -4.898994019976963266 ) ) ;
#7658=ORIENTED_EDGE ( 'NONE', *, *, #32723, .T. ) ;
#7670=AXIS2_PLACEMENT_3D ( 'NONE', #9190, #12275, #35381 ) ;
#7672=DIRECTION ( 'NONE',  ( 0.000000000000000000, 0.000000000000000000, 1.000000000000000000 ) ) ;
#7674=ORIENTED_EDGE ( 'NONE', *, *, #19958, .F. ) ;
#7683=VERTEX_POINT ( 'NONE', #15071 ) ;
#7711=CARTESIAN_POINT ( 'NONE',  ( 17.99999999999999645, -11.49545354908914518, -29.80986809967271967 ) ) ;
#7714=DIRECTION ( 'NONE',  ( -1.000000000000000000, -0.000000000000000000, -0.000000000000000000 ) ) ;
#7715=VERTEX_POINT ( 'NONE', #41199 ) ;
#7719=EDGE_CURVE ( 'NONE', #9615, #30643, #34448, .T. ) ;
#7729=EDGE_LOOP ( 'NONE', ( #2433, #8027, #3018, #24779 ) ) ;
#7742=CARTESIAN_POINT ( 'NONE',  ( 17.99999999999999645, -30.78424799127072120, 6.672111855473074726 ) ) ;
#7748=DIRECTION ( 'NONE',  ( 0.000000000000000000, 0.000000000000000000, -1.000000000000000000 ) ) ;
#7750=DIRECTION ( 'NONE',  ( 0.000000000000000000, 0.000000000000000000, -1.000000000000000000 ) ) ;
#7766=VERTEX_POINT ( 'NONE', #4792 ) ;
#7794=EDGE_CURVE ( 'NONE', #40062, #6784, #32771, .T. ) ;
#7814=ADVANCED_FACE ( 'NONE', ( #5436 ), #18800, .T. ) ;
#7843=EDGE_CURVE ( 'NONE', #26674, #39350, #15501, .T. ) ;
#7854=CYLINDRICAL_SURFACE ( 'NONE', #39724, 13.59999999999999964 ) ;
#7884=CARTESIAN_POINT ( 'NONE',  ( 17.99999999999999645, 29.68570942776486987, -10.53307442156903662 ) ) ;
#7898=EDGE_CURVE ( 'NONE', #6403, #36912, #9129, .T. ) ;
#7900=EDGE_CURVE ( 'NONE', #30670, #23378, #25868, .T. ) ;
#7922=VERTEX_POINT ( 'NONE', #32688 ) ;
#7928=EDGE_CURVE ( 'NONE', #43048, #35650, #39049, .T. ) ;
#7938=AXIS2_PLACEMENT_3D ( 'NONE', #31203, #15069, #14637 ) ;
#7953=DIRECTION ( 'NONE',  ( 0.000000000000000000, 0.000000000000000000, -1.000000000000000000 ) ) ;
#7956=VERTEX_POINT ( 'NONE', #37029 ) ;
#7957=LINE ( 'NONE', #8597, #42418 ) ;
#7980=CARTESIAN_POINT ( 'NONE',  ( -10.00000000000000000, 0.000000000000000000, 0.000000000000000000 ) ) ;
#7986=EDGE_LOOP ( 'NONE', ( #36624, #28370, #41271, #20052 ) ) ;
#7991=CARTESIAN_POINT ( 'NONE',  ( 0.000000000000000000, -31.94619804602776725, 16.59639811537345366 ) ) ;
#7996=CARTESIAN_POINT ( 'NONE',  ( 0.000000000000000000, -31.48608500567869584, -0.9019157472707834966 ) ) ;
#8000=DIRECTION ( 'NONE',  ( -1.000000000000000000, 0.000000000000000000, 0.000000000000000000 ) ) ;
#8002=ADVANCED_FACE ( 'NONE', ( #36586 ), #36815, .T. ) ;
#8017=CYLINDRICAL_SURFACE ( 'NONE', #1697, 13.59999999999999964 ) ;
#8023=CARTESIAN_POINT ( 'NONE',  ( 17.99999999999999645, -31.80866420683992857, 16.59709355804118402 ) ) ;
#8024=AXIS2_PLACEMENT_3D ( 'NONE', #10049, #6138, #6346 ) ;
#8027=ORIENTED_EDGE ( 'NONE', *, *, #32960, .F. ) ;
#8033=CARTESIAN_POINT ( 'NONE',  ( 17.99999999999999645, 31.48608500567870294, -0.9019157472705674472 ) ) ;
#8036=CARTESIAN_POINT ( 'NONE',  ( 0.000000000000000000, 0.000000000000000000, 0.000000000000000000 ) ) ;
#8038=CARTESIAN_POINT ( 'NONE',  ( 17.99999999999999645, -31.81777574834303124, -2.898764365605651427 ) ) ;
#8060=CIRCLE ( 'NONE', #38697, 13.60000000000000142 ) ;
#8067=ORIENTED_EDGE ( 'NONE', *, *, #14413, .T. ) ;
#8083=VERTEX_POINT ( 'NONE', #20280 ) ;
#8094=AXIS2_PLACEMENT_3D ( 'NONE', #11874, #11656, #24999 ) ;
#8121=CARTESIAN_POINT ( 'NONE',  ( 17.99999999999999645, 27.24480646643629811, -15.80846360676556372 ) ) ;
#8132=ORIENTED_EDGE ( 'NONE', *, *, #30375, .F. ) ;
#8141=AXIS2_PLACEMENT_3D ( 'NONE', #37845, #21767, #25045 ) ;
#8144=DIRECTION ( 'NONE',  ( -1.000000000000000000, 0.000000000000000000, -0.000000000000000000 ) ) ;
#8161=ORIENTED_EDGE ( 'NONE', *, *, #22771, .F. ) ;
#8171=ORIENTED_EDGE ( 'NONE', *, *, #40677, .T. ) ;
#8174=LINE ( 'NONE', #21534, #21575 ) ;
#8177=CARTESIAN_POINT ( 'NONE',  ( 0.000000000000000000, 5.919241748379588053, 31.39643714728458690 ) ) ;
#8178=VERTEX_POINT ( 'NONE', #18309 ) ;
#8182=EDGE_CURVE ( 'NONE', #1507, #34733, #16112, .T. ) ;
#8195=CIRCLE ( 'NONE', #4728, 13.59999999999999964 ) ;
#8204=CARTESIAN_POINT ( 'NONE',  ( 0.000000000000000000, -30.78424799127072120, 6.672111855473074726 ) ) ;
#8208=CIRCLE ( 'NONE', #38155, 36.00000000000000000 ) ;
#8213=EDGE_LOOP ( 'NONE', ( #8385, #11994, #34419, #42980 ) ) ;
#8225=DIRECTION ( 'NONE',  ( -1.000000000000000000, 0.000000000000000000, 0.000000000000000000 ) ) ;
#8229=DIRECTION ( 'NONE',  ( -1.000000000000000000, -0.000000000000000000, -0.000000000000000000 ) ) ;
#8232=ORIENTED_EDGE ( 'NONE', *, *, #18023, .F. ) ;
#8240=EDGE_CURVE ( 'NONE', #33247, #25006, #14800, .T. ) ;
#8248=CARTESIAN_POINT ( 'NONE',  ( 0.000000000000000000, 7.220349212960960550, -35.26849241522656087 ) ) ;
#8250=CYLINDRICAL_SURFACE ( 'NONE', #6325, 13.60000000000000142 ) ;
#8252=VECTOR ( 'NONE', #4121, 1000.000000000000000 ) ;
#8254=DIRECTION ( 'NONE',  ( -1.000000000000000000, 0.000000000000000000, 0.000000000000000000 ) ) ;
#8276=EDGE_CURVE ( 'NONE', #1401, #3853, #42442, .T. ) ;
#8282=CARTESIAN_POINT ( 'NONE',  ( -10.00000000000000000, 0.000000000000000000, 0.000000000000000000 ) ) ;
#8287=CARTESIAN_POINT ( 'NONE',  ( -10.00000000000000000, 0.000000000000000000, 0.000000000000000000 ) ) ;
#8290=CARTESIAN_POINT ( 'NONE',  ( 17.99999999999999645, 5.919241748379588053, 31.39643714728458690 ) ) ;
#8291=VERTEX_POINT ( 'NONE', #6231 ) ;
#8297=CARTESIAN_POINT ( 'NONE',  ( 0.000000000000000000, -0.6168405712484118508, -35.99471499692226928 ) ) ;
#8298=DIRECTION ( 'NONE',  ( 0.000000000000000000, 0.000000000000000000, 1.000000000000000000 ) ) ;
#8308=DIRECTION ( 'NONE',  ( -1.000000000000000000, 0.000000000000000000, -0.000000000000000000 ) ) ;
#8315=FACE_OUTER_BOUND ( 'NONE', #13898, .T. ) ;
#8317=EDGE_CURVE ( 'NONE', #6169, #14830, #6016, .T. ) ;
#8324=FACE_OUTER_BOUND ( 'NONE', #35954, .T. ) ;
#8330=DIRECTION ( 'NONE',  ( 0.000000000000000000, 0.000000000000000000, 1.000000000000000000 ) ) ;
#8342=CARTESIAN_POINT ( 'NONE',  ( 0.000000000000000000, -31.81777574834303124, 10.70123563439434733 ) ) ;
#8347=ORIENTED_EDGE ( 'NONE', *, *, #18157, .T. ) ;
#8353=CARTESIAN_POINT ( 'NONE',  ( 17.99999999999999645, -30.78424799127063238, -6.672111855473501940 ) ) ;
#8354=CARTESIAN_POINT ( 'NONE',  ( 0.000000000000000000, 0.000000000000000000, 0.000000000000000000 ) ) ;
#8356=EDGE_CURVE ( 'NONE', #26654, #31369, #35262, .T. ) ;
#8360=ORIENTED_EDGE ( 'NONE', *, *, #1893, .T. ) ;
#8365=DIRECTION ( 'NONE',  ( 0.000000000000000000, 0.1837495178165707566, -0.9829730996839017854 ) ) ;
#8379=CARTESIAN_POINT ( 'NONE',  ( 0.000000000000000000, -7.220349212960696761, 35.26849241522661771 ) ) ;
#8385=ORIENTED_EDGE ( 'NONE', *, *, #7064, .F. ) ;
#8408=EDGE_CURVE ( 'NONE', #31369, #18067, #23133, .T. ) ;
#8415=ORIENTED_EDGE ( 'NONE', *, *, #37583, .F. ) ;
#8421=ORIENTED_EDGE ( 'NONE', *, *, #8240, .F. ) ;
#8443=EDGE_CURVE ( 'NONE', #17756, #38173, #26594, .T. ) ;
#8444=CARTESIAN_POINT ( 'NONE',  ( 17.99999999999999645, -28.62203781743013664, 14.19692359621445199 ) ) ;
#8446=DIRECTION ( 'NONE',  ( -1.000000000000000000, -0.000000000000000000, -0.000000000000000000 ) ) ;
#8450=DIRECTION ( 'NONE',  ( 1.000000000000000000, -0.000000000000000000, -0.000000000000000000 ) ) ;
#8460=DIRECTION ( 'NONE',  ( -1.000000000000000000, 0.000000000000000000, 0.000000000000000000 ) ) ;
#8477=ORIENTED_EDGE ( 'NONE', *, *, #7399, .F. ) ;
#8487=DIRECTION ( 'NONE',  ( 0.000000000000000000, -0.9618256431728219313, 0.2736629900720728981 ) ) ;
#8488=ORIENTED_EDGE ( 'NONE', *, *, #32242, .F. ) ;
#8495=EDGE_CURVE ( 'NONE', #8083, #2224, #18259, .T. ) ;
#8496=EDGE_CURVE ( 'NONE', #10112, #36592, #33286, .T. ) ;
#8501=CYLINDRICAL_SURFACE ( 'NONE', #965, 36.00000000000000000 ) ;
#8515=VERTEX_POINT ( 'NONE', #23919 ) ;
#8520=CARTESIAN_POINT ( 'NONE',  ( 17.99999999999999645, -31.80866420683992857, 16.59709355804118402 ) ) ;
#8528=DIRECTION ( 'NONE',  ( -1.000000000000000000, -0.000000000000000000, -0.000000000000000000 ) ) ;
#8530=DIRECTION ( 'NONE',  ( -1.000000000000000000, 0.000000000000000000, -0.000000000000000000 ) ) ;
#8535=ORIENTED_EDGE ( 'NONE', *, *, #27025, .T. ) ;
#8536=CARTESIAN_POINT ( 'NONE',  ( 0.000000000000000000, 16.77727049691110750, 27.19001440037552086 ) ) ;
#8538=VECTOR ( 'NONE', #17646, 1000.000000000000000 ) ;
#8547=AXIS2_PLACEMENT_3D ( 'NONE', #11547, #31602, #41627 ) ;
#8556=CARTESIAN_POINT ( 'NONE',  ( 17.99999999999999645, -0.04937522221101428577, -31.94951095880159286 ) ) ;
#8579=CARTESIAN_POINT ( 'NONE',  ( 17.99999999999999645, 0.000000000000000000, 0.000000000000000000 ) ) ;
#8585=ORIENTED_EDGE ( 'NONE', *, *, #2222, .F. ) ;
#8590=DIRECTION ( 'NONE',  ( -1.000000000000000000, 0.000000000000000000, -0.000000000000000000 ) ) ;
#8591=ORIENTED_EDGE ( 'NONE', *, *, #24856, .F. ) ;
#8594=CARTESIAN_POINT ( 'NONE',  ( 0.000000000000000000, -14.84191762912334767, 27.78316904333121684 ) ) ;
#8597=CARTESIAN_POINT ( 'NONE',  ( 17.99999999999999645, 18.25486108452660972, -25.66996392254254644 ) ) ;
#8635=ORIENTED_EDGE ( 'NONE', *, *, #22428, .T. ) ;
#8640=EDGE_CURVE ( 'NONE', #31678, #6403, #18290, .T. ) ;
#8641=DIRECTION ( 'NONE',  ( 0.000000000000000000, 0.000000000000000000, -1.000000000000000000 ) ) ;
#8644=CARTESIAN_POINT ( 'NONE',  ( 9.000000000000000000, 0.6168405712491942250, -35.99471499692226217 ) ) ;
#8652=ORIENTED_EDGE ( 'NONE', *, *, #34873, .F. ) ;
#8657=DIRECTION ( 'NONE',  ( 0.000000000000000000, 0.000000000000000000, 1.000000000000000000 ) ) ;
#8673=CARTESIAN_POINT ( 'NONE',  ( 17.99999999999999645, 0.000000000000000000, 0.000000000000000000 ) ) ;
#8712=CARTESIAN_POINT ( 'NONE',  ( -10.00000000000000000, 0.000000000000000000, 0.000000000000000000 ) ) ;
#8728=DIRECTION ( 'NONE',  ( -1.000000000000000000, 0.000000000000000000, -0.000000000000000000 ) ) ;
#8738=ADVANCED_FACE ( 'NONE', ( #25801 ), #36422, .T. ) ;
#8740=CIRCLE ( 'NONE', #1057, 13.59999999999999787 ) ;
#8744=CIRCLE ( 'NONE', #29661, 13.59999999999999964 ) ;
#8760=ORIENTED_EDGE ( 'NONE', *, *, #32430, .T. ) ;
#8766=ORIENTED_EDGE ( 'NONE', *, *, #39699, .T. ) ;
#8780=CIRCLE ( 'NONE', #26234, 36.00000000000000000 ) ;
#8782=DIRECTION ( 'NONE',  ( 0.000000000000000000, 0.1837495178165637066, 0.9829730996839030066 ) ) ;
#8783=CARTESIAN_POINT ( 'NONE',  ( 0.000000000000000000, 7.749090474611513457, 30.53094492177216068 ) ) ;
#8784=ORIENTED_EDGE ( 'NONE', *, *, #29913, .F. ) ;
#8807=VERTEX_POINT ( 'NONE', #26211 ) ;
#8818=ORIENTED_EDGE ( 'NONE', *, *, #18157, .F. ) ;
#8826=CYLINDRICAL_SURFACE ( 'NONE', #16108, 31.49899999999999878 ) ;
#8835=LINE ( 'NONE', #12347, #19238 ) ;
#8849=EDGE_CURVE ( 'NONE', #4662, #10112, #20354, .T. ) ;
#8859=EDGE_CURVE ( 'NONE', #41335, #15839, #22744, .T. ) ;
#8862=VERTEX_POINT ( 'NONE', #22968 ) ;
#8884=EDGE_CURVE ( 'NONE', #8807, #38409, #16168, .T. ) ;
#8890=CARTESIAN_POINT ( 'NONE',  ( 17.99999999999999645, -30.74337109795213863, -8.695908345466433431 ) ) ;
#8910=VECTOR ( 'NONE', #26877, 1000.000000000000000 ) ;
#8924=ORIENTED_EDGE ( 'NONE', *, *, #32091, .F. ) ;
#8925=ADVANCED_FACE ( 'NONE', ( #17286 ), #30982, .T. ) ;
#8927=DIRECTION ( 'NONE',  ( 1.000000000000000000, 0.000000000000000000, 0.000000000000000000 ) ) ;
#8941=AXIS2_PLACEMENT_3D ( 'NONE', #30182, #36477, #33232 ) ;
#8948=DIRECTION ( 'NONE',  ( 0.000000000000000000, -0.3612416661871603596, 0.9324722294043529258 ) ) ;
#8951=ORIENTED_EDGE ( 'NONE', *, *, #39652, .F. ) ;
#8959=CARTESIAN_POINT ( 'NONE',  ( 0.000000000000000000, 30.78424799127067502, 6.672111855473287001 ) ) ;
#8988=EDGE_CURVE ( 'NONE', #5335, #25212, #37068, .T. ) ;
#8995=DIRECTION ( 'NONE',  ( 0.000000000000000000, -0.5264321628773447337, -0.8502171357296209875 ) ) ;
#8996=CARTESIAN_POINT ( 'NONE',  ( 17.99999999999999645, 2.007101075700415738, -31.43498920425966858 ) ) ;
#9014=EDGE_CURVE ( 'NONE', #32794, #35367, #4125, .T. ) ;
#9043=CIRCLE ( 'NONE', #41775, 13.59999999999999964 ) ;
#9051=VERTEX_POINT ( 'NONE', #35324 ) ;
#9059=ORIENTED_EDGE ( 'NONE', *, *, #19150, .T. ) ;
#9075=VECTOR ( 'NONE', #12007, 1000.000000000000000 ) ;
#9079=DIRECTION ( 'NONE',  ( 0.000000000000000000, 0.8951632913550634507, -0.4457383557765359217 ) ) ;
#9097=EDGE_LOOP ( 'NONE', ( #39863, #5050, #912, #40998 ) ) ;
#9108=ORIENTED_EDGE ( 'NONE', *, *, #2021, .F. ) ;
#9115=VERTEX_POINT ( 'NONE', #38582 ) ;
#9119=EDGE_CURVE ( 'NONE', #23378, #42608, #9909, .T. ) ;
#9121=EDGE_CURVE ( 'NONE', #13471, #17450, #34896, .T. ) ;
#9122=CYLINDRICAL_SURFACE ( 'NONE', #1104, 31.49899999999999878 ) ;
#9128=CIRCLE ( 'NONE', #28650, 36.00000000000000000 ) ;
#9129=LINE ( 'NONE', #35723, #24477 ) ;
#9151=ORIENTED_EDGE ( 'NONE', *, *, #12158, .F. ) ;
#9169=EDGE_CURVE ( 'NONE', #12063, #990, #1297, .T. ) ;
#9182=DIRECTION ( 'NONE',  ( -1.000000000000000000, 0.000000000000000000, -0.000000000000000000 ) ) ;
#9186=ORIENTED_EDGE ( 'NONE', *, *, #36883, .T. ) ;
#9190=CARTESIAN_POINT ( 'NONE',  ( 17.99999999999999645, -16.86122981692037825, 27.13802899033285954 ) ) ;
#9196=DIRECTION ( 'NONE',  ( -1.000000000000000000, 0.000000000000000000, 0.000000000000000000 ) ) ;
#9197=CARTESIAN_POINT ( 'NONE',  ( 17.99999999999999645, 28.62203781743003717, -14.19692359621465094 ) ) ;
#9198=ORIENTED_EDGE ( 'NONE', *, *, #40467, .T. ) ;
#9200=ADVANCED_FACE ( 'NONE', ( #41865 ), #22063, .T. ) ;
#9216=ORIENTED_EDGE ( 'NONE', *, *, #32072, .T. ) ;
#9218=EDGE_CURVE ( 'NONE', #13944, #7683, #42497, .T. ) ;
#9229=CARTESIAN_POINT ( 'NONE',  ( 9.000000000000000000, 7.220349212960450735, 35.26849241522667455 ) ) ;
#9230=DIRECTION ( 'NONE',  ( 0.000000000000000000, 0.7980172272802407152, -0.6026346363792548511 ) ) ;
#9231=ORIENTED_EDGE ( 'NONE', *, *, #35388, .T. ) ;
#9232=LINE ( 'NONE', #35823, #33320 ) ;
#9241=EDGE_LOOP ( 'NONE', ( #27594, #42677, #27418, #8161 ) ) ;
#9249=DIRECTION ( 'NONE',  ( -1.000000000000000000, -0.000000000000000000, -0.000000000000000000 ) ) ;
#9251=EDGE_LOOP ( 'NONE', ( #22422, #10094, #39979, #5222 ) ) ;
#9284=CARTESIAN_POINT ( 'NONE',  ( 0.000000000000000000, -23.79363200506935172, -27.01597816121672224 ) ) ;
#9287=ORIENTED_EDGE ( 'NONE', *, *, #24012, .T. ) ;
#9292=ORIENTED_EDGE ( 'NONE', *, *, #52, .F. ) ;
#9299=DIRECTION ( 'NONE',  ( 0.000000000000000000, 0.000000000000000000, 1.000000000000000000 ) ) ;
#9303=AXIS2_PLACEMENT_3D ( 'NONE', #37598, #41074, #1810 ) ;
#9305=VECTOR ( 'NONE', #41020, 1000.000000000000000 ) ;
#9310=CIRCLE ( 'NONE', #212, 13.59999999999999787 ) ;
#9315=VERTEX_POINT ( 'NONE', #39439 ) ;
#9318=AXIS2_PLACEMENT_3D ( 'NONE', #7980, #4041, #11067 ) ;
#9329=CIRCLE ( 'NONE', #35778, 13.60000000000000497 ) ;
#9332=CYLINDRICAL_SURFACE ( 'NONE', #23472, 13.59999999999999964 ) ;
#9350=ORIENTED_EDGE ( 'NONE', *, *, #2174, .T. ) ;
#9362=ORIENTED_EDGE ( 'NONE', *, *, #18344, .F. ) ;
#9376=DIRECTION ( 'NONE',  ( -1.000000000000000000, 0.000000000000000000, 0.000000000000000000 ) ) ;
#9381=ADVANCED_FACE ( 'NONE', ( #26801 ), #4291, .T. ) ;
#9397=ORIENTED_EDGE ( 'NONE', *, *, #22251, .T. ) ;
#9403=DIRECTION ( 'NONE',  ( -1.000000000000000000, 0.000000000000000000, 0.000000000000000000 ) ) ;
#9404=ORIENTED_EDGE ( 'NONE', *, *, #8408, .T. ) ;
#9416=ORIENTED_EDGE ( 'NONE', *, *, #28891, .T. ) ;
#9435=DIRECTION ( 'NONE',  ( 0.000000000000000000, 0.000000000000000000, 1.000000000000000000 ) ) ;
#9437=DIRECTION ( 'NONE',  ( 0.000000000000000000, 0.000000000000000000, 1.000000000000000000 ) ) ;
#9443=DIRECTION ( 'NONE',  ( -1.000000000000000000, 0.000000000000000000, -0.000000000000000000 ) ) ;
#9447=AXIS2_PLACEMENT_3D ( 'NONE', #35172, #21920, #41504 ) ;
#9452=DIRECTION ( 'NONE',  ( -1.000000000000000000, 0.000000000000000000, 0.000000000000000000 ) ) ;
#9456=AXIS2_PLACEMENT_3D ( 'NONE', #23532, #10184, #36800 ) ;
#9469=AXIS2_PLACEMENT_3D ( 'NONE', #22925, #31909, #26162 ) ;
#9480=( NAMED_UNIT ( * ) PLANE_ANGLE_UNIT ( ) SI_UNIT ( $, .RADIAN. ) );
#9494=DIRECTION ( 'NONE',  ( -1.000000000000000000, 0.000000000000000000, 0.000000000000000000 ) ) ;
#9499=CYLINDRICAL_SURFACE ( 'NONE', #14948, 31.49899999999999878 ) ;
#9508=VECTOR ( 'NONE', #28932, 1000.000000000000000 ) ;
#9515=DIRECTION ( 'NONE',  ( -1.000000000000000000, 0.000000000000000000, 0.000000000000000000 ) ) ;
#9526=CARTESIAN_POINT ( 'NONE',  ( 17.99999999999999645, -25.46650492921884279, -19.29328419707811193 ) ) ;
#9549=CARTESIAN_POINT ( 'NONE',  ( 17.99999999999999645, -30.74337109795213863, -8.695908345466433431 ) ) ;
#9558=AXIS2_PLACEMENT_3D ( 'NONE', #26001, #36647, #39062 ) ;
#9559=ORIENTED_EDGE ( 'NONE', *, *, #37927, .F. ) ;
#9563=DIRECTION ( 'NONE',  ( -1.000000000000000000, -0.000000000000000000, 0.000000000000000000 ) ) ;
#9590=AXIS2_PLACEMENT_3D ( 'NONE', #2150, #21437, #1302 ) ;
#9593=CIRCLE ( 'NONE', #42304, 31.49900000000000588 ) ;
#9612=DIRECTION ( 'NONE',  ( 0.000000000000000000, -0.6736956436465636466, 0.7390089172206532053 ) ) ;
#9613=CIRCLE ( 'NONE', #20814, 13.60000000000000142 ) ;
#9614=AXIS2_PLACEMENT_3D ( 'NONE', #36096, #23261, #13007 ) ;
#9615=VERTEX_POINT ( 'NONE', #14808 ) ;
#9619=CARTESIAN_POINT ( 'NONE',  ( 17.99999999999999645, 0.04937522221122418731, 31.94951095880159286 ) ) ;
#9626=CARTESIAN_POINT ( 'NONE',  ( 0.000000000000000000, -25.46650492921910924, 19.29328419707777087 ) ) ;
#9635=DIRECTION ( 'NONE',  ( -1.000000000000000000, -0.000000000000000000, 0.000000000000000000 ) ) ;
#9637=DIRECTION ( 'NONE',  ( -1.000000000000000000, -0.000000000000000000, -0.000000000000000000 ) ) ;
#9638=DIRECTION ( 'NONE',  ( -1.000000000000000000, 0.000000000000000000, -0.000000000000000000 ) ) ;
#9640=AXIS2_PLACEMENT_3D ( 'NONE', #17281, #41652, #15075 ) ;
#9646=ORIENTED_EDGE ( 'NONE', *, *, #39699, .F. ) ;
#9647=EDGE_CURVE ( 'NONE', #2925, #23705, #5734, .T. ) ;
#9651=DIRECTION ( 'NONE',  ( 0.000000000000000000, 0.9957341762950341346, 0.09226835946330559646 ) ) ;
#9659=ORIENTED_EDGE ( 'NONE', *, *, #26038, .T. ) ;
#9669=CYLINDRICAL_SURFACE ( 'NONE', #20906, 13.59999999999999964 ) ;
#9674=DIRECTION ( 'NONE',  ( -1.000000000000000000, 0.000000000000000000, 0.000000000000000000 ) ) ;
#9689=CARTESIAN_POINT ( 'NONE',  ( 17.99999999999999645, 0.000000000000000000, 0.000000000000000000 ) ) ;
#9694=DIRECTION ( 'NONE',  ( 0.000000000000000000, 0.6736956436465532105, 0.7390089172206629753 ) ) ;
#9702=AXIS2_PLACEMENT_3D ( 'NONE', #27622, #28277, #38062 ) ;
#9709=CARTESIAN_POINT ( 'NONE',  ( 17.99999999999999645, 28.35267316522783432, 22.18391138608718549 ) ) ;
#9721=CARTESIAN_POINT ( 'NONE',  ( 0.000000000000000000, 31.81777574834305966, -2.898764365605425830 ) ) ;
#9723=DIRECTION ( 'NONE',  ( -1.000000000000000000, 0.000000000000000000, 0.000000000000000000 ) ) ;
#9726=CARTESIAN_POINT ( 'NONE',  ( 8.999999999999998224, 0.6168405712486720871, 35.99471499692226928 ) ) ;
#9736=ORIENTED_EDGE ( 'NONE', *, *, #42433, .F. ) ;
#9766=DIRECTION ( 'NONE',  ( 0.000000000000000000, 0.7980172272802363853, 0.6026346363792605132 ) ) ;
#9772=CYLINDRICAL_SURFACE ( 'NONE', #17073, 13.59999999999999787 ) ;
#9783=ORIENTED_EDGE ( 'NONE', *, *, #4701, .F. ) ;
#9825=CARTESIAN_POINT ( 'NONE',  ( 17.99999999999999645, -2.007101075699733173, -31.43498920425971832 ) ) ;
#9830=ORIENTED_EDGE ( 'NONE', *, *, #13395, .F. ) ;
#9835=DIRECTION ( 'NONE',  ( 0.000000000000000000, 0.000000000000000000, 1.000000000000000000 ) ) ;
#9838=ORIENTED_EDGE ( 'NONE', *, *, #16974, .F. ) ;
#9852=CARTESIAN_POINT ( 'NONE',  ( 17.99999999999999645, -12.42760411676062127, 33.78690065568420664 ) ) ;
#9853=DIRECTION ( 'NONE',  ( 0.000000000000000000, -0.8951632913550664483, 0.4457383557765300930 ) ) ;
#9865=LINE ( 'NONE', #9229, #5729 ) ;
#9899=CARTESIAN_POINT ( 'NONE',  ( 17.99999999999999645, -25.52601536738605859, 19.21447964122688390 ) ) ;
#9901=SURFACE_STYLE_USAGE ( .BOTH. , #12771 ) ;
#9908=ORIENTED_EDGE ( 'NONE', *, *, #33246, .T. ) ;
#9909=CIRCLE ( 'NONE', #31513, 13.59999999999999964 ) ;
#9929=EDGE_CURVE ( 'NONE', #8178, #29573, #32765, .T. ) ;
#9938=CARTESIAN_POINT ( 'NONE',  ( 17.99999999999999645, 0.000000000000000000, 0.000000000000000000 ) ) ;
#9946=CARTESIAN_POINT ( 'NONE',  ( 0.000000000000000000, 21.48775762007893420, -23.64423737150114135 ) ) ;
#9964=EDGE_LOOP ( 'NONE', ( #42989, #22084, #17529, #30149 ) ) ;
#9972=AXIS2_PLACEMENT_3D ( 'NONE', #13693, #19817, #37003 ) ;
#9977=ORIENTED_EDGE ( 'NONE', *, *, #3207, .F. ) ;
#9984=EDGE_LOOP ( 'NONE', ( #79, #41965, #11497, #2320 ) ) ;
#9987=CARTESIAN_POINT ( 'NONE',  ( 17.99999999999999645, 0.000000000000000000, 0.000000000000000000 ) ) ;
#9989=EDGE_CURVE ( 'NONE', #9115, #24259, #39019, .T. ) ;
#9999=DIRECTION ( 'NONE',  ( 0.000000000000000000, 0.8951632913550634507, -0.4457383557765359217 ) ) ;
#10011=FACE_OUTER_BOUND ( 'NONE', #13234, .T. ) ;
#10021=CIRCLE ( 'NONE', #36481, 36.00000000000000000 ) ;
#10049=CARTESIAN_POINT ( 'NONE',  ( 0.000000000000000000, -30.74337109795213863, -8.695908345466433431 ) ) ;
#10053=CIRCLE ( 'NONE', #37925, 31.49899999999999878 ) ;
#10058=DIRECTION ( 'NONE',  ( -1.000000000000000000, 0.000000000000000000, -0.000000000000000000 ) ) ;
#10070=CARTESIAN_POINT ( 'NONE',  ( 17.99999999999999645, 0.000000000000000000, 0.000000000000000000 ) ) ;
#10085=LINE ( 'NONE', #3307, #1922 ) ;
#10087=DIRECTION ( 'NONE',  ( -1.000000000000000000, 0.000000000000000000, -0.000000000000000000 ) ) ;
#10094=ORIENTED_EDGE ( 'NONE', *, *, #22622, .F. ) ;
#10101=ORIENTED_EDGE ( 'NONE', *, *, #3582, .F. ) ;
#10103=ORIENTED_EDGE ( 'NONE', *, *, #37302, .T. ) ;
#10105=CIRCLE ( 'NONE', #16395, 36.00000000000000000 ) ;
#10110=EDGE_CURVE ( 'NONE', #13372, #11747, #17493, .T. ) ;
#10112=VERTEX_POINT ( 'NONE', #37836 ) ;
#10132=AXIS2_PLACEMENT_3D ( 'NONE', #41923, #25389, #35390 ) ;
#10136=EDGE_LOOP ( 'NONE', ( #9838, #18844, #13461, #13864 ) ) ;
#10138=VECTOR ( 'NONE', #18304, 1000.000000000000000 ) ;
#10145=DIRECTION ( 'NONE',  ( 0.000000000000000000, 0.5264321628773507289, 0.8502171357296173237 ) ) ;
#10153=VERTEX_POINT ( 'NONE', #28282 ) ;
#10165=VECTOR ( 'NONE', #26090, 1000.000000000000000 ) ;
#10179=AXIS2_PLACEMENT_3D ( 'NONE', #40948, #20941, #25284 ) ;
#10184=DIRECTION ( 'NONE',  ( -1.000000000000000000, 0.000000000000000000, -0.000000000000000000 ) ) ;
#10200=EDGE_CURVE ( 'NONE', #42739, #8178, #25865, .T. ) ;
#10204=EDGE_CURVE ( 'NONE', #7021, #28925, #39756, .T. ) ;
#10205=AXIS2_PLACEMENT_3D ( 'NONE', #23006, #36249, #29517 ) ;
#10211=VERTEX_POINT ( 'NONE', #2463 ) ;
#10213=DIRECTION ( 'NONE',  ( 1.000000000000000000, 0.000000000000000000, 0.000000000000000000 ) ) ;
#10214=ORIENTED_EDGE ( 'NONE', *, *, #9989, .F. ) ;
#10216=VERTEX_POINT ( 'NONE', #39552 ) ;
#10221=FACE_OUTER_BOUND ( 'NONE', #3411, .T. ) ;
#10228=CARTESIAN_POINT ( 'NONE',  ( 17.99999999999999645, 0.000000000000000000, 0.000000000000000000 ) ) ;
#10230=VECTOR ( 'NONE', #7352, 1000.000000000000000 ) ;
#10234=AXIS2_PLACEMENT_3D ( 'NONE', #30861, #28255, #34336 ) ;
#10236=EDGE_CURVE ( 'NONE', #41169, #31298, #29336, .T. ) ;
#10249=ORIENTED_EDGE ( 'NONE', *, *, #29466, .T. ) ;
#10259=ADVANCED_FACE ( 'NONE', ( #32804 ), #8826, .T. ) ;
#10278=DIRECTION ( 'NONE',  ( -1.000000000000000000, 0.000000000000000000, 0.000000000000000000 ) ) ;
#10285=CYLINDRICAL_SURFACE ( 'NONE', #36345, 36.00000000000000000 ) ;
#10295=DIRECTION ( 'NONE',  ( 0.000000000000000000, 0.000000000000000000, 1.000000000000000000 ) ) ;
#10300=CIRCLE ( 'NONE', #2609, 36.00000000000000000 ) ;
#10309=ORIENTED_EDGE ( 'NONE', *, *, #41149, .T. ) ;
#10311=VERTEX_POINT ( 'NONE', #13845 ) ;
#10314=AXIS2_PLACEMENT_3D ( 'NONE', #14323, #7311, #33944 ) ;
#10318=CARTESIAN_POINT ( 'NONE',  ( 0.000000000000000000, 35.89808275599445153, 2.706964063997353342 ) ) ;
#10319=EDGE_CURVE ( 'NONE', #39631, #13079, #38374, .T. ) ;
#10330=ORIENTED_EDGE ( 'NONE', *, *, #27210, .F. ) ;
#10336=AXIS2_PLACEMENT_3D ( 'NONE', #14133, #4718, #17858 ) ;
#10338=ORIENTED_EDGE ( 'NONE', *, *, #38340, .T. ) ;
#10342=DIRECTION ( 'NONE',  ( -1.000000000000000000, 0.000000000000000000, 0.000000000000000000 ) ) ;
#10349=CARTESIAN_POINT ( 'NONE',  ( 17.99999999999999645, -31.80866420683989304, -2.997093558041628025 ) ) ;
#10372=VERTEX_POINT ( 'NONE', #3536 ) ;
#10414=DIRECTION ( 'NONE',  ( -1.000000000000000000, -0.000000000000000000, -0.000000000000000000 ) ) ;
#10436=EDGE_CURVE ( 'NONE', #24676, #4662, #17526, .T. ) ;
#10440=ORIENTED_EDGE ( 'NONE', *, *, #9929, .T. ) ;
#10442=DIRECTION ( 'NONE',  ( -1.000000000000000000, 0.000000000000000000, -0.000000000000000000 ) ) ;
#10453=AXIS2_PLACEMENT_3D ( 'NONE', #21052, #24978, #31043 ) ;
#10470=EDGE_CURVE ( 'NONE', #10990, #35040, #4229, .T. ) ;
#10484=EDGE_CURVE ( 'NONE', #24756, #39386, #11640, .T. ) ;
#10498=DIRECTION ( 'NONE',  ( 0.000000000000000000, 0.000000000000000000, 1.000000000000000000 ) ) ;
#10499=FACE_OUTER_BOUND ( 'NONE', #15318, .T. ) ;
#10500=CIRCLE ( 'NONE', #32094, 13.59999999999999787 ) ;
#10502=ORIENTED_EDGE ( 'NONE', *, *, #10484, .F. ) ;
#10561=CARTESIAN_POINT ( 'NONE',  ( 17.99999999999999645, 35.78425302087544679, -3.935382540232420734 ) ) ;
#10573=FILL_AREA_STYLE_COLOUR ( '', #34562 ) ;
#10617=EDGE_CURVE ( 'NONE', #41650, #14228, #36304, .T. ) ;
#10631=ORIENTED_EDGE ( 'NONE', *, *, #13641, .T. ) ;
#10644=CARTESIAN_POINT ( 'NONE',  ( 17.99999999999999645, -31.48608500567869584, -0.9019157472707834966 ) ) ;
#10668=DIRECTION ( 'NONE',  ( -1.000000000000000000, -0.000000000000000000, 0.000000000000000000 ) ) ;
#10670=STYLED_ITEM ( 'NONE', ( #19761 ), #38478 ) ;
#10692=VERTEX_POINT ( 'NONE', #38433 ) ;
#10705=CARTESIAN_POINT ( 'NONE',  ( 8.999999999999998224, -12.42760411676013810, -33.78690065568439138 ) ) ;
#10710=CIRCLE ( 'NONE', #21909, 31.49899999999999878 ) ;
#10711=DIRECTION ( 'NONE',  ( -1.000000000000000000, -0.000000000000000000, -0.000000000000000000 ) ) ;
#10713=ADVANCED_FACE ( 'NONE', ( #32119 ), #2200, .T. ) ;
#10721=ORIENTED_EDGE ( 'NONE', *, *, #24562, .F. ) ;
#10729=ADVANCED_FACE ( 'NONE', ( #13143 ), #20344, .T. ) ;
#10730=AXIS2_PLACEMENT_3D ( 'NONE', #2268, #38504, #42195 ) ;
#10736=CARTESIAN_POINT ( 'NONE',  ( 17.99999999999999645, -21.56073507908662634, 23.57770962728557151 ) ) ;
#10739=VERTEX_POINT ( 'NONE', #19692 ) ;
#10741=VERTEX_POINT ( 'NONE', #26220 ) ;
#10746=CARTESIAN_POINT ( 'NONE',  ( 17.99999999999999645, 31.11570115861502828, -4.898994019976315784 ) ) ;
#10770=CARTESIAN_POINT ( 'NONE',  ( 17.99999999999999645, -16.77727049691128869, 27.19001440037539297 ) ) ;
#10788=VECTOR ( 'NONE', #34837, 1000.000000000000000 ) ;
#10806=ORIENTED_EDGE ( 'NONE', *, *, #39218, .F. ) ;
#10828=CYLINDRICAL_SURFACE ( 'NONE', #10314, 31.49899999999999878 ) ;
#10829=DIRECTION ( 'NONE',  ( -1.000000000000000000, 0.000000000000000000, -0.000000000000000000 ) ) ;
#10847=CARTESIAN_POINT ( 'NONE',  ( 17.99999999999999645, 18.42432724429473367, 30.92804820216009531 ) ) ;
#10853=LINE ( 'NONE', #40051, #8538 ) ;
#10881=VERTEX_POINT ( 'NONE', #4968 ) ;
#10886=CIRCLE ( 'NONE', #40084, 13.59999999999999787 ) ;
#10892=CARTESIAN_POINT ( 'NONE',  ( 9.000000000000000000, 13.57797752207923381, 33.34124362422479493 ) ) ;
#10903=ADVANCED_FACE ( 'NONE', ( #15465 ), #35278, .T. ) ;
#10909=CIRCLE ( 'NONE', #35270, 13.59999999999999964 ) ;
#10924=CARTESIAN_POINT ( 'NONE',  ( 17.99999999999999645, 35.89808275599445153, -2.706964063997355119 ) ) ;
#10931=ORIENTED_EDGE ( 'NONE', *, *, #38657, .T. ) ;
#10948=DIRECTION ( 'NONE',  ( -1.000000000000000000, 0.000000000000000000, 0.000000000000000000 ) ) ;
#10959=CARTESIAN_POINT ( 'NONE',  ( 0.000000000000000000, 0.04937522221168735848, -31.94951095880158576 ) ) ;
#10962=CARTESIAN_POINT ( 'NONE',  ( 17.99999999999999645, 21.48775762007859669, 23.64423737150145399 ) ) ;
#10964=FACE_OUTER_BOUND ( 'NONE', #29030, .T. ) ;
#10980=ORIENTED_EDGE ( 'NONE', *, *, #6501, .T. ) ;
#10990=VERTEX_POINT ( 'NONE', #8248 ) ;
#11004=DIRECTION ( 'NONE',  ( -1.000000000000000000, 0.000000000000000000, -0.000000000000000000 ) ) ;
#11005=CYLINDRICAL_SURFACE ( 'NONE', #27718, 31.49899999999999878 ) ;
#11014=CARTESIAN_POINT ( 'NONE',  ( 8.999999999999998224, -23.79363200506935172, -27.01597816121672224 ) ) ;
#11029=DIRECTION ( 'NONE',  ( -1.000000000000000000, 0.000000000000000000, -0.000000000000000000 ) ) ;
#11044=AXIS2_PLACEMENT_3D ( 'NONE', #1127, #14696, #34091 ) ;
#11046=CARTESIAN_POINT ( 'NONE',  ( 0.000000000000000000, -18.25486108452607681, -25.66996392254292658 ) ) ;
#11051=EDGE_CURVE ( 'NONE', #18492, #42739, #13391, .T. ) ;
#11053=FACE_OUTER_BOUND ( 'NONE', #23742, .T. ) ;
#11057=EDGE_CURVE ( 'NONE', #37206, #23356, #29397, .T. ) ;
#11067=DIRECTION ( 'NONE',  ( 0.000000000000000000, 0.000000000000000000, 1.000000000000000000 ) ) ;
#11070=DIRECTION ( 'NONE',  ( -1.000000000000000000, 0.000000000000000000, 0.000000000000000000 ) ) ;
#11085=CARTESIAN_POINT ( 'NONE',  ( 9.000000000000000000, -35.89808275599443022, -2.706964063997606917 ) ) ;
#11091=EDGE_CURVE ( 'NONE', #35650, #38585, #32861, .T. ) ;
#11106=DIRECTION ( 'NONE',  ( 0.000000000000000000, 0.000000000000000000, 1.000000000000000000 ) ) ;
#11121=DIRECTION ( 'NONE',  ( -1.000000000000000000, 0.000000000000000000, -0.000000000000000000 ) ) ;
#11123=EDGE_CURVE ( 'NONE', #34690, #38106, #14082, .T. ) ;
#11129=EDGE_CURVE ( 'NONE', #28874, #23736, #28037, .T. ) ;
#11135=LINE ( 'NONE', #37512, #41801 ) ;
#11153=CARTESIAN_POINT ( 'NONE',  ( 17.99999999999999645, 28.57802095670106723, -14.28532136906642691 ) ) ;
#11159=VERTEX_POINT ( 'NONE', #25719 ) ;
#11161=DIRECTION ( 'NONE',  ( 0.000000000000000000, 0.000000000000000000, 1.000000000000000000 ) ) ;
#11176=CYLINDRICAL_SURFACE ( 'NONE', #38695, 13.59999999999999964 ) ;
#11183=DIRECTION ( 'NONE',  ( -1.000000000000000000, -0.000000000000000000, -0.000000000000000000 ) ) ;
#11184=AXIS2_PLACEMENT_3D ( 'NONE', #37531, #5017, #27745 ) ;
#11192=CYLINDRICAL_SURFACE ( 'NONE', #15324, 13.59999999999999964 ) ;
#11195=ORIENTED_EDGE ( 'NONE', *, *, #22036, .F. ) ;
#11202=CARTESIAN_POINT ( 'NONE',  ( -10.00000000000000000, 0.000000000000000000, 0.000000000000000000 ) ) ;
#11219=FACE_OUTER_BOUND ( 'NONE', #24859, .T. ) ;
#11227=ADVANCED_FACE ( 'NONE', ( #547, #6667 ), #16962, .F. ) ;
#11243=VECTOR ( 'NONE', #39128, 1000.000000000000000 ) ;
#11246=VECTOR ( 'NONE', #22230, 1000.000000000000000 ) ;
#11249=ORIENTED_EDGE ( 'NONE', *, *, #32054, .T. ) ;
#11257=CARTESIAN_POINT ( 'NONE',  ( 0.000000000000000000, 0.000000000000000000, 0.000000000000000000 ) ) ;
#11260=FACE_OUTER_BOUND ( 'NONE', #36151, .T. ) ;
#11267=CARTESIAN_POINT ( 'NONE',  ( 0.000000000000000000, 0.04937522221122418731, 31.94951095880159286 ) ) ;
#11277=ORIENTED_EDGE ( 'NONE', *, *, #6640, .F. ) ;
#11282=DIRECTION ( 'NONE',  ( -1.000000000000000000, -0.000000000000000000, -0.000000000000000000 ) ) ;
#11286=EDGE_CURVE ( 'NONE', #10372, #7044, #20452, .T. ) ;
#11290=CARTESIAN_POINT ( 'NONE',  ( 17.99999999999999645, 0.000000000000000000, 0.000000000000000000 ) ) ;
#11304=DIRECTION ( 'NONE',  ( 0.000000000000000000, 0.000000000000000000, 1.000000000000000000 ) ) ;
#11316=EDGE_CURVE ( 'NONE', #37373, #14052, #9865, .T. ) ;
#11345=ORIENTED_EDGE ( 'NONE', *, *, #39785, .F. ) ;
#11349=ORIENTED_EDGE ( 'NONE', *, *, #34542, .F. ) ;
#11360=ORIENTED_EDGE ( 'NONE', *, *, #42578, .T. ) ;
#11361=DIRECTION ( 'NONE',  ( -1.000000000000000000, 0.000000000000000000, 0.000000000000000000 ) ) ;
#11365=EDGE_CURVE ( 'NONE', #31678, #18694, #32988, .T. ) ;
#11367=DIRECTION ( 'NONE',  ( -1.000000000000000000, 0.000000000000000000, 0.000000000000000000 ) ) ;
#11378=EDGE_CURVE ( 'NONE', #33094, #37148, #42795, .T. ) ;
#11390=ADVANCED_FACE ( 'NONE', ( #32781 ), #6375, .F. ) ;
#11395=DIRECTION ( 'NONE',  ( 1.000000000000000000, -0.000000000000000000, -0.000000000000000000 ) ) ;
#11397=COLOUR_RGB ( '', 0.40784314, 0.44705882, 0.49803922) ;
#11421=CARTESIAN_POINT ( 'NONE',  ( 0.000000000000000000, -5.919241748379815427, 31.39643714728454427 ) ) ;
#11424=VERTEX_POINT ( 'NONE', #42381 ) ;
#11428=DIRECTION ( 'NONE',  ( 0.000000000000000000, 0.3612416661871471479, 0.9324722294043580328 ) ) ;
#11432=ORIENTED_EDGE ( 'NONE', *, *, #13360, .F. ) ;
#11436=ORIENTED_EDGE ( 'NONE', *, *, #35877, .T. ) ;
#11468=ORIENTED_EDGE ( 'NONE', *, *, #29294, .T. ) ;
#11475=CARTESIAN_POINT ( 'NONE',  ( 17.99999999999999645, 0.6168405712491924486, -35.99471499692226217 ) ) ;
#11478=ORIENTED_EDGE ( 'NONE', *, *, #22280, .F. ) ;
#11497=ORIENTED_EDGE ( 'NONE', *, *, #12443, .T. ) ;
#11498=CARTESIAN_POINT ( 'NONE',  ( 17.99999999999999645, 31.48608500567870294, 0.9019157472705636724 ) ) ;
#11502=DIRECTION ( 'NONE',  ( -1.000000000000000000, -0.000000000000000000, -0.000000000000000000 ) ) ;
#11514=ORIENTED_EDGE ( 'NONE', *, *, #21258, .F. ) ;
#11523=FACE_OUTER_BOUND ( 'NONE', #11688, .T. ) ;
#11531=DIRECTION ( 'NONE',  ( 0.000000000000000000, 0.000000000000000000, 1.000000000000000000 ) ) ;
#11546=ORIENTED_EDGE ( 'NONE', *, *, #23616, .F. ) ;
#11547=CARTESIAN_POINT ( 'NONE',  ( 17.99999999999999645, -5.919241748379376666, -31.39643714728462953 ) ) ;
#11558=DIRECTION ( 'NONE',  ( 0.000000000000000000, 0.000000000000000000, 1.000000000000000000 ) ) ;
#11560=CYLINDRICAL_SURFACE ( 'NONE', #22708, 13.59999999999999787 ) ;
#11563=ORIENTED_EDGE ( 'NONE', *, *, #588, .F. ) ;
#11568=AXIS2_PLACEMENT_3D ( 'NONE', #27768, #41027, #29628 ) ;
#11571=DIRECTION ( 'NONE',  ( -1.000000000000000000, 0.000000000000000000, 0.000000000000000000 ) ) ;
#11577=CIRCLE ( 'NONE', #35923, 13.59999999999999787 ) ;
#11605=CARTESIAN_POINT ( 'NONE',  ( 0.000000000000000000, 0.000000000000000000, 0.000000000000000000 ) ) ;
#11606=CYLINDRICAL_SURFACE ( 'NONE', #431, 31.49899999999999878 ) ;
#11609=CIRCLE ( 'NONE', #40114, 13.59999999999999964 ) ;
#11615=CARTESIAN_POINT ( 'NONE',  ( 17.99999999999999645, 28.62203781743003717, -14.19692359621465094 ) ) ;
#11616=DIRECTION ( 'NONE',  ( 0.000000000000000000, 0.000000000000000000, 1.000000000000000000 ) ) ;
#11623=CYLINDRICAL_SURFACE ( 'NONE', #23665, 13.60000000000000142 ) ;
#11625=ORIENTED_EDGE ( 'NONE', *, *, #11650, .T. ) ;
#11626=CIRCLE ( 'NONE', #11661, 36.00000000000000000 ) ;
#11629=ORIENTED_EDGE ( 'NONE', *, *, #2257, .F. ) ;
#11640=LINE ( 'NONE', #24538, #34206 ) ;
#11650=EDGE_CURVE ( 'NONE', #1507, #10739, #1337, .T. ) ;
#11652=CYLINDRICAL_SURFACE ( 'NONE', #31885, 13.60000000000000142 ) ;
#11656=DIRECTION ( 'NONE',  ( 1.000000000000000000, 0.000000000000000000, 0.000000000000000000 ) ) ;
#11661=AXIS2_PLACEMENT_3D ( 'NONE', #34835, #24850, #40940 ) ;
#11688=EDGE_LOOP ( 'NONE', ( #22294, #5114, #36680, #28744 ) ) ;
#11696=ORIENTED_EDGE ( 'NONE', *, *, #11057, .F. ) ;
#11703=EDGE_CURVE ( 'NONE', #23971, #36837, #39168, .T. ) ;
#11709=CIRCLE ( 'NONE', #16570, 36.00000000000000000 ) ;
#11710=EDGE_CURVE ( 'NONE', #20287, #3093, #14146, .T. ) ;
#11717=( NAMED_UNIT ( * ) SI_UNIT ( $, .STERADIAN. ) SOLID_ANGLE_UNIT ( ) );
#11719=DIRECTION ( 'NONE',  ( 1.000000000000000000, 0.000000000000000000, 0.000000000000000000 ) ) ;
#11721=AXIS2_PLACEMENT_3D ( 'NONE', #29839, #6250, #19805 ) ;
#11723=FACE_OUTER_BOUND ( 'NONE', #2793, .T. ) ;
#11724=EDGE_LOOP ( 'NONE', ( #33178, #42800, #41619, #10631 ) ) ;
#11725=LINE ( 'NONE', #18083, #30316 ) ;
#11726=ORIENTED_EDGE ( 'NONE', *, *, #23093, .T. ) ;
#11727=CARTESIAN_POINT ( 'NONE',  ( 17.99999999999999645, 0.04937522221168735848, -31.94951095880158576 ) ) ;
#11729=AXIS2_PLACEMENT_3D ( 'NONE', #30178, #39744, #3960 ) ;
#11744=DIRECTION ( 'NONE',  ( 0.000000000000000000, 0.000000000000000000, 1.000000000000000000 ) ) ;
#11747=VERTEX_POINT ( 'NONE', #22681 ) ;
#11759=ORIENTED_EDGE ( 'NONE', *, *, #9218, .F. ) ;
#11760=FACE_OUTER_BOUND ( 'NONE', #2563, .T. ) ;
#11761=VERTEX_POINT ( 'NONE', #35713 ) ;
#11773=ORIENTED_EDGE ( 'NONE', *, *, #28224, .T. ) ;
#11796=CARTESIAN_POINT ( 'NONE',  ( 0.000000000000000000, 0.000000000000000000, 0.000000000000000000 ) ) ;
#11806=EDGE_CURVE ( 'NONE', #23971, #27819, #10853, .T. ) ;
#11817=CYLINDRICAL_SURFACE ( 'NONE', #41222, 31.49899999999999878 ) ;
#11820=CIRCLE ( 'NONE', #14593, 36.00000000000000000 ) ;
#11824=CARTESIAN_POINT ( 'NONE',  ( 0.000000000000000000, 0.000000000000000000, 0.000000000000000000 ) ) ;
#11830=DIRECTION ( 'NONE',  ( 0.000000000000000000, 0.000000000000000000, 1.000000000000000000 ) ) ;
#11856=ORIENTED_EDGE ( 'NONE', *, *, #5368, .F. ) ;
#11869=DIRECTION ( 'NONE',  ( -1.000000000000000000, 0.000000000000000000, 0.000000000000000000 ) ) ;
#11874=CARTESIAN_POINT ( 'NONE',  ( 0.000000000000000000, -31.81777574834303124, -2.898764365605651427 ) ) ;
#11880=FACE_OUTER_BOUND ( 'NONE', #26772, .T. ) ;
#11881=ORIENTED_EDGE ( 'NONE', *, *, #8408, .F. ) ;
#11904=CARTESIAN_POINT ( 'NONE',  ( 0.000000000000000000, 5.822172717930716779, -31.41458249383134671 ) ) ;
#11915=CARTESIAN_POINT ( 'NONE',  ( 0.000000000000000000, 0.000000000000000000, 0.000000000000000000 ) ) ;
#11916=CARTESIAN_POINT ( 'NONE',  ( 17.99999999999999645, -26.29521155129861398, 17.34211205339337880 ) ) ;
#11917=VERTEX_POINT ( 'NONE', #14139 ) ;
#11923=ADVANCED_FACE ( 'NONE', ( #20924 ), #34179, .T. ) ;
#11927=CARTESIAN_POINT ( 'NONE',  ( 8.999999999999998224, 29.09613215194482549, 21.19941258140333673 ) ) ;
#11931=CIRCLE ( 'NONE', #37676, 13.59999999999999964 ) ;
#11953=DIRECTION ( 'NONE',  ( 1.000000000000000000, 0.000000000000000000, -0.000000000000000000 ) ) ;
#11954=EDGE_LOOP ( 'NONE', ( #4744, #35261, #24919, #29226 ) ) ;
#11962=CARTESIAN_POINT ( 'NONE',  ( 17.99999999999999645, 0.000000000000000000, 0.000000000000000000 ) ) ;
#11967=DIRECTION ( 'NONE',  ( 0.000000000000000000, 0.000000000000000000, 1.000000000000000000 ) ) ;
#11968=AXIS2_PLACEMENT_3D ( 'NONE', #11915, #25241, #22185 ) ;
#11975=ADVANCED_FACE ( 'NONE', ( #34609 ), #4723, .T. ) ;
#11986=DIRECTION ( 'NONE',  ( -1.000000000000000000, 0.000000000000000000, -0.000000000000000000 ) ) ;
#11994=ORIENTED_EDGE ( 'NONE', *, *, #6365, .F. ) ;
#11997=ORIENTED_EDGE ( 'NONE', *, *, #39060, .F. ) ;
#12007=DIRECTION ( 'NONE',  ( -1.000000000000000000, 0.000000000000000000, 0.000000000000000000 ) ) ;
#12008=ADVANCED_FACE ( 'NONE', ( #18299 ), #1438, .T. ) ;
#12013=VERTEX_POINT ( 'NONE', #41137 ) ;
#12017=ORIENTED_EDGE ( 'NONE', *, *, #11806, .F. ) ;
#12023=CARTESIAN_POINT ( 'NONE',  ( 0.000000000000000000, 31.80866420683990725, 2.997093558041416195 ) ) ;
#12029=UNCERTAINTY_MEASURE_WITH_UNIT (LENGTH_MEASURE( 1.000000000000000082E-05 ), #3755, 'distance_accuracy_value', 'NONE');
#12034=FACE_OUTER_BOUND ( 'NONE', #23989, .T. ) ;
#12045=CARTESIAN_POINT ( 'NONE',  ( 17.99999999999999645, 0.000000000000000000, 0.000000000000000000 ) ) ;
#12052=CIRCLE ( 'NONE', #28782, 13.60000000000000142 ) ;
#12057=CARTESIAN_POINT ( 'NONE',  ( 0.000000000000000000, 28.57802095670106723, -14.28532136906642691 ) ) ;
#12058=ORIENTED_EDGE ( 'NONE', *, *, #30962, .F. ) ;
#12063=VERTEX_POINT ( 'NONE', #7991 ) ;
#12074=CARTESIAN_POINT ( 'NONE',  ( 17.99999999999999645, 0.000000000000000000, 0.000000000000000000 ) ) ;
#12078=CARTESIAN_POINT ( 'NONE',  ( 17.99999999999999645, 0.000000000000000000, 0.000000000000000000 ) ) ;
#12098=DIRECTION ( 'NONE',  ( 0.000000000000000000, 0.3612416661871538093, -0.9324722294043554793 ) ) ;
#12104=ORIENTED_EDGE ( 'NONE', *, *, #37550, .F. ) ;
#12106=EDGE_CURVE ( 'NONE', #40378, #4807, #26079, .T. ) ;
#12114=DIRECTION ( 'NONE',  ( 1.000000000000000000, 0.000000000000000000, 0.000000000000000000 ) ) ;
#12125=VERTEX_POINT ( 'NONE', #2917 ) ;
#12127=DIRECTION ( 'NONE',  ( -1.000000000000000000, -0.000000000000000000, -0.000000000000000000 ) ) ;
#12139=CARTESIAN_POINT ( 'NONE',  ( 17.99999999999999645, 9.484061862023926537, 30.03730300138984433 ) ) ;
#12156=EDGE_CURVE ( 'NONE', #16072, #40285, #22419, .T. ) ;
#12158=EDGE_CURVE ( 'NONE', #16458, #17796, #19157, .T. ) ;
#12162=VERTEX_POINT ( 'NONE', #12785 ) ;
#12178=DIRECTION ( 'NONE',  ( -1.000000000000000000, -0.000000000000000000, 0.000000000000000000 ) ) ;
#12201=VERTEX_POINT ( 'NONE', #42213 ) ;
#12207=ADVANCED_FACE ( 'NONE', ( #22631 ), #9499, .T. ) ;
#12208=CARTESIAN_POINT ( 'NONE',  ( 17.99999999999999645, 0.000000000000000000, 0.000000000000000000 ) ) ;
#12213=DIRECTION ( 'NONE',  ( 1.000000000000000000, -0.000000000000000000, -0.000000000000000000 ) ) ;
#12218=VERTEX_POINT ( 'NONE', #30017 ) ;
#12224=AXIS2_PLACEMENT_3D ( 'NONE', #38647, #2202, #25187 ) ;
#12275=DIRECTION ( 'NONE',  ( -1.000000000000000000, 0.000000000000000000, 0.000000000000000000 ) ) ;
#12290=CARTESIAN_POINT ( 'NONE',  ( -10.00000000000000000, 0.000000000000000000, 0.000000000000000000 ) ) ;
#12298=VECTOR ( 'NONE', #17005, 1000.000000000000000 ) ;
#12316=CARTESIAN_POINT ( 'NONE',  ( 17.99999999999999645, 0.000000000000000000, 0.000000000000000000 ) ) ;
#12324=EDGE_CURVE ( 'NONE', #31747, #19127, #9329, .T. ) ;
#12327=ORIENTED_EDGE ( 'NONE', *, *, #41149, .F. ) ;
#12333=VERTEX_POINT ( 'NONE', #6865 ) ;
#12335=ORIENTED_EDGE ( 'NONE', *, *, #40108, .T. ) ;
#12337=ORIENTED_EDGE ( 'NONE', *, *, #3824, .T. ) ;
#12347=CARTESIAN_POINT ( 'NONE',  ( 17.99999999999999645, -7.749090474611724844, 30.53094492177211094 ) ) ;
#12348=ORIENTED_EDGE ( 'NONE', *, *, #29913, .T. ) ;
#12361=CIRCLE ( 'NONE', #13077, 36.00000000000000000 ) ;
#12363=CARTESIAN_POINT ( 'NONE',  ( 0.000000000000000000, 18.25486108452660972, -25.66996392254254644 ) ) ;
#12364=AXIS2_PLACEMENT_3D ( 'NONE', #4167, #17752, #39588 ) ;
#12396=DIRECTION ( 'NONE',  ( 0.000000000000000000, -6.982962677686266711E-15, 1.000000000000000000 ) ) ;
#12403=CARTESIAN_POINT ( 'NONE',  ( 0.000000000000000000, 0.000000000000000000, 36.00000000000000000 ) ) ;
#12405=EDGE_CURVE ( 'NONE', #6807, #6792, #34338, .T. ) ;
#12429=DIRECTION ( 'NONE',  ( -1.000000000000000000, 0.000000000000000000, -0.000000000000000000 ) ) ;
#12433=DIRECTION ( 'NONE',  ( -1.000000000000000000, -0.000000000000000000, -0.000000000000000000 ) ) ;
#12443=EDGE_CURVE ( 'NONE', #16643, #43048, #14290, .T. ) ;
#12445=AXIS2_PLACEMENT_3D ( 'NONE', #38944, #22210, #25686 ) ;
#12455=ORIENTED_EDGE ( 'NONE', *, *, #19034, .T. ) ;
#12456=DIRECTION ( 'NONE',  ( -1.000000000000000000, 0.000000000000000000, 0.000000000000000000 ) ) ;
#12461=VERTEX_POINT ( 'NONE', #25217 ) ;
#12473=AXIS2_PLACEMENT_3D ( 'NONE', #29320, #12956, #25847 ) ;
#12474=DIRECTION ( 'NONE',  ( 0.000000000000000000, 0.000000000000000000, 1.000000000000000000 ) ) ;
#12484=ORIENTED_EDGE ( 'NONE', *, *, #33087, .F. ) ;
#12495=AXIS2_PLACEMENT_3D ( 'NONE', #13454, #17395, #37409 ) ;
#12502=CARTESIAN_POINT ( 'NONE',  ( 17.99999999999999645, 0.04937522221168735848, -31.94951095880158576 ) ) ;
#12529=DIRECTION ( 'NONE',  ( -1.000000000000000000, 0.000000000000000000, -0.000000000000000000 ) ) ;
#12530=ORIENTED_EDGE ( 'NONE', *, *, #41605, .F. ) ;
#12535=CARTESIAN_POINT ( 'NONE',  ( 0.000000000000000000, -28.62203781742993414, -14.19692359621484989 ) ) ;
#12544=CARTESIAN_POINT ( 'NONE',  ( 17.99999999999999645, -23.87611429743648017, -20.54551452399645939 ) ) ;
#12552=CIRCLE ( 'NONE', #20929, 36.00000000000000000 ) ;
#12563=CARTESIAN_POINT ( 'NONE',  ( 17.99999999999999645, 29.03409033315599075, -12.21509719675360373 ) ) ;
#12568=ORIENTED_EDGE ( 'NONE', *, *, #1189, .T. ) ;
#12578=DIRECTION ( 'NONE',  ( 0.000000000000000000, -0.5264321628773447337, -0.8502171357296209875 ) ) ;
#12583=VECTOR ( 'NONE', #14210, 1000.000000000000000 ) ;
#12585=VECTOR ( 'NONE', #22526, 1000.000000000000000 ) ;
#12628=ORIENTED_EDGE ( 'NONE', *, *, #38502, .T. ) ;
#12632=FACE_OUTER_BOUND ( 'NONE', #20658, .T. ) ;
#12644=CARTESIAN_POINT ( 'NONE',  ( 17.99999999999999645, 11.49545354908979888, -29.80986809967247453 ) ) ;
#12645=EDGE_CURVE ( 'NONE', #18492, #5647, #16019, .T. ) ;
#12671=CARTESIAN_POINT ( 'NONE',  ( 17.99999999999999645, -29.68570942776479527, 10.53307442156924267 ) ) ;
#12674=ORIENTED_EDGE ( 'NONE', *, *, #39347, .F. ) ;
#12676=AXIS2_PLACEMENT_3D ( 'NONE', #32947, #13133, #26425 ) ;
#12684=ORIENTED_EDGE ( 'NONE', *, *, #8849, .F. ) ;
#12696=CIRCLE ( 'NONE', #14113, 31.49900000000000588 ) ;
#12709=ADVANCED_FACE ( 'NONE', ( #32987 ), #14631, .T. ) ;
#12724=LINE ( 'NONE', #26890, #18824 ) ;
#12734=DIRECTION ( 'NONE',  ( -1.000000000000000000, 0.000000000000000000, -0.000000000000000000 ) ) ;
#12736=ORIENTED_EDGE ( 'NONE', *, *, #1893, .F. ) ;
#12756=ORIENTED_EDGE ( 'NONE', *, *, #24944, .T. ) ;
#12766=CARTESIAN_POINT ( 'NONE',  ( 0.000000000000000000, -23.87611429743648017, -20.54551452399645939 ) ) ;
#12771=SURFACE_SIDE_STYLE ('',( #42831 ) ) ;
#12785=CARTESIAN_POINT ( 'NONE',  ( 17.99999999999999645, 23.87611429743662939, 20.54551452399628531 ) ) ;
#12788=ORIENTED_EDGE ( 'NONE', *, *, #7719, .T. ) ;
#12806=DIRECTION ( 'NONE',  ( -1.000000000000000000, 0.000000000000000000, 0.000000000000000000 ) ) ;
#12807=ORIENTED_EDGE ( 'NONE', *, *, #14034, .T. ) ;
#12808=ORIENTED_EDGE ( 'NONE', *, *, #12324, .T. ) ;
#12809=DIRECTION ( 'NONE',  ( -1.000000000000000000, 0.000000000000000000, 0.000000000000000000 ) ) ;
#12820=ORIENTED_EDGE ( 'NONE', *, *, #41596, .T. ) ;
#12831=CARTESIAN_POINT ( 'NONE',  ( 17.99999999999999645, 25.46650492921924425, -19.29328419707757547 ) ) ;
#12837=VERTEX_POINT ( 'NONE', #40983 ) ;
#12841=LINE ( 'NONE', #39424, #3103 ) ;
#12853=DIRECTION ( 'NONE',  ( -1.000000000000000000, 0.000000000000000000, 0.000000000000000000 ) ) ;
#12869=AXIS2_PLACEMENT_3D ( 'NONE', #35276, #28112, #1459 ) ;
#12891=CIRCLE ( 'NONE', #18508, 31.49900000000000233 ) ;
#12893=AXIS2_PLACEMENT_3D ( 'NONE', #42456, #25915, #9299 ) ;
#12909=VERTEX_POINT ( 'NONE', #2333 ) ;
#12933=ORIENTED_EDGE ( 'NONE', *, *, #36715, .T. ) ;
#12936=VECTOR ( 'NONE', #26133, 1000.000000000000000 ) ;
#12954=CYLINDRICAL_SURFACE ( 'NONE', #2644, 13.59999999999999787 ) ;
#12956=DIRECTION ( 'NONE',  ( -1.000000000000000000, 0.000000000000000000, -0.000000000000000000 ) ) ;
#12962=LINE ( 'NONE', #16456, #25699 ) ;
#12991=LINE ( 'NONE', #4365, #9305 ) ;
#12997=DIRECTION ( 'NONE',  ( -1.000000000000000000, 0.000000000000000000, 0.000000000000000000 ) ) ;
#13000=ADVANCED_FACE ( 'NONE', ( #34672 ), #11560, .T. ) ;
#13007=DIRECTION ( 'NONE',  ( 0.000000000000000000, -0.5264321628773627193, 0.8502171357296098853 ) ) ;
#13012=DIRECTION ( 'NONE',  ( -1.000000000000000000, 0.000000000000000000, -0.000000000000000000 ) ) ;
#13013=AXIS2_PLACEMENT_3D ( 'NONE', #33550, #33762, #16797 ) ;
#13015=ORIENTED_EDGE ( 'NONE', *, *, #42187, .F. ) ;
#13021=DIRECTION ( 'NONE',  ( 0.000000000000000000, 0.000000000000000000, 1.000000000000000000 ) ) ;
#13023=CARTESIAN_POINT ( 'NONE',  ( 8.999999999999998224, -13.57797752207946829, 33.34124362422470256 ) ) ;
#13025=ADVANCED_FACE ( 'NONE', ( #33104 ), #43132, .T. ) ;
#13028=EDGE_LOOP ( 'NONE', ( #6266, #21650, #42059, #16947 ) ) ;
#13033=VECTOR ( 'NONE', #4761, 1000.000000000000000 ) ;
#13043=AXIS2_PLACEMENT_3D ( 'NONE', #11290, #37876, #25477 ) ;
#13045=CARTESIAN_POINT ( 'NONE',  ( 0.000000000000000000, 21.56073507908678977, -23.57770962728541875 ) ) ;
#13047=CARTESIAN_POINT ( 'NONE',  ( 0.000000000000000000, -28.35267316522799419, 22.18391138608698299 ) ) ;
#13048=AXIS2_PLACEMENT_3D ( 'NONE', #2782, #13518, #26394 ) ;
#13067=EDGE_CURVE ( 'NONE', #42608, #39242, #22675, .T. ) ;
#13077=AXIS2_PLACEMENT_3D ( 'NONE', #18465, #1828, #38266 ) ;
#13079=VERTEX_POINT ( 'NONE', #3416 ) ;
#13080=DIRECTION ( 'NONE',  ( -1.000000000000000000, 0.000000000000000000, 0.000000000000000000 ) ) ;
#13089=VERTEX_POINT ( 'NONE', #16786 ) ;
#13102=CIRCLE ( 'NONE', #43012, 13.60000000000000142 ) ;
#13106=ORIENTED_EDGE ( 'NONE', *, *, #5706, .T. ) ;
#13109=ADVANCED_FACE ( 'NONE', ( #39001 ), #32467, .T. ) ;
#13110=DIRECTION ( 'NONE',  ( -1.000000000000000000, -0.000000000000000000, 0.000000000000000000 ) ) ;
#13115=VERTEX_POINT ( 'NONE', #22915 ) ;
#13122=EDGE_CURVE ( 'NONE', #7021, #17035, #29215, .T. ) ;
#13124=LINE ( 'NONE', #16625, #12585 ) ;
#13133=DIRECTION ( 'NONE',  ( -1.000000000000000000, -0.000000000000000000, 0.000000000000000000 ) ) ;
#13143=FACE_OUTER_BOUND ( 'NONE', #26535, .T. ) ;
#13168=ORIENTED_EDGE ( 'NONE', *, *, #13246, .T. ) ;
#13170=EDGE_CURVE ( 'NONE', #16404, #26405, #12841, .T. ) ;
#13173=CARTESIAN_POINT ( 'NONE',  ( 50.00005079999999680, 0.000000000000000000, 0.000000000000000000 ) ) ;
#13184=DIRECTION ( 'NONE',  ( 0.000000000000000000, 0.000000000000000000, 1.000000000000000000 ) ) ;
#13188=AXIS2_PLACEMENT_3D ( 'NONE', #14959, #25222, #4440 ) ;
#13189=CARTESIAN_POINT ( 'NONE',  ( 17.99999999999999645, 7.749090474611950441, -30.53094492177204700 ) ) ;
#13191=ORIENTED_EDGE ( 'NONE', *, *, #25577, .T. ) ;
#13214=AXIS2_PLACEMENT_3D ( 'NONE', #10070, #23000, #20161 ) ;
#13216=ADVANCED_FACE ( 'NONE', ( #37235 ), #23756, .T. ) ;
#13228=VERTEX_POINT ( 'NONE', #24191 ) ;
#13230=ORIENTED_EDGE ( 'NONE', *, *, #4697, .T. ) ;
#13234=EDGE_LOOP ( 'NONE', ( #40513, #13106, #32092, #20828 ) ) ;
#13246=EDGE_CURVE ( 'NONE', #7956, #40062, #33974, .T. ) ;
#13254=DIRECTION ( 'NONE',  ( -1.000000000000000000, 0.000000000000000000, -0.000000000000000000 ) ) ;
#13265=DIRECTION ( 'NONE',  ( -1.000000000000000000, 0.000000000000000000, -0.000000000000000000 ) ) ;
#13266=EDGE_LOOP ( 'NONE', ( #38159, #12628, #6831, #11277 ) ) ;
#13272=EDGE_CURVE ( 'NONE', #13089, #6694, #30920, .T. ) ;
#13291=DIRECTION ( 'NONE',  ( -1.000000000000000000, -0.000000000000000000, -0.000000000000000000 ) ) ;
#13302=ORIENTED_EDGE ( 'NONE', *, *, #12158, .T. ) ;
#13312=AXIS2_PLACEMENT_3D ( 'NONE', #23125, #8927, #36374 ) ;
#13315=DIRECTION ( 'NONE',  ( -1.000000000000000000, 0.000000000000000000, 0.000000000000000000 ) ) ;
#13316=ORIENTED_EDGE ( 'NONE', *, *, #38502, .F. ) ;
#13332=CARTESIAN_POINT ( 'NONE',  ( 17.99999999999999645, 0.000000000000000000, 0.000000000000000000 ) ) ;
#13350=ADVANCED_FACE ( 'NONE', ( #15246 ), #5153, .T. ) ;
#13353=CYLINDRICAL_SURFACE ( 'NONE', #673, 36.00000000000000000 ) ;
#13360=EDGE_CURVE ( 'NONE', #27819, #35211, #8060, .T. ) ;
#13365=DIRECTION ( 'NONE',  ( 0.000000000000000000, 0.000000000000000000, 1.000000000000000000 ) ) ;
#13366=CARTESIAN_POINT ( 'NONE',  ( 0.000000000000000000, 2.007101075699966763, 31.43498920425970411 ) ) ;
#13367=LINE ( 'NONE', #22992, #8910 ) ;
#13372=VERTEX_POINT ( 'NONE', #41804 ) ;
#13376=CARTESIAN_POINT ( 'NONE',  ( 0.000000000000000000, 27.24480646643629811, -15.80846360676556372 ) ) ;
#13377=ADVANCED_FACE ( 'NONE', ( #32001 ), #18519, .T. ) ;
#13391=CIRCLE ( 'NONE', #21083, 31.49900000000000233 ) ;
#13393=DIRECTION ( 'NONE',  ( 0.000000000000000000, 0.5264321628773569461, -0.8502171357296133269 ) ) ;
#13395=EDGE_CURVE ( 'NONE', #10692, #1826, #28540, .T. ) ;
#13407=EDGE_CURVE ( 'NONE', #8083, #39631, #31145, .T. ) ;
#13419=DIRECTION ( 'NONE',  ( 0.000000000000000000, 0.1837495178165637066, 0.9829730996839030066 ) ) ;
#13429=AXIS2_PLACEMENT_3D ( 'NONE', #27287, #40557, #36869 ) ;
#13433=AXIS2_PLACEMENT_3D ( 'NONE', #15322, #38188, #28612 ) ;
#13435=DIRECTION ( 'NONE',  ( 1.000000000000000000, 0.000000000000000000, 0.000000000000000000 ) ) ;
#13445=DIRECTION ( 'NONE',  ( -1.000000000000000000, -0.000000000000000000, 0.000000000000000000 ) ) ;
#13449=CARTESIAN_POINT ( 'NONE',  ( 17.99999999999999645, 0.000000000000000000, 0.000000000000000000 ) ) ;
#13454=CARTESIAN_POINT ( 'NONE',  ( 17.99999999999999645, 25.46650492921896713, 19.29328419707794495 ) ) ;
#13459=EDGE_CURVE ( 'NONE', #4224, #39574, #8744, .T. ) ;
#13461=ORIENTED_EDGE ( 'NONE', *, *, #6908, .T. ) ;
#13471=VERTEX_POINT ( 'NONE', #34323 ) ;
#13511=ADVANCED_FACE ( 'NONE', ( #21286 ), #17790, .T. ) ;
#13518=DIRECTION ( 'NONE',  ( -1.000000000000000000, -0.000000000000000000, -0.000000000000000000 ) ) ;
#13528=EDGE_CURVE ( 'NONE', #18562, #4807, #14277, .T. ) ;
#13531=CARTESIAN_POINT ( 'NONE',  ( 0.000000000000000000, 0.000000000000000000, 0.000000000000000000 ) ) ;
#13552=AXIS2_PLACEMENT_3D ( 'NONE', #3852, #14597, #10213 ) ;
#13553=DIRECTION ( 'NONE',  ( -1.000000000000000000, -0.000000000000000000, -0.000000000000000000 ) ) ;
#13558=DIRECTION ( 'NONE',  ( -1.000000000000000000, -0.000000000000000000, 0.000000000000000000 ) ) ;
#13560=CIRCLE ( 'NONE', #27474, 13.59999999999999964 ) ;
#13573=ORIENTED_EDGE ( 'NONE', *, *, #30632, .F. ) ;
#13579=DIRECTION ( 'NONE',  ( -1.000000000000000000, 0.000000000000000000, 0.000000000000000000 ) ) ;
#13583=AXIS2_PLACEMENT_3D ( 'NONE', #25001, #31291, #35180 ) ;
#13607=CARTESIAN_POINT ( 'NONE',  ( -10.00000000000000000, 0.000000000000000000, 0.000000000000000000 ) ) ;
#13613=FACE_OUTER_BOUND ( 'NONE', #11724, .T. ) ;
#13623=VECTOR ( 'NONE', #15331, 1000.000000000000000 ) ;
#13630=CARTESIAN_POINT ( 'NONE',  ( 0.000000000000000000, 31.48608500567870294, -0.9019157472705674472 ) ) ;
#13641=EDGE_CURVE ( 'NONE', #33690, #37185, #23444, .T. ) ;
#13646=DIRECTION ( 'NONE',  ( -1.000000000000000000, -0.000000000000000000, -0.000000000000000000 ) ) ;
#13648=CARTESIAN_POINT ( 'NONE',  ( 0.000000000000000000, -14.84191762912296930, -27.78316904333141224 ) ) ;
#13658=FACE_OUTER_BOUND ( 'NONE', #27503, .T. ) ;
#13663=CARTESIAN_POINT ( 'NONE',  ( 0.000000000000000000, 0.000000000000000000, 0.000000000000000000 ) ) ;
#13669=CARTESIAN_POINT ( 'NONE',  ( 17.99999999999999645, 21.56073507908645936, 23.57770962728572428 ) ) ;
#13672=DIRECTION ( 'NONE',  ( 0.000000000000000000, 0.9618256431728199329, -0.2736629900720800590 ) ) ;
#13676=DIRECTION ( 'NONE',  ( -1.000000000000000000, 0.000000000000000000, 0.000000000000000000 ) ) ;
#13693=CARTESIAN_POINT ( 'NONE',  ( 17.99999999999999645, 0.000000000000000000, 0.000000000000000000 ) ) ;
#13694=AXIS2_PLACEMENT_3D ( 'NONE', #41191, #27486, #30328 ) ;
#13695=ORIENTED_EDGE ( 'NONE', *, *, #27567, .T. ) ;
#13709=DIRECTION ( 'NONE',  ( 0.000000000000000000, 0.000000000000000000, 1.000000000000000000 ) ) ;
#13715=DIRECTION ( 'NONE',  ( 0.000000000000000000, -0.9618256431728219313, 0.2736629900720728981 ) ) ;
#13719=DIRECTION ( 'NONE',  ( -1.000000000000000000, 0.000000000000000000, 0.000000000000000000 ) ) ;
#13741=MANIFOLD_SOLID_BREP ( 'Bore', #5156 ) ;
#13748=DIRECTION ( 'NONE',  ( -1.000000000000000000, -0.000000000000000000, -0.000000000000000000 ) ) ;
#13750=VECTOR ( 'NONE', #41360, 1000.000000000000000 ) ;
#13757=AXIS2_PLACEMENT_3D ( 'NONE', #20019, #2927, #26328 ) ;
#13763=CIRCLE ( 'NONE', #7375, 31.49899999999999878 ) ;
#13768=EDGE_LOOP ( 'NONE', ( #39089, #40273, #20241, #11360 ) ) ;
#13772=ORIENTED_EDGE ( 'NONE', *, *, #38687, .F. ) ;
#13779=DIRECTION ( 'NONE',  ( 0.000000000000000000, 0.5264321628773506179, 0.8502171357296174348 ) ) ;
#13806=CARTESIAN_POINT ( 'NONE',  ( 0.000000000000000000, 28.35267316522815406, -22.18391138608678403 ) ) ;
#13813=CARTESIAN_POINT ( 'NONE',  ( 0.000000000000000000, -31.11570115861498920, 4.898994019976531611 ) ) ;
#13814=CIRCLE ( 'NONE', #11729, 36.00000000000000000 ) ;
#13822=CIRCLE ( 'NONE', #7529, 13.60000000000000142 ) ;
#13823=EDGE_LOOP ( 'NONE', ( #23386, #24358, #34795, #28290 ) ) ;
#13844=ORIENTED_EDGE ( 'NONE', *, *, #40250, .T. ) ;
#13845=CARTESIAN_POINT ( 'NONE',  ( 0.000000000000000000, -34.78944633786272789, -9.257128253673986507 ) ) ;
#13864=ORIENTED_EDGE ( 'NONE', *, *, #21608, .T. ) ;
#13865=DIRECTION ( 'NONE',  ( -1.000000000000000000, -0.000000000000000000, 0.000000000000000000 ) ) ;
#13868=CARTESIAN_POINT ( 'NONE',  ( 0.000000000000000000, 0.000000000000000000, 0.000000000000000000 ) ) ;
#13872=PRESENTATION_STYLE_ASSIGNMENT (( #937 ) ) ;
#13881=LINE ( 'NONE', #30661, #33943 ) ;
#13898=EDGE_LOOP ( 'NONE', ( #8784, #11629, #12933, #26310 ) ) ;
#13903=DIRECTION ( 'NONE',  ( 0.000000000000000000, 0.8951632913550604531, 0.4457383557765421944 ) ) ;
#13908=DIRECTION ( 'NONE',  ( -1.000000000000000000, 0.000000000000000000, 0.000000000000000000 ) ) ;
#13939=CARTESIAN_POINT ( 'NONE',  ( 0.000000000000000000, 12.42760411676086818, -33.78690065568411427 ) ) ;
#13941=CARTESIAN_POINT ( 'NONE',  ( 17.99999999999999645, -29.09613215194468339, -21.19941258140352858 ) ) ;
#13944=VERTEX_POINT ( 'NONE', #18039 ) ;
#13956=DIRECTION ( 'NONE',  ( 0.000000000000000000, 0.9957341762950341346, 0.09226835946330559646 ) ) ;
#13965=EDGE_LOOP ( 'NONE', ( #21962, #13302, #4339, #4539 ) ) ;
#13980=DIRECTION ( 'NONE',  ( 0.000000000000000000, 0.000000000000000000, 1.000000000000000000 ) ) ;
#13992=AXIS2_PLACEMENT_3D ( 'NONE', #11796, #25124, #8487 ) ;
#14000=EDGE_LOOP ( 'NONE', ( #3538, #41211, #4527, #13844 ) ) ;
#14006=EDGE_CURVE ( 'NONE', #16643, #34774, #22802, .T. ) ;
#14007=DIRECTION ( 'NONE',  ( -1.000000000000000000, 0.000000000000000000, 0.000000000000000000 ) ) ;
#14011=CIRCLE ( 'NONE', #15402, 36.00000000000000000 ) ;
#14017=CIRCLE ( 'NONE', #36271, 36.00000000000000000 ) ;
#14020=AXIS2_PLACEMENT_3D ( 'NONE', #32378, #28708, #41974 ) ;
#14034=EDGE_CURVE ( 'NONE', #20730, #20374, #3201, .T. ) ;
#14035=CARTESIAN_POINT ( 'NONE',  ( 0.000000000000000000, -0.6168405712489287707, 35.99471499692226217 ) ) ;
#14039=ORIENTED_EDGE ( 'NONE', *, *, #16011, .F. ) ;
#14052=VERTEX_POINT ( 'NONE', #22787 ) ;
#14062=EDGE_CURVE ( 'NONE', #36837, #33813, #3510, .T. ) ;
#14074=EDGE_LOOP ( 'NONE', ( #19931, #19634, #40276, #2348 ) ) ;
#14079=CYLINDRICAL_SURFACE ( 'NONE', #41468, 13.60000000000000142 ) ;
#14082=CIRCLE ( 'NONE', #5701, 31.49899999999999878 ) ;
#14107=EDGE_LOOP ( 'NONE', ( #39642, #37756, #35096, #12337 ) ) ;
#14113=AXIS2_PLACEMENT_3D ( 'NONE', #12074, #26226, #8995 ) ;
#14133=CARTESIAN_POINT ( 'NONE',  ( 17.99999999999999645, 0.000000000000000000, 0.000000000000000000 ) ) ;
#14139=CARTESIAN_POINT ( 'NONE',  ( 0.000000000000000000, -13.22719389141960100, -28.58720592780609593 ) ) ;
#14141=CIRCLE ( 'NONE', #24619, 36.00000000000000000 ) ;
#14146=CIRCLE ( 'NONE', #32921, 36.00000000000000000 ) ;
#14150=LINE ( 'NONE', #1239, #10788 ) ;
#14160=ORIENTED_EDGE ( 'NONE', *, *, #33807, .T. ) ;
#14161=ORIENTED_EDGE ( 'NONE', *, *, #11286, .F. ) ;
#14200=CARTESIAN_POINT ( 'NONE',  ( 17.99999999999999645, 0.04937522221122418731, 31.94951095880159286 ) ) ;
#14209=ORIENTED_EDGE ( 'NONE', *, *, #7900, .F. ) ;
#14210=DIRECTION ( 'NONE',  ( 1.000000000000000000, -0.000000000000000000, -0.000000000000000000 ) ) ;
#14225=DIRECTION ( 'NONE',  ( -1.000000000000000000, 0.000000000000000000, 0.000000000000000000 ) ) ;
#14228=VERTEX_POINT ( 'NONE', #41899 ) ;
#14239=DIRECTION ( 'NONE',  ( -1.000000000000000000, 0.000000000000000000, 0.000000000000000000 ) ) ;
#14246=DIRECTION ( 'NONE',  ( 0.000000000000000000, 0.000000000000000000, 1.000000000000000000 ) ) ;
#14253=ORIENTED_EDGE ( 'NONE', *, *, #25492, .F. ) ;
#14274=CARTESIAN_POINT ( 'NONE',  ( -10.00000000000000000, 0.000000000000000000, 0.000000000000000000 ) ) ;
#14277=LINE ( 'NONE', #27158, #33812 ) ;
#14290=LINE ( 'NONE', #24355, #27479 ) ;
#14309=ORIENTED_EDGE ( 'NONE', *, *, #5706, .F. ) ;
#14316=CARTESIAN_POINT ( 'NONE',  ( 0.000000000000000000, -25.52601536738579213, -19.21447964122724272 ) ) ;
#14321=EDGE_CURVE ( 'NONE', #34774, #30296, #30471, .T. ) ;
#14323=CARTESIAN_POINT ( 'NONE',  ( 17.99999999999999645, 0.000000000000000000, 0.000000000000000000 ) ) ;
#14339=LINE ( 'NONE', #1428, #3068 ) ;
#14350=DIRECTION ( 'NONE',  ( 0.000000000000000000, 0.000000000000000000, 1.000000000000000000 ) ) ;
#14363=CARTESIAN_POINT ( 'NONE',  ( 0.000000000000000000, 19.69434969228073484, 24.58291258574055860 ) ) ;
#14364=ORIENTED_EDGE ( 'NONE', *, *, #9989, .T. ) ;
#14366=CARTESIAN_POINT ( 'NONE',  ( 17.99999999999999645, -25.46650492921884279, -19.29328419707811193 ) ) ;
#14371=ORIENTED_EDGE ( 'NONE', *, *, #6241, .F. ) ;
#14382=CIRCLE ( 'NONE', #34565, 13.59999999999999787 ) ;
#14384=ORIENTED_EDGE ( 'NONE', *, *, #27567, .F. ) ;
#14386=DIRECTION ( 'NONE',  ( 0.000000000000000000, -0.6736956436465478815, -0.7390089172206675272 ) ) ;
#14392=ORIENTED_EDGE ( 'NONE', *, *, #9014, .T. ) ;
#14400=ORIENTED_EDGE ( 'NONE', *, *, #1170, .F. ) ;
#14407=DIRECTION ( 'NONE',  ( 0.000000000000000000, 0.000000000000000000, 1.000000000000000000 ) ) ;
#14413=EDGE_CURVE ( 'NONE', #7766, #26460, #29754, .T. ) ;
#14430=DIRECTION ( 'NONE',  ( -1.000000000000000000, 0.000000000000000000, 0.000000000000000000 ) ) ;
#14437=ORIENTED_EDGE ( 'NONE', *, *, #14504, .T. ) ;
#14441=AXIS2_PLACEMENT_3D ( 'NONE', #19789, #33054, #22866 ) ;
#14447=VERTEX_POINT ( 'NONE', #19461 ) ;
#14448=ADVANCED_FACE ( 'NONE', ( #39246 ), #32726, .T. ) ;
#14454=CYLINDRICAL_SURFACE ( 'NONE', #38617, 13.59999999999999964 ) ;
#14460=CYLINDRICAL_SURFACE ( 'NONE', #11568, 36.00000000000000000 ) ;
#14464=DIRECTION ( 'NONE',  ( 0.000000000000000000, 0.000000000000000000, 1.000000000000000000 ) ) ;
#14466=CARTESIAN_POINT ( 'NONE',  ( 8.999999999999998224, 19.47322409167269441, 30.27859877001407796 ) ) ;
#14474=DIRECTION ( 'NONE',  ( 0.000000000000000000, 0.000000000000000000, 1.000000000000000000 ) ) ;
#14488=EDGE_LOOP ( 'NONE', ( #8951, #12017, #40127, #33444 ) ) ;
#14495=ORIENTED_EDGE ( 'NONE', *, *, #4487, .T. ) ;
#14504=EDGE_CURVE ( 'NONE', #14228, #20215, #24205, .T. ) ;
#14506=DIRECTION ( 'NONE',  ( -1.000000000000000000, -0.000000000000000000, 0.000000000000000000 ) ) ;
#14535=AXIS2_PLACEMENT_3D ( 'NONE', #12208, #25531, #41412 ) ;
#14542=ORIENTED_EDGE ( 'NONE', *, *, #28224, .F. ) ;
#14556=VERTEX_POINT ( 'NONE', #7344 ) ;
#14562=AXIS2_PLACEMENT_3D ( 'NONE', #24032, #31212, #24687 ) ;
#14573=CARTESIAN_POINT ( 'NONE',  ( 0.000000000000000000, 0.000000000000000000, 15.00000000000000000 ) ) ;
#14591=ORIENTED_EDGE ( 'NONE', *, *, #6860, .F. ) ;
#14593=AXIS2_PLACEMENT_3D ( 'NONE', #30881, #20892, #33704 ) ;
#14597=DIRECTION ( 'NONE',  ( 0.000000000000000000, 0.000000000000000000, 1.000000000000000000 ) ) ;
#14600=EDGE_CURVE ( 'NONE', #9115, #3440, #2589, .T. ) ;
#14610=DIRECTION ( 'NONE',  ( -1.000000000000000000, 0.000000000000000000, 0.000000000000000000 ) ) ;
#14615=ADVANCED_FACE ( 'NONE', ( #30711 ), #31142, .T. ) ;
#14629=EDGE_CURVE ( 'NONE', #14052, #18492, #27016, .T. ) ;
#14631=CYLINDRICAL_SURFACE ( 'NONE', #15689, 31.49899999999999878 ) ;
#14637=DIRECTION ( 'NONE',  ( 0.000000000000000000, 0.3612416661871471479, 0.9324722294043581439 ) ) ;
#14644=CARTESIAN_POINT ( 'NONE',  ( 9.000000000000000000, -31.94619804602776725, 16.59639811537345366 ) ) ;
#14662=ORIENTED_EDGE ( 'NONE', *, *, #24719, .T. ) ;
#14669=EDGE_LOOP ( 'NONE', ( #18523, #13015, #1173, #30310 ) ) ;
#14679=DIRECTION ( 'NONE',  ( 0.000000000000000000, 0.000000000000000000, -1.000000000000000000 ) ) ;
#14686=EDGE_CURVE ( 'NONE', #21082, #8807, #9593, .T. ) ;
#14696=DIRECTION ( 'NONE',  ( -1.000000000000000000, 0.000000000000000000, 0.000000000000000000 ) ) ;
#14731=ORIENTED_EDGE ( 'NONE', *, *, #29228, .F. ) ;
#14747=AXIS2_PLACEMENT_3D ( 'NONE', #15453, #42010, #38745 ) ;
#14769=LINE ( 'NONE', #18281, #16129 ) ;
#14773=AXIS2_PLACEMENT_3D ( 'NONE', #5917, #9637, #29288 ) ;
#14782=CARTESIAN_POINT ( 'NONE',  ( 17.99999999999999645, -18.42432724429495750, 30.92804820215996742 ) ) ;
#14800=LINE ( 'NONE', #38322, #25227 ) ;
#14808=CARTESIAN_POINT ( 'NONE',  ( 17.99999999999999645, -14.84191762912334767, 27.78316904333121684 ) ) ;
#14810=DIRECTION ( 'NONE',  ( -1.000000000000000000, 0.000000000000000000, 0.000000000000000000 ) ) ;
#14822=CARTESIAN_POINT ( 'NONE',  ( 0.000000000000000000, 3.803237743091921086, 31.26855263151016118 ) ) ;
#14830=VERTEX_POINT ( 'NONE', #29375 ) ;
#14837=ORIENTED_EDGE ( 'NONE', *, *, #24856, .T. ) ;
#14848=ORIENTED_EDGE ( 'NONE', *, *, #31800, .F. ) ;
#14849=DIRECTION ( 'NONE',  ( -1.000000000000000000, -0.000000000000000000, -0.000000000000000000 ) ) ;
#14851=EDGE_CURVE ( 'NONE', #27145, #34791, #36039, .T. ) ;
#14852=ORIENTED_EDGE ( 'NONE', *, *, #26962, .T. ) ;
#14863=CARTESIAN_POINT ( 'NONE',  ( 17.99999999999999645, 0.000000000000000000, 0.000000000000000000 ) ) ;
#14872=CARTESIAN_POINT ( 'NONE',  ( 17.99999999999999645, -12.42760411676013810, -33.78690065568439138 ) ) ;
#14887=DIRECTION ( 'NONE',  ( -1.000000000000000000, 0.000000000000000000, -0.000000000000000000 ) ) ;
#14896=DIRECTION ( 'NONE',  ( -1.000000000000000000, -0.000000000000000000, -0.000000000000000000 ) ) ;
#14898=CARTESIAN_POINT ( 'NONE',  ( 0.000000000000000000, 0.000000000000000000, 0.000000000000000000 ) ) ;
#14916=DIRECTION ( 'NONE',  ( -1.000000000000000000, -0.000000000000000000, -0.000000000000000000 ) ) ;
#14920=DIRECTION ( 'NONE',  ( -1.000000000000000000, -0.000000000000000000, 0.000000000000000000 ) ) ;
#14929=CARTESIAN_POINT ( 'NONE',  ( 17.99999999999999645, 32.49609705003704363, 15.49205204337285657 ) ) ;
#14933=DIRECTION ( 'NONE',  ( 0.000000000000000000, 0.000000000000000000, 1.000000000000000000 ) ) ;
#14948=AXIS2_PLACEMENT_3D ( 'NONE', #32836, #13012, #26315 ) ;
#14959=CARTESIAN_POINT ( 'NONE',  ( 0.000000000000000000, -0.04937522221101428577, -31.94951095880159286 ) ) ;
#14960=CARTESIAN_POINT ( 'NONE',  ( -10.00000000000000000, 0.000000000000000000, 0.000000000000000000 ) ) ;
#14962=FACE_OUTER_BOUND ( 'NONE', #18100, .T. ) ;
#14978=AXIS2_PLACEMENT_3D ( 'NONE', #35738, #29893, #19861 ) ;
#14979=ORIENTED_EDGE ( 'NONE', *, *, #988, .T. ) ;
#14987=VERTEX_POINT ( 'NONE', #1174 ) ;
#14990=AXIS2_PLACEMENT_3D ( 'NONE', #4067, #13080, #23972 ) ;
#14992=CARTESIAN_POINT ( 'NONE',  ( 17.99999999999999645, 12.42760411676038323, 33.78690065568429191 ) ) ;
#14995=DIRECTION ( 'NONE',  ( 0.000000000000000000, 0.000000000000000000, -1.000000000000000000 ) ) ;
#14996=ORIENTED_EDGE ( 'NONE', *, *, #24496, .T. ) ;
#15018=ORIENTED_EDGE ( 'NONE', *, *, #35442, .F. ) ;
#15020=AXIS2_PLACEMENT_3D ( 'NONE', #34566, #4232, #41540 ) ;
#15024=ORIENTED_EDGE ( 'NONE', *, *, #25625, .F. ) ;
#15027=DIRECTION ( 'NONE',  ( -1.000000000000000000, 0.000000000000000000, 0.000000000000000000 ) ) ;
#15034=CIRCLE ( 'NONE', #21339, 13.59999999999999964 ) ;
#15040=ORIENTED_EDGE ( 'NONE', *, *, #37930, .F. ) ;
#15043=CIRCLE ( 'NONE', #36599, 13.59999999999999964 ) ;
#15044=VERTEX_POINT ( 'NONE', #18044 ) ;
#15063=FACE_OUTER_BOUND ( 'NONE', #21524, .T. ) ;
#15069=DIRECTION ( 'NONE',  ( -1.000000000000000000, 0.000000000000000000, 0.000000000000000000 ) ) ;
#15071=CARTESIAN_POINT ( 'NONE',  ( 0.000000000000000000, 34.45183346761135113, 10.44371441202667761 ) ) ;
#15075=DIRECTION ( 'NONE',  ( 0.000000000000000000, 0.000000000000000000, 1.000000000000000000 ) ) ;
#15076=EDGE_CURVE ( 'NONE', #15150, #31530, #40932, .T. ) ;
#15088=ORIENTED_EDGE ( 'NONE', *, *, #41659, .T. ) ;
#15089=DIRECTION ( 'NONE',  ( -1.000000000000000000, -0.000000000000000000, -0.000000000000000000 ) ) ;
#15090=ORIENTED_EDGE ( 'NONE', *, *, #13067, .F. ) ;
#15102=FACE_OUTER_BOUND ( 'NONE', #5655, .T. ) ;
#15104=VECTOR ( 'NONE', #28312, 1000.000000000000000 ) ;
#15127=FACE_OUTER_BOUND ( 'NONE', #34253, .T. ) ;
#15132=CIRCLE ( 'NONE', #21444, 13.60000000000000320 ) ;
#15140=VECTOR ( 'NONE', #8460, 1000.000000000000000 ) ;
#15149=DIRECTION ( 'NONE',  ( 0.000000000000000000, 0.000000000000000000, 1.000000000000000000 ) ) ;
#15150=VERTEX_POINT ( 'NONE', #33919 ) ;
#15156=DIRECTION ( 'NONE',  ( 0.000000000000000000, 0.000000000000000000, 1.000000000000000000 ) ) ;
#15158=DIRECTION ( 'NONE',  ( -1.000000000000000000, 0.000000000000000000, 0.000000000000000000 ) ) ;
#15168=ORIENTED_EDGE ( 'NONE', *, *, #39856, .T. ) ;
#15169=CIRCLE ( 'NONE', #39488, 36.00000000000000000 ) ;
#15173=AXIS2_PLACEMENT_3D ( 'NONE', #14200, #17708, #9079 ) ;
#15182=VERTEX_POINT ( 'NONE', #28488 ) ;
#15187=AXIS2_PLACEMENT_3D ( 'NONE', #38017, #8144, #4865 ) ;
#15206=AXIS2_PLACEMENT_3D ( 'NONE', #29973, #9674, #36263 ) ;
#15218=CARTESIAN_POINT ( 'NONE',  ( 0.000000000000000000, 30.74337109795208178, 8.695908345466650147 ) ) ;
#15222=FILL_AREA_STYLE_COLOUR ( '', #11397 ) ;
#15239=CIRCLE ( 'NONE', #12445, 13.59999999999999964 ) ;
#15245=DIRECTION ( 'NONE',  ( -1.000000000000000000, 0.000000000000000000, 0.000000000000000000 ) ) ;
#15246=FACE_OUTER_BOUND ( 'NONE', #6969, .T. ) ;
#15251=EDGE_CURVE ( 'NONE', #1962, #16404, #35373, .T. ) ;
#15258=DIRECTION ( 'NONE',  ( -1.000000000000000000, -0.000000000000000000, -0.000000000000000000 ) ) ;
#15318=EDGE_LOOP ( 'NONE', ( #29441, #39256, #28160, #17224 ) ) ;
#15322=CARTESIAN_POINT ( 'NONE',  ( 17.99999999999999645, 28.62203781743003717, 14.19692359621465094 ) ) ;
#15324=AXIS2_PLACEMENT_3D ( 'NONE', #895, #38214, #8330 ) ;
#15331=DIRECTION ( 'NONE',  ( -1.000000000000000000, -0.000000000000000000, 0.000000000000000000 ) ) ;
#15364=DIRECTION ( 'NONE',  ( -1.000000000000000000, -0.000000000000000000, -0.000000000000000000 ) ) ;
#15365=CARTESIAN_POINT ( 'NONE',  ( 17.99999999999999645, 0.000000000000000000, 0.000000000000000000 ) ) ;
#15374=AXIS2_PLACEMENT_3D ( 'NONE', #25265, #27880, #21989 ) ;
#15387=CARTESIAN_POINT ( 'NONE',  ( 0.000000000000000000, -16.77727049691090500, -27.19001440037564166 ) ) ;
#15393=DIRECTION ( 'NONE',  ( 0.000000000000000000, -0.1837495178165775567, 0.9829730996839004531 ) ) ;
#15398=DIRECTION ( 'NONE',  ( -1.000000000000000000, -0.000000000000000000, 0.000000000000000000 ) ) ;
#15402=AXIS2_PLACEMENT_3D ( 'NONE', #25509, #15896, #42888 ) ;
#15408=ORIENTED_EDGE ( 'NONE', *, *, #41049, .F. ) ;
#15447=CIRCLE ( 'NONE', #18265, 13.59999999999999964 ) ;
#15451=DIRECTION ( 'NONE',  ( -1.000000000000000000, 0.000000000000000000, -0.000000000000000000 ) ) ;
#15453=CARTESIAN_POINT ( 'NONE',  ( 17.99999999999999645, 31.81777574834302058, 2.898764365605871696 ) ) ;
#15464=CIRCLE ( 'NONE', #38427, 13.59999999999999964 ) ;
#15465=FACE_OUTER_BOUND ( 'NONE', #31433, .T. ) ;
#15469=DIRECTION ( 'NONE',  ( -1.000000000000000000, -0.000000000000000000, -0.000000000000000000 ) ) ;
#15471=LINE ( 'NONE', #5405, #17223 ) ;
#15482=ADVANCED_FACE ( 'NONE', ( #3304 ), #12954, .T. ) ;
#15483=EDGE_CURVE ( 'NONE', #20704, #27145, #9232, .T. ) ;
#15494=EDGE_CURVE ( 'NONE', #37143, #17989, #12962, .T. ) ;
#15501=LINE ( 'NONE', #15924, #34208 ) ;
#15505=AXIS2_PLACEMENT_3D ( 'NONE', #27522, #10711, #10498 ) ;
#15522=CARTESIAN_POINT ( 'NONE',  ( 0.000000000000000000, 34.78944633786279184, 9.257128253673750251 ) ) ;
#15525=AXIS2_PLACEMENT_3D ( 'NONE', #9987, #32481, #19010 ) ;
#15529=DIRECTION ( 'NONE',  ( 0.000000000000000000, 0.000000000000000000, -1.000000000000000000 ) ) ;
#15532=VERTEX_POINT ( 'NONE', #6180 ) ;
#15533=DIRECTION ( 'NONE',  ( 0.000000000000000000, -0.7980172272802448230, 0.6026346363792494110 ) ) ;
#15535=ADVANCED_FACE ( 'NONE', ( #29760 ), #26479, .T. ) ;
#15544=ORIENTED_EDGE ( 'NONE', *, *, #26558, .T. ) ;
#15555=ADVANCED_FACE ( 'NONE', ( #13613 ), #39748, .T. ) ;
#15560=CARTESIAN_POINT ( 'NONE',  ( 17.99999999999999645, 31.80866420683990725, 2.997093558041416195 ) ) ;
#15596=CIRCLE ( 'NONE', #39244, 36.00000000000000000 ) ;
#15608=ADVANCED_FACE ( 'NONE', ( #26271 ), #42597, .T. ) ;
#15616=DIRECTION ( 'NONE',  ( -1.000000000000000000, 0.000000000000000000, 0.000000000000000000 ) ) ;
#15646=ORIENTED_EDGE ( 'NONE', *, *, #28509, .F. ) ;
#15647=CARTESIAN_POINT ( 'NONE',  ( -10.00000000000000000, 0.000000000000000000, 0.000000000000000000 ) ) ;
#15648=ORIENTED_EDGE ( 'NONE', *, *, #3207, .T. ) ;
#15656=ADVANCED_FACE ( 'NONE', ( #30620 ), #27342, .T. ) ;
#15678=DIRECTION ( 'NONE',  ( 1.000000000000000000, -0.000000000000000000, -0.000000000000000000 ) ) ;
#15684=CIRCLE ( 'NONE', #12869, 13.59999999999999964 ) ;
#15689=AXIS2_PLACEMENT_3D ( 'NONE', #23009, #21192, #30555 ) ;
#15690=EDGE_CURVE ( 'NONE', #20538, #17206, #27707, .T. ) ;
#15699=DIRECTION ( 'NONE',  ( -1.000000000000000000, 0.000000000000000000, 0.000000000000000000 ) ) ;
#15716=AXIS2_PLACEMENT_3D ( 'NONE', #11421, #24754, #38007 ) ;
#15719=FACE_OUTER_BOUND ( 'NONE', #37502, .T. ) ;
#15742=AXIS2_PLACEMENT_3D ( 'NONE', #38612, #22098, #15533 ) ;
#15757=DIRECTION ( 'NONE',  ( 1.000000000000000000, 0.000000000000000000, 0.000000000000000000 ) ) ;
#15764=ORIENTED_EDGE ( 'NONE', *, *, #9014, .F. ) ;
#15778=EDGE_CURVE ( 'NONE', #12201, #4714, #40896, .T. ) ;
#15780=DIRECTION ( 'NONE',  ( 0.000000000000000000, 0.000000000000000000, 1.000000000000000000 ) ) ;
#15784=DIRECTION ( 'NONE',  ( 0.000000000000000000, -0.6736956436465638687, 0.7390089172206529833 ) ) ;
#15790=CARTESIAN_POINT ( 'NONE',  ( 17.99999999999999645, 0.000000000000000000, 0.000000000000000000 ) ) ;
#15808=CYLINDRICAL_SURFACE ( 'NONE', #12473, 13.59999999999999964 ) ;
#15817=EDGE_CURVE ( 'NONE', #39668, #35149, #42979, .T. ) ;
#15825=CARTESIAN_POINT ( 'NONE',  ( 0.000000000000000000, 28.62203781743003717, -14.19692359621465094 ) ) ;
#15838=AXIS2_PLACEMENT_3D ( 'NONE', #8579, #31946, #28887 ) ;
#15839=VERTEX_POINT ( 'NONE', #22330 ) ;
#15853=CIRCLE ( 'NONE', #41615, 36.00000000000000000 ) ;
#15855=LINE ( 'NONE', #42427, #22761 ) ;
#15863=VERTEX_POINT ( 'NONE', #5496 ) ;
#15887=DIRECTION ( 'NONE',  ( 0.000000000000000000, 0.000000000000000000, -1.000000000000000000 ) ) ;
#15896=DIRECTION ( 'NONE',  ( -1.000000000000000000, -0.000000000000000000, -0.000000000000000000 ) ) ;
#15909=AXIS2_PLACEMENT_3D ( 'NONE', #30444, #11029, #23911 ) ;
#15910=EDGE_CURVE ( 'NONE', #41773, #29952, #29100, .T. ) ;
#15913=CIRCLE ( 'NONE', #40249, 36.00000000000000000 ) ;
#15922=VERTEX_POINT ( 'NONE', #8121 ) ;
#15924=CARTESIAN_POINT ( 'NONE',  ( 9.000000000000000000, 31.94619804602787738, -16.59639811537322984 ) ) ;
#15935=CIRCLE ( 'NONE', #29853, 13.59999999999999964 ) ;
#15941=ORIENTED_EDGE ( 'NONE', *, *, #8317, .T. ) ;
#15945=LINE ( 'NONE', #2784, #27507 ) ;
#15946=DIRECTION ( 'NONE',  ( 0.000000000000000000, 0.000000000000000000, 1.000000000000000000 ) ) ;
#15983=ORIENTED_EDGE ( 'NONE', *, *, #3317, .F. ) ;
#15990=DIRECTION ( 'NONE',  ( 0.000000000000000000, -0.9957341762950334685, -0.09226835946331306271 ) ) ;
#16006=ORIENTED_EDGE ( 'NONE', *, *, #38657, .F. ) ;
#16008=EDGE_CURVE ( 'NONE', #30643, #3236, #22834, .T. ) ;
#16011=EDGE_CURVE ( 'NONE', #25635, #40989, #28402, .T. ) ;
#16015=DIRECTION ( 'NONE',  ( -1.000000000000000000, -0.000000000000000000, -0.000000000000000000 ) ) ;
#16019=LINE ( 'NONE', #39303, #28918 ) ;
#16026=DIRECTION ( 'NONE',  ( -1.000000000000000000, -0.000000000000000000, -0.000000000000000000 ) ) ;
#16029=DIRECTION ( 'NONE',  ( 0.000000000000000000, -0.3612416661871404866, -0.9324722294043605864 ) ) ;
#16048=CARTESIAN_POINT ( 'NONE',  ( 0.000000000000000000, 31.81777574834305966, 10.70123563439457293 ) ) ;
#16062=ORIENTED_EDGE ( 'NONE', *, *, #885, .T. ) ;
#16072=VERTEX_POINT ( 'NONE', #5904 ) ;
#16080=CYLINDRICAL_SURFACE ( 'NONE', #1740, 36.00000000000000000 ) ;
#16102=ORIENTED_EDGE ( 'NONE', *, *, #16651, .T. ) ;
#16103=CARTESIAN_POINT ( 'NONE',  ( 17.99999999999999645, -34.45183346761142928, 10.44371441202643247 ) ) ;
#16104=VERTEX_POINT ( 'NONE', #24034 ) ;
#16108=AXIS2_PLACEMENT_3D ( 'NONE', #22182, #2884, #29132 ) ;
#16110=CARTESIAN_POINT ( 'NONE',  ( 17.99999999999999645, -23.79363200506935527, -27.01597816121672224 ) ) ;
#16112=CIRCLE ( 'NONE', #34900, 31.49900000000000588 ) ;
#16115=AXIS2_PLACEMENT_3D ( 'NONE', #16816, #40524, #36611 ) ;
#16129=VECTOR ( 'NONE', #5128, 1000.000000000000000 ) ;
#16133=CIRCLE ( 'NONE', #11968, 31.49899999999999523 ) ;
#16150=ORIENTED_EDGE ( 'NONE', *, *, #10319, .T. ) ;
#16168=CIRCLE ( 'NONE', #12676, 13.59999999999999787 ) ;
#16173=DIRECTION ( 'NONE',  ( -1.000000000000000000, 0.000000000000000000, 0.000000000000000000 ) ) ;
#16184=DIRECTION ( 'NONE',  ( -1.000000000000000000, -0.000000000000000000, -0.000000000000000000 ) ) ;
#16187=ORIENTED_EDGE ( 'NONE', *, *, #15494, .F. ) ;
#16195=EDGE_CURVE ( 'NONE', #26550, #8083, #37451, .T. ) ;
#16196=ADVANCED_FACE ( 'NONE', ( #34250 ), #41002, .T. ) ;
#16225=ADVANCED_FACE ( 'NONE', ( #23614 ), #6981, .T. ) ;
#16234=FACE_OUTER_BOUND ( 'NONE', #4762, .T. ) ;
#16258=CARTESIAN_POINT ( 'NONE',  ( 0.000000000000000000, 3.803237743092368284, -31.26855263151010789 ) ) ;
#16300=ORIENTED_EDGE ( 'NONE', *, *, #43051, .T. ) ;
#16309=CARTESIAN_POINT ( 'NONE',  ( 0.000000000000000000, 0.000000000000000000, 0.000000000000000000 ) ) ;
#16311=ORIENTED_EDGE ( 'NONE', *, *, #15483, .T. ) ;
#16323=ORIENTED_EDGE ( 'NONE', *, *, #15817, .T. ) ;
#16337=ORIENTED_EDGE ( 'NONE', *, *, #36514, .T. ) ;
#16347=EDGE_CURVE ( 'NONE', #14447, #12013, #7494, .T. ) ;
#16351=AXIS2_PLACEMENT_3D ( 'NONE', #1327, #4079, #20944 ) ;
#16352=ORIENTED_EDGE ( 'NONE', *, *, #7898, .F. ) ;
#16374=VECTOR ( 'NONE', #13719, 1000.000000000000000 ) ;
#16384=CIRCLE ( 'NONE', #8024, 13.59999999999999964 ) ;
#16395=AXIS2_PLACEMENT_3D ( 'NONE', #19922, #17076, #6998 ) ;
#16396=CARTESIAN_POINT ( 'NONE',  ( 0.000000000000000000, 0.000000000000000000, 0.000000000000000000 ) ) ;
#16404=VERTEX_POINT ( 'NONE', #23956 ) ;
#16422=ORIENTED_EDGE ( 'NONE', *, *, #35589, .T. ) ;
#16437=EDGE_CURVE ( 'NONE', #17206, #4224, #18054, .T. ) ;
#16440=EDGE_CURVE ( 'NONE', #19537, #24676, #40696, .T. ) ;
#16445=DIRECTION ( 'NONE',  ( 0.000000000000000000, 0.000000000000000000, 1.000000000000000000 ) ) ;
#16450=DIRECTION ( 'NONE',  ( -1.000000000000000000, -0.000000000000000000, 0.000000000000000000 ) ) ;
#16456=CARTESIAN_POINT ( 'NONE',  ( 17.99999999999999645, 13.22719389142019608, -28.58720592780581882 ) ) ;
#16458=VERTEX_POINT ( 'NONE', #10847 ) ;
#16460=CIRCLE ( 'NONE', #3850, 36.00000000000000000 ) ;
#16500=AXIS2_PLACEMENT_3D ( 'NONE', #12290, #19703, #15780 ) ;
#16506=EDGE_CURVE ( 'NONE', #19749, #16458, #15239, .T. ) ;
#16507=CARTESIAN_POINT ( 'NONE',  ( 0.000000000000000000, 5.822172717930266472, 31.41458249383143198 ) ) ;
#16521=CYLINDRICAL_SURFACE ( 'NONE', #27098, 13.60000000000000142 ) ;
#16530=ORIENTED_EDGE ( 'NONE', *, *, #39694, .T. ) ;
#16556=AXIS2_PLACEMENT_3D ( 'NONE', #30226, #13445, #27176 ) ;
#16570=AXIS2_PLACEMENT_3D ( 'NONE', #36758, #23712, #40240 ) ;
#16571=CARTESIAN_POINT ( 'NONE',  ( 0.000000000000000000, -34.45183346761128718, -10.44371441202691564 ) ) ;
#16572=CARTESIAN_POINT ( 'NONE',  ( 17.99999999999999645, 0.000000000000000000, 0.000000000000000000 ) ) ;
#16576=FACE_OUTER_BOUND ( 'NONE', #3420, .T. ) ;
#16606=CARTESIAN_POINT ( 'NONE',  ( 17.99999999999999645, 31.80866420683990725, 16.59709355804141495 ) ) ;
#16608=ORIENTED_EDGE ( 'NONE', *, *, #22930, .F. ) ;
#16610=AXIS2_PLACEMENT_3D ( 'NONE', #13607, #34083, #40175 ) ;
#16625=CARTESIAN_POINT ( 'NONE',  ( 9.000000000000000000, 29.09613215194512748, -21.19941258140292106 ) ) ;
#16626=VECTOR ( 'NONE', #15699, 1000.000000000000000 ) ;
#16643=VERTEX_POINT ( 'NONE', #11498 ) ;
#16651=EDGE_CURVE ( 'NONE', #37143, #31287, #40271, .T. ) ;
#16655=EDGE_CURVE ( 'NONE', #39631, #30103, #33315, .T. ) ;
#16664=DIRECTION ( 'NONE',  ( -1.000000000000000000, 0.000000000000000000, 0.000000000000000000 ) ) ;
#16665=CARTESIAN_POINT ( 'NONE',  ( 17.99999999999999645, 11.58753559615527529, -29.77419532459249751 ) ) ;
#16680=CARTESIAN_POINT ( 'NONE',  ( 17.99999999999999645, -30.71634675606060227, 8.790889055186445589 ) ) ;
#16681=VERTEX_POINT ( 'NONE', #23480 ) ;
#16684=ORIENTED_EDGE ( 'NONE', *, *, #35697, .T. ) ;
#16688=CARTESIAN_POINT ( 'NONE',  ( 17.99999999999999645, 0.000000000000000000, 0.000000000000000000 ) ) ;
#16690=DIRECTION ( 'NONE',  ( -1.000000000000000000, 0.000000000000000000, -0.000000000000000000 ) ) ;
#16705=EDGE_CURVE ( 'NONE', #1839, #25006, #41660, .T. ) ;
#16737=CARTESIAN_POINT ( 'NONE',  ( 0.000000000000000000, 0.000000000000000000, 0.000000000000000000 ) ) ;
#16738=CARTESIAN_POINT ( 'NONE',  ( -10.00000000000000000, 0.000000000000000000, 0.000000000000000000 ) ) ;
#16743=AXIS2_PLACEMENT_3D ( 'NONE', #31139, #11502, #21138 ) ;
#16760=EDGE_CURVE ( 'NONE', #13115, #41773, #15855, .T. ) ;
#16763=DIRECTION ( 'NONE',  ( 0.000000000000000000, 0.9618256431728180456, 0.2736629900720866648 ) ) ;
#16769=ORIENTED_EDGE ( 'NONE', *, *, #11051, .T. ) ;
#16774=AXIS2_PLACEMENT_3D ( 'NONE', #17176, #23502, #13672 ) ;
#16775=ORIENTED_EDGE ( 'NONE', *, *, #24111, .F. ) ;
#16780=CIRCLE ( 'NONE', #24447, 13.59999999999999964 ) ;
#16786=CARTESIAN_POINT ( 'NONE',  ( 0.000000000000000000, -35.89808275599443022, -2.706964063997605141 ) ) ;
#16794=CARTESIAN_POINT ( 'NONE',  ( -10.00000000000000000, 0.000000000000000000, 0.000000000000000000 ) ) ;
#16795=ORIENTED_EDGE ( 'NONE', *, *, #8495, .F. ) ;
#16797=DIRECTION ( 'NONE',  ( 0.000000000000000000, 0.9957341762950348008, -0.09226835946329869920 ) ) ;
#16798=DIRECTION ( 'NONE',  ( -1.000000000000000000, -0.000000000000000000, 0.000000000000000000 ) ) ;
#16800=CIRCLE ( 'NONE', #18905, 31.49900000000000588 ) ;
#16804=ORIENTED_EDGE ( 'NONE', *, *, #19770, .F. ) ;
#16806=DIRECTION ( 'NONE',  ( 0.000000000000000000, 0.5264321628773568351, -0.8502171357296134380 ) ) ;
#16808=DIRECTION ( 'NONE',  ( 0.000000000000000000, 0.000000000000000000, 1.000000000000000000 ) ) ;
#16811=EDGE_CURVE ( 'NONE', #12162, #31530, #6000, .T. ) ;
#16814=CARTESIAN_POINT ( 'NONE',  ( 17.99999999999999645, 11.49545354908979888, -29.80986809967247453 ) ) ;
#16815=ORIENTED_EDGE ( 'NONE', *, *, #13528, .T. ) ;
#16816=CARTESIAN_POINT ( 'NONE',  ( 0.000000000000000000, 11.58753559615527529, -29.77419532459249751 ) ) ;
#16823=CARTESIAN_POINT ( 'NONE',  ( 17.99999999999999645, 28.35267316522815406, -22.18391138608678048 ) ) ;
#16834=CIRCLE ( 'NONE', #4966, 13.59999999999999787 ) ;
#16844=EDGE_LOOP ( 'NONE', ( #38319, #17839, #4685, #28738 ) ) ;
#16846=DIRECTION ( 'NONE',  ( 0.000000000000000000, 0.3612416661871538093, -0.9324722294043554793 ) ) ;
#16860=CARTESIAN_POINT ( 'NONE',  ( 17.99999999999999645, 0.000000000000000000, 0.000000000000000000 ) ) ;
#16871=AXIS2_PLACEMENT_3D ( 'NONE', #34138, #21542, #30876 ) ;
#16880=FACE_OUTER_BOUND ( 'NONE', #42399, .T. ) ;
#16882=DIRECTION ( 'NONE',  ( -1.000000000000000000, 0.000000000000000000, -0.000000000000000000 ) ) ;
#16895=CYLINDRICAL_SURFACE ( 'NONE', #16610, 36.00000000000000000 ) ;
#16898=LINE ( 'NONE', #39956, #24260 ) ;
#16901=ORIENTED_EDGE ( 'NONE', *, *, #10236, .T. ) ;
#16914=CYLINDRICAL_SURFACE ( 'NONE', #29393, 36.00000000000000000 ) ;
#16930=EDGE_CURVE ( 'NONE', #36754, #34450, #2486, .T. ) ;
#16931=CARTESIAN_POINT ( 'NONE',  ( 0.000000000000000000, -29.03409033315590904, 12.21509719675380623 ) ) ;
#16947=ORIENTED_EDGE ( 'NONE', *, *, #31292, .T. ) ;
#16948=DIRECTION ( 'NONE',  ( 1.000000000000000000, -0.000000000000000000, -0.000000000000000000 ) ) ;
#16961=LINE ( 'NONE', #28227, #19889 ) ;
#16962=PLANE ( 'NONE',  #20350 ) ;
#16974=EDGE_CURVE ( 'NONE', #10211, #20449, #19272, .T. ) ;
#16989=ORIENTED_EDGE ( 'NONE', *, *, #37793, .T. ) ;
#16992=EDGE_CURVE ( 'NONE', #41473, #24259, #16460, .T. ) ;
#16997=LINE ( 'NONE', #30921, #24928 ) ;
#16998=ORIENTED_EDGE ( 'NONE', *, *, #29129, .F. ) ;
#17005=DIRECTION ( 'NONE',  ( -1.000000000000000000, 0.000000000000000000, -0.000000000000000000 ) ) ;
#17008=VECTOR ( 'NONE', #25880, 1000.000000000000000 ) ;
#17016=CARTESIAN_POINT ( 'NONE',  ( 0.000000000000000000, 0.000000000000000000, 0.000000000000000000 ) ) ;
#17021=DIRECTION ( 'NONE',  ( -1.000000000000000000, -0.000000000000000000, 0.000000000000000000 ) ) ;
#17030=CARTESIAN_POINT ( 'NONE',  ( 9.000000000000000000, -7.220349212960190499, -35.26849241522671718 ) ) ;
#17035=VERTEX_POINT ( 'NONE', #14573 ) ;
#17045=CARTESIAN_POINT ( 'NONE',  ( 17.99999999999999645, 5.919241748380035695, -31.39643714728450163 ) ) ;
#17055=CARTESIAN_POINT ( 'NONE',  ( 17.99999999999999645, -3.803237743092135581, 31.26855263151013276 ) ) ;
#17073=AXIS2_PLACEMENT_3D ( 'NONE', #3627, #20073, #23328 ) ;
#17076=DIRECTION ( 'NONE',  ( -1.000000000000000000, -0.000000000000000000, -0.000000000000000000 ) ) ;
#17078=DIRECTION ( 'NONE',  ( 0.000000000000000000, -0.3612416661871601375, 0.9324722294043530368 ) ) ;
#17082=AXIS2_PLACEMENT_3D ( 'NONE', #20632, #30647, #23687 ) ;
#17101=EDGE_CURVE ( 'NONE', #8291, #23736, #18505, .T. ) ;
#17123=CIRCLE ( 'NONE', #23369, 31.49899999999999878 ) ;
#17134=AXIS2_PLACEMENT_3D ( 'NONE', #29801, #13646, #39992 ) ;
#17135=CARTESIAN_POINT ( 'NONE',  ( 0.000000000000000000, -25.52601536738605859, 19.21447964122688390 ) ) ;
#17155=VECTOR ( 'NONE', #31456, 1000.000000000000000 ) ;
#17162=CARTESIAN_POINT ( 'NONE',  ( 17.99999999999999645, -34.78944633786272789, -9.257128253673986507 ) ) ;
#17166=ORIENTED_EDGE ( 'NONE', *, *, #41659, .F. ) ;
#17171=LINE ( 'NONE', #7742, #36881 ) ;
#17176=CARTESIAN_POINT ( 'NONE',  ( 0.000000000000000000, 21.48775762007859669, 23.64423737150145399 ) ) ;
#17187=AXIS2_PLACEMENT_3D ( 'NONE', #5660, #21657, #1737 ) ;
#17206=VERTEX_POINT ( 'NONE', #42632 ) ;
#17213=ORIENTED_EDGE ( 'NONE', *, *, #42821, .F. ) ;
#17218=VECTOR ( 'NONE', #11953, 1000.000000000000000 ) ;
#17220=EDGE_LOOP ( 'NONE', ( #41410, #20030, #16769, #18602 ) ) ;
#17223=VECTOR ( 'NONE', #19176, 1000.000000000000000 ) ;
#17224=ORIENTED_EDGE ( 'NONE', *, *, #13170, .T. ) ;
#17243=CARTESIAN_POINT ( 'NONE',  ( 17.99999999999999645, -5.919241748379815427, 31.39643714728454427 ) ) ;
#17245=DIRECTION ( 'NONE',  ( 0.000000000000000000, 0.3612416661871471479, 0.9324722294043580328 ) ) ;
#17256=ORIENTED_EDGE ( 'NONE', *, *, #15251, .F. ) ;
#17281=CARTESIAN_POINT ( 'NONE',  ( 17.99999999999999645, 21.48775762007859669, 23.64423737150145399 ) ) ;
#17286=FACE_OUTER_BOUND ( 'NONE', #22976, .T. ) ;
#17293=DIRECTION ( 'NONE',  ( 0.000000000000000000, 0.000000000000000000, 1.000000000000000000 ) ) ;
#17299=ORIENTED_EDGE ( 'NONE', *, *, #4922, .T. ) ;
#17305=VECTOR ( 'NONE', #35065, 1000.000000000000000 ) ;
#17309=CARTESIAN_POINT ( 'NONE',  ( -10.00000000000000000, 0.000000000000000000, 0.000000000000000000 ) ) ;
#17313=ORIENTED_EDGE ( 'NONE', *, *, #40674, .T. ) ;
#17315=CARTESIAN_POINT ( 'NONE',  ( 0.000000000000000000, -25.46650492921884279, -19.29328419707811193 ) ) ;
#17332=DIRECTION ( 'NONE',  ( 0.000000000000000000, -0.7980172272802321665, -0.6026346363792661753 ) ) ;
#17337=CARTESIAN_POINT ( 'NONE',  ( 17.99999999999999645, 13.57797752207923381, 33.34124362422479493 ) ) ;
#17341=DIRECTION ( 'NONE',  ( -1.000000000000000000, 0.000000000000000000, 0.000000000000000000 ) ) ;
#17343=ORIENTED_EDGE ( 'NONE', *, *, #39114, .T. ) ;
#17344=CARTESIAN_POINT ( 'NONE',  ( 0.000000000000000000, -30.71634675606060227, 8.790889055186445589 ) ) ;
#17356=EDGE_LOOP ( 'NONE', ( #22173, #29867, #12788, #41116 ) ) ;
#17364=DIRECTION ( 'NONE',  ( -1.000000000000000000, 0.000000000000000000, 0.000000000000000000 ) ) ;
#17371=CARTESIAN_POINT ( 'NONE',  ( 0.000000000000000000, -22.66088087769164972, -21.87856208362581256 ) ) ;
#17373=ADVANCED_FACE ( 'NONE', ( #26312 ), #33039, .T. ) ;
#17377=AXIS2_PLACEMENT_3D ( 'NONE', #36645, #30131, #13779 ) ;
#17380=DIRECTION ( 'NONE',  ( 0.000000000000000000, 0.9618256431728180456, 0.2736629900720866093 ) ) ;
#17387=DIRECTION ( 'NONE',  ( 1.000000000000000000, 0.000000000000000000, 0.000000000000000000 ) ) ;
#17390=ORIENTED_EDGE ( 'NONE', *, *, #15910, .F. ) ;
#17393=DIRECTION ( 'NONE',  ( 0.000000000000000000, -0.3612416661871601375, 0.9324722294043530368 ) ) ;
#17395=DIRECTION ( 'NONE',  ( -1.000000000000000000, 0.000000000000000000, 0.000000000000000000 ) ) ;
#17432=CARTESIAN_POINT ( 'NONE',  ( 0.000000000000000000, 0.000000000000000000, 0.000000000000000000 ) ) ;
#17448=DIRECTION ( 'NONE',  ( -1.000000000000000000, -0.000000000000000000, 0.000000000000000000 ) ) ;
#17450=VERTEX_POINT ( 'NONE', #13648 ) ;
#17458=DIRECTION ( 'NONE',  ( -1.000000000000000000, 0.000000000000000000, 0.000000000000000000 ) ) ;
#17461=LINE ( 'NONE', #10892, #1128 ) ;
#17474=DIRECTION ( 'NONE',  ( 0.000000000000000000, 0.8951632913550635617, -0.4457383557765359772 ) ) ;
#17484=FACE_OUTER_BOUND ( 'NONE', #26399, .T. ) ;
#17490=AXIS2_PLACEMENT_3D ( 'NONE', #9938, #12806, #6030 ) ;
#17493=CIRCLE ( 'NONE', #41834, 31.49899999999999878 ) ;
#17499=VECTOR ( 'NONE', #27070, 1000.000000000000000 ) ;
#17506=CARTESIAN_POINT ( 'NONE',  ( 0.000000000000000000, -11.49545354908914518, -29.80986809967271967 ) ) ;
#17510=ORIENTED_EDGE ( 'NONE', *, *, #22301, .F. ) ;
#17520=DIRECTION ( 'NONE',  ( 0.000000000000000000, 0.000000000000000000, 1.000000000000000000 ) ) ;
#17526=CIRCLE ( 'NONE', #41863, 36.00000000000000000 ) ;
#17529=ORIENTED_EDGE ( 'NONE', *, *, #11365, .F. ) ;
#17544=DIRECTION ( 'NONE',  ( -1.000000000000000000, 0.000000000000000000, -0.000000000000000000 ) ) ;
#17545=EDGE_CURVE ( 'NONE', #3430, #20704, #36003, .T. ) ;
#17557=ORIENTED_EDGE ( 'NONE', *, *, #10204, .T. ) ;
#17569=VECTOR ( 'NONE', #10342, 1000.000000000000000 ) ;
#17573=DIRECTION ( 'NONE',  ( 0.000000000000000000, 0.000000000000000000, 1.000000000000000000 ) ) ;
#17584=AXIS2_PLACEMENT_3D ( 'NONE', #28860, #22987, #36228 ) ;
#17598=AXIS2_PLACEMENT_3D ( 'NONE', #39278, #6147, #22553 ) ;
#17600=EDGE_CURVE ( 'NONE', #7715, #28643, #26257, .T. ) ;
#17616=DIRECTION ( 'NONE',  ( -1.000000000000000000, 0.000000000000000000, 0.000000000000000000 ) ) ;
#17617=ORIENTED_EDGE ( 'NONE', *, *, #6241, .T. ) ;
#17620=VECTOR ( 'NONE', #27966, 1000.000000000000000 ) ;
#17622=VECTOR ( 'NONE', #22106, 1000.000000000000000 ) ;
#17625=VECTOR ( 'NONE', #30341, 1000.000000000000000 ) ;
#17632=CARTESIAN_POINT ( 'NONE',  ( 0.000000000000000000, 31.11570115861502828, -4.898994019976315784 ) ) ;
#17633=CARTESIAN_POINT ( 'NONE',  ( 9.000000000000000000, -35.89808275599447285, 2.706964063997107317 ) ) ;
#17635=CARTESIAN_POINT ( 'NONE',  ( 0.000000000000000000, 31.81777574834302058, 2.898764365605871696 ) ) ;
#17638=DIRECTION ( 'NONE',  ( 0.000000000000000000, 0.1837495178165706178, -0.9829730996839017854 ) ) ;
#17646=DIRECTION ( 'NONE',  ( -1.000000000000000000, -0.000000000000000000, 0.000000000000000000 ) ) ;
#17649=DIRECTION ( 'NONE',  ( 0.000000000000000000, -0.9957341762950355779, 0.09226835946329130234 ) ) ;
#17650=VERTEX_POINT ( 'NONE', #4430 ) ;
#17654=CARTESIAN_POINT ( 'NONE',  ( 17.99999999999999645, -23.87611429743677505, 20.54551452399611478 ) ) ;
#17659=DIRECTION ( 'NONE',  ( 0.000000000000000000, -0.5264321628773627193, 0.8502171357296098853 ) ) ;
#17666=VERTEX_POINT ( 'NONE', #24565 ) ;
#17670=CYLINDRICAL_SURFACE ( 'NONE', #35843, 13.59999999999999964 ) ;
#17674=ADVANCED_FACE ( 'NONE', ( #19296 ), #1816, .T. ) ;
#17708=DIRECTION ( 'NONE',  ( -1.000000000000000000, 0.000000000000000000, -0.000000000000000000 ) ) ;
#17711=DIRECTION ( 'NONE',  ( 0.000000000000000000, 0.6736956436465584286, -0.7390089172206580903 ) ) ;
#17723=ORIENTED_EDGE ( 'NONE', *, *, #29962, .T. ) ;
#17725=DIRECTION ( 'NONE',  ( 0.000000000000000000, -0.1837495178165570453, -0.9829730996839042279 ) ) ;
#17742=EDGE_CURVE ( 'NONE', #3440, #3853, #40170, .T. ) ;
#17752=DIRECTION ( 'NONE',  ( -1.000000000000000000, -0.000000000000000000, -0.000000000000000000 ) ) ;
#17756=VERTEX_POINT ( 'NONE', #2435 ) ;
#17768=ORIENTED_EDGE ( 'NONE', *, *, #40250, .F. ) ;
#17769=ADVANCED_FACE ( 'NONE', ( #36044 ), #28681, .T. ) ;
#17776=DIRECTION ( 'NONE',  ( 0.000000000000000000, 0.000000000000000000, 1.000000000000000000 ) ) ;
#17789=AXIS2_PLACEMENT_3D ( 'NONE', #17896, #37048, #7151 ) ;
#17790=CYLINDRICAL_SURFACE ( 'NONE', #3857, 13.59999999999999964 ) ;
#17795=CYLINDRICAL_SURFACE ( 'NONE', #5816, 36.00000000000000000 ) ;
#17796=VERTEX_POINT ( 'NONE', #41742 ) ;
#17800=VECTOR ( 'NONE', #15451, 1000.000000000000000 ) ;
#17837=ORIENTED_EDGE ( 'NONE', *, *, #29054, .T. ) ;
#17839=ORIENTED_EDGE ( 'NONE', *, *, #35186, .F. ) ;
#17858=DIRECTION ( 'NONE',  ( 0.000000000000000000, -0.9957341762950334685, -0.09226835946331306271 ) ) ;
#17875=ORIENTED_EDGE ( 'NONE', *, *, #40622, .T. ) ;
#17896=CARTESIAN_POINT ( 'NONE',  ( 0.000000000000000000, -28.62203781743013664, 14.19692359621445199 ) ) ;
#17901=LINE ( 'NONE', #41829, #38043 ) ;
#17916=CIRCLE ( 'NONE', #42230, 13.60000000000000320 ) ;
#17926=DIRECTION ( 'NONE',  ( -1.000000000000000000, -0.000000000000000000, -0.000000000000000000 ) ) ;
#17944=ORIENTED_EDGE ( 'NONE', *, *, #1017, .T. ) ;
#17949=ORIENTED_EDGE ( 'NONE', *, *, #13407, .F. ) ;
#17953=ORIENTED_EDGE ( 'NONE', *, *, #26578, .F. ) ;
#17983=DIRECTION ( 'NONE',  ( 0.000000000000000000, 0.1837495178165706455, -0.9829730996839017854 ) ) ;
#17986=AXIS2_PLACEMENT_3D ( 'NONE', #41709, #42340, #21694 ) ;
#17989=VERTEX_POINT ( 'NONE', #23648 ) ;
#18018=CYLINDRICAL_SURFACE ( 'NONE', #30118, 15.00000000000000000 ) ;
#18023=EDGE_CURVE ( 'NONE', #6599, #10153, #32562, .T. ) ;
#18039=CARTESIAN_POINT ( 'NONE',  ( 17.99999999999999645, 34.45183346761135113, 10.44371441202667761 ) ) ;
#18044=CARTESIAN_POINT ( 'NONE',  ( 17.99999999999999645, 0.000000000000000000, 36.00000000000000000 ) ) ;
#18054=CIRCLE ( 'NONE', #10336, 31.49899999999999878 ) ;
#18067=VERTEX_POINT ( 'NONE', #7884 ) ;
#18079=CARTESIAN_POINT ( 'NONE',  ( 0.000000000000000000, -11.49545354908957862, 29.80986809967256335 ) ) ;
#18083=CARTESIAN_POINT ( 'NONE',  ( 8.999999999999998224, -19.47322409167248480, -30.27859877001420941 ) ) ;
#18100=EDGE_LOOP ( 'NONE', ( #42659, #22491, #41255, #39485 ) ) ;
#18104=ORIENTED_EDGE ( 'NONE', *, *, #9119, .T. ) ;
#18107=CIRCLE ( 'NONE', #37539, 13.60000000000000497 ) ;
#18133=DIRECTION ( 'NONE',  ( 0.000000000000000000, 0.3612416661871471479, 0.9324722294043580328 ) ) ;
#18137=AXIS2_PLACEMENT_3D ( 'NONE', #41614, #28763, #5814 ) ;
#18138=VERTEX_POINT ( 'NONE', #1549 ) ;
#18144=DIRECTION ( 'NONE',  ( -1.000000000000000000, 0.000000000000000000, 0.000000000000000000 ) ) ;
#18149=FACE_OUTER_BOUND ( 'NONE', #36713, .T. ) ;
#18157=EDGE_CURVE ( 'NONE', #31298, #20435, #15169, .T. ) ;
#18208=ORIENTED_EDGE ( 'NONE', *, *, #19227, .F. ) ;
#18210=EDGE_LOOP ( 'NONE', ( #6912, #20837, #9292, #10103 ) ) ;
#18229=CYLINDRICAL_SURFACE ( 'NONE', #24573, 36.00000000000000000 ) ;
#18230=FACE_OUTER_BOUND ( 'NONE', #42936, .T. ) ;
#18238=DIRECTION ( 'NONE',  ( -1.000000000000000000, -0.000000000000000000, 0.000000000000000000 ) ) ;
#18250=AXIS2_PLACEMENT_3D ( 'NONE', #11267, #4920, #28516 ) ;
#18259=CIRCLE ( 'NONE', #25895, 31.49899999999999878 ) ;
#18265=AXIS2_PLACEMENT_3D ( 'NONE', #20955, #4305, #27915 ) ;
#18279=CARTESIAN_POINT ( 'NONE',  ( -10.00000000000000000, 0.000000000000000000, 0.000000000000000000 ) ) ;
#18281=CARTESIAN_POINT ( 'NONE',  ( 9.000000000000000000, 6.007673836298521586, -35.49518073029990717 ) ) ;
#18289=ORIENTED_EDGE ( 'NONE', *, *, #39954, .T. ) ;
#18290=CIRCLE ( 'NONE', #16871, 13.60000000000000320 ) ;
#18293=ORIENTED_EDGE ( 'NONE', *, *, #35614, .T. ) ;
#18299=FACE_OUTER_BOUND ( 'NONE', #24657, .T. ) ;
#18304=DIRECTION ( 'NONE',  ( -1.000000000000000000, 0.000000000000000000, 0.000000000000000000 ) ) ;
#18308=ORIENTED_EDGE ( 'NONE', *, *, #13272, .T. ) ;
#18309=CARTESIAN_POINT ( 'NONE',  ( 0.000000000000000000, 9.484061862023926537, 30.03730300138984433 ) ) ;
#18317=DIRECTION ( 'NONE',  ( 0.000000000000000000, 0.000000000000000000, 1.000000000000000000 ) ) ;
#18318=VECTOR ( 'NONE', #21433, 1000.000000000000000 ) ;
#18320=DIRECTION ( 'NONE',  ( 0.000000000000000000, 0.000000000000000000, 1.000000000000000000 ) ) ;
#18333=VERTEX_POINT ( 'NONE', #31890 ) ;
#18336=LINE ( 'NONE', #27699, #2928 ) ;
#18341=CARTESIAN_POINT ( 'NONE',  ( 9.000000000000000000, -34.45183346761128718, -10.44371441202691742 ) ) ;
#18344=EDGE_CURVE ( 'NONE', #10739, #15532, #9613, .T. ) ;
#18396=ORIENTED_EDGE ( 'NONE', *, *, #29202, .T. ) ;
#18397=ADVANCED_FACE ( 'NONE', ( #42734 ), #39896, .T. ) ;
#18407=CARTESIAN_POINT ( 'NONE',  ( 17.99999999999999645, 30.71634675606066267, -8.790889055186230649 ) ) ;
#18412=DIRECTION ( 'NONE',  ( -1.000000000000000000, 0.000000000000000000, -0.000000000000000000 ) ) ;
#18448=CIRCLE ( 'NONE', #3031, 13.59999999999999964 ) ;
#18465=CARTESIAN_POINT ( 'NONE',  ( 0.000000000000000000, 0.000000000000000000, 0.000000000000000000 ) ) ;
#18468=CARTESIAN_POINT ( 'NONE',  ( 17.99999999999999645, 32.49609705003727100, -15.49205204337240005 ) ) ;
#18484=EDGE_LOOP ( 'NONE', ( #40349, #29537, #38426, #37897 ) ) ;
#18492=VERTEX_POINT ( 'NONE', #35988 ) ;
#18502=DIRECTION ( 'NONE',  ( 1.000000000000000000, 0.000000000000000000, -0.000000000000000000 ) ) ;
#18505=LINE ( 'NONE', #1434, #15104 ) ;
#18508=AXIS2_PLACEMENT_3D ( 'NONE', #4576, #11367, #24697 ) ;
#18516=DIRECTION ( 'NONE',  ( 0.000000000000000000, -0.1837495178165570453, -0.9829730996839042279 ) ) ;
#18519=CYLINDRICAL_SURFACE ( 'NONE', #28982, 36.00000000000000000 ) ;
#18520=VECTOR ( 'NONE', #10058, 1000.000000000000000 ) ;
#18523=ORIENTED_EDGE ( 'NONE', *, *, #38552, .F. ) ;
#18543=LINE ( 'NONE', #8023, #4711 ) ;
#18556=DIRECTION ( 'NONE',  ( -1.000000000000000000, -0.000000000000000000, -0.000000000000000000 ) ) ;
#18560=CIRCLE ( 'NONE', #25487, 13.60000000000000320 ) ;
#18562=VERTEX_POINT ( 'NONE', #37281 ) ;
#18602=ORIENTED_EDGE ( 'NONE', *, *, #10200, .T. ) ;
#18608=CARTESIAN_POINT ( 'NONE',  ( 0.000000000000000000, 13.22719389141978930, 28.58720592780601066 ) ) ;
#18631=DIRECTION ( 'NONE',  ( 0.000000000000000000, -0.6736956436465481035, -0.7390089172206674162 ) ) ;
#18633=ORIENTED_EDGE ( 'NONE', *, *, #32241, .F. ) ;
#18639=EDGE_CURVE ( 'NONE', #14830, #19624, #10300, .T. ) ;
#18642=DIRECTION ( 'NONE',  ( 0.000000000000000000, 0.000000000000000000, 1.000000000000000000 ) ) ;
#18662=CIRCLE ( 'NONE', #13048, 15.00000000000000000 ) ;
#18669=CARTESIAN_POINT ( 'NONE',  ( 0.000000000000000000, -30.78424799127063238, -6.672111855473501940 ) ) ;
#18681=AXIS2_PLACEMENT_3D ( 'NONE', #40830, #475, #30827 ) ;
#18683=ORIENTED_EDGE ( 'NONE', *, *, #20845, .F. ) ;
#18689=AXIS2_PLACEMENT_3D ( 'NONE', #9721, #28949, #5792 ) ;
#18691=DIRECTION ( 'NONE',  ( 1.000000000000000000, -0.000000000000000000, 0.000000000000000000 ) ) ;
#18694=VERTEX_POINT ( 'NONE', #38566 ) ;
#18701=ORIENTED_EDGE ( 'NONE', *, *, #39473, .T. ) ;
#18702=ORIENTED_EDGE ( 'NONE', *, *, #27368, .F. ) ;
#18724=( LENGTH_UNIT ( ) NAMED_UNIT ( * ) SI_UNIT ( .MILLI., .METRE. ) );
#18739=EDGE_CURVE ( 'NONE', #12013, #12125, #32047, .T. ) ;
#18740=CIRCLE ( 'NONE', #13188, 13.60000000000000142 ) ;
#18745=AXIS2_PLACEMENT_3D ( 'NONE', #39960, #36060, #23438 ) ;
#18766=CARTESIAN_POINT ( 'NONE',  ( 0.000000000000000000, 0.000000000000000000, 0.000000000000000000 ) ) ;
#18780=EDGE_CURVE ( 'NONE', #10372, #14556, #34719, .T. ) ;
#18782=ORIENTED_EDGE ( 'NONE', *, *, #9119, .F. ) ;
#18792=CARTESIAN_POINT ( 'NONE',  ( 17.99999999999999645, 0.000000000000000000, 0.000000000000000000 ) ) ;
#18800=CYLINDRICAL_SURFACE ( 'NONE', #29341, 36.00000000000000000 ) ;
#18806=DIRECTION ( 'NONE',  ( -1.000000000000000000, -0.000000000000000000, 0.000000000000000000 ) ) ;
#18810=ORIENTED_EDGE ( 'NONE', *, *, #4697, .F. ) ;
#18811=CARTESIAN_POINT ( 'NONE',  ( 17.99999999999999645, 0.000000000000000000, 0.000000000000000000 ) ) ;
#18815=DIRECTION ( 'NONE',  ( 0.000000000000000000, 0.5264321628773568351, -0.8502171357296134380 ) ) ;
#18817=ORIENTED_EDGE ( 'NONE', *, *, #34136, .F. ) ;
#18818=CARTESIAN_POINT ( 'NONE',  ( 0.000000000000000000, -31.81777574834303124, -2.898764365605651427 ) ) ;
#18824=VECTOR ( 'NONE', #27986, 1000.000000000000000 ) ;
#18836=EDGE_CURVE ( 'NONE', #39379, #34690, #15935, .T. ) ;
#18841=DIRECTION ( 'NONE',  ( 0.000000000000000000, -0.6736956436465636466, 0.7390089172206532053 ) ) ;
#18842=VERTEX_POINT ( 'NONE', #16571 ) ;
#18844=ORIENTED_EDGE ( 'NONE', *, *, #39114, .F. ) ;
#18860=CYLINDRICAL_SURFACE ( 'NONE', #10132, 13.59999999999999964 ) ;
#18904=ORIENTED_EDGE ( 'NONE', *, *, #25429, .T. ) ;
#18905=AXIS2_PLACEMENT_3D ( 'NONE', #3391, #13908, #16763 ) ;
#18909=ORIENTED_EDGE ( 'NONE', *, *, #37550, .T. ) ;
#18928=CIRCLE ( 'NONE', #4122, 31.49899999999999878 ) ;
#18965=ORIENTED_EDGE ( 'NONE', *, *, #21503, .F. ) ;
#18973=AXIS2_PLACEMENT_3D ( 'NONE', #633, #30569, #37523 ) ;
#18990=ORIENTED_EDGE ( 'NONE', *, *, #40108, .F. ) ;
#19000=CARTESIAN_POINT ( 'NONE',  ( 0.000000000000000000, -19.47322409167248480, -30.27859877001420941 ) ) ;
#19002=CARTESIAN_POINT ( 'NONE',  ( 17.99999999999999645, 0.000000000000000000, 0.000000000000000000 ) ) ;
#19003=DIRECTION ( 'NONE',  ( 0.000000000000000000, 0.000000000000000000, 1.000000000000000000 ) ) ;
#19007=CARTESIAN_POINT ( 'NONE',  ( 17.99999999999999645, -18.25486108452607681, -25.66996392254292658 ) ) ;
#19009=ORIENTED_EDGE ( 'NONE', *, *, #36140, .F. ) ;
#19010=DIRECTION ( 'NONE',  ( 0.000000000000000000, 0.000000000000000000, 1.000000000000000000 ) ) ;
#19015=CARTESIAN_POINT ( 'NONE',  ( 8.999999999999998224, 28.35267316522815406, -22.18391138608678403 ) ) ;
#19018=CARTESIAN_POINT ( 'NONE',  ( 0.000000000000000000, 0.000000000000000000, 0.000000000000000000 ) ) ;
#19034=EDGE_CURVE ( 'NONE', #11917, #18562, #18740, .T. ) ;
#19066=EDGE_CURVE ( 'NONE', #27860, #32609, #27803, .T. ) ;
#19067=DIRECTION ( 'NONE',  ( 0.000000000000000000, 0.3612416661871538093, -0.9324722294043554793 ) ) ;
#19073=ORIENTED_EDGE ( 'NONE', *, *, #7794, .T. ) ;
#19084=CIRCLE ( 'NONE', #9972, 36.00000000000000000 ) ;
#19085=ORIENTED_EDGE ( 'NONE', *, *, #988, .F. ) ;
#19091=EDGE_CURVE ( 'NONE', #20435, #3075, #8174, .T. ) ;
#19095=CARTESIAN_POINT ( 'NONE',  ( 17.99999999999999645, 0.000000000000000000, 0.000000000000000000 ) ) ;
#19097=DIRECTION ( 'NONE',  ( 0.000000000000000000, 0.000000000000000000, 1.000000000000000000 ) ) ;
#19102=CARTESIAN_POINT ( 'NONE',  ( 17.99999999999999645, 16.77727049691110750, 27.19001440037552086 ) ) ;
#19106=ORIENTED_EDGE ( 'NONE', *, *, #3995, .F. ) ;
#19127=VERTEX_POINT ( 'NONE', #8379 ) ;
#19150=EDGE_CURVE ( 'NONE', #637, #20538, #30591, .T. ) ;
#19157=CIRCLE ( 'NONE', #30247, 36.00000000000000000 ) ;
#19175=ADVANCED_FACE ( 'NONE', ( #16234 ), #15808, .T. ) ;
#19176=DIRECTION ( 'NONE',  ( -1.000000000000000000, 0.000000000000000000, 0.000000000000000000 ) ) ;
#19186=ORIENTED_EDGE ( 'NONE', *, *, #32934, .F. ) ;
#19205=DIRECTION ( 'NONE',  ( -1.000000000000000000, 0.000000000000000000, -0.000000000000000000 ) ) ;
#19209=CYLINDRICAL_SURFACE ( 'NONE', #34025, 36.00000000000000000 ) ;
#19210=EDGE_LOOP ( 'NONE', ( #7620, #21253, #1878, #18909 ) ) ;
#19214=CIRCLE ( 'NONE', #1727, 31.49900000000000233 ) ;
#19227=EDGE_CURVE ( 'NONE', #15182, #21901, #34752, .T. ) ;
#19228=CIRCLE ( 'NONE', #1046, 36.00000000000000000 ) ;
#19238=VECTOR ( 'NONE', #15616, 1000.000000000000000 ) ;
#19249=CARTESIAN_POINT ( 'NONE',  ( 17.99999999999999645, 0.000000000000000000, 0.000000000000000000 ) ) ;
#19251=CIRCLE ( 'NONE', #383, 13.60000000000000142 ) ;
#19254=DIRECTION ( 'NONE',  ( -1.000000000000000000, -0.000000000000000000, -0.000000000000000000 ) ) ;
#19255=FACE_OUTER_BOUND ( 'NONE', #36705, .T. ) ;
#19258=DIRECTION ( 'NONE',  ( 1.000000000000000000, 0.000000000000000000, -0.000000000000000000 ) ) ;
#19266=DIRECTION ( 'NONE',  ( -1.000000000000000000, -0.000000000000000000, -0.000000000000000000 ) ) ;
#19267=CIRCLE ( 'NONE', #24827, 13.60000000000000142 ) ;
#19272=CIRCLE ( 'NONE', #9456, 31.49899999999999878 ) ;
#19277=FACE_OUTER_BOUND ( 'NONE', #22692, .T. ) ;
#19280=CIRCLE ( 'NONE', #41539, 13.60000000000000142 ) ;
#19293=ORIENTED_EDGE ( 'NONE', *, *, #22832, .F. ) ;
#19296=FACE_OUTER_BOUND ( 'NONE', #7986, .T. ) ;
#19306=DIRECTION ( 'NONE',  ( -1.000000000000000000, 0.000000000000000000, -0.000000000000000000 ) ) ;
#19319=AXIS2_PLACEMENT_3D ( 'NONE', #20091, #25963, #16808 ) ;
#19320=ORIENTED_EDGE ( 'NONE', *, *, #7900, .T. ) ;
#19331=ORIENTED_EDGE ( 'NONE', *, *, #5368, .T. ) ;
#19346=LINE ( 'NONE', #19768, #20702 ) ;
#19350=CIRCLE ( 'NONE', #5395, 13.59999999999999964 ) ;
#19354=CARTESIAN_POINT ( 'NONE',  ( 17.99999999999999645, 23.87611429743662939, 20.54551452399628531 ) ) ;
#19383=VERTEX_POINT ( 'NONE', #17337 ) ;
#19389=CIRCLE ( 'NONE', #11721, 31.49899999999999523 ) ;
#19396=EDGE_CURVE ( 'NONE', #10739, #1839, #36857, .T. ) ;
#19405=DIRECTION ( 'NONE',  ( -1.000000000000000000, 0.000000000000000000, 0.000000000000000000 ) ) ;
#19424=DIRECTION ( 'NONE',  ( -1.000000000000000000, -0.000000000000000000, -0.000000000000000000 ) ) ;
#19444=ORIENTED_EDGE ( 'NONE', *, *, #24910, .F. ) ;
#19461=CARTESIAN_POINT ( 'NONE',  ( 17.99999999999999645, 30.78424799127067502, 6.672111855473287001 ) ) ;
#19463=ADVANCED_FACE ( 'NONE', ( #6817 ), #9669, .T. ) ;
#19480=ADVANCED_FACE ( 'NONE', ( #19951 ), #11192, .T. ) ;
#19482=EDGE_LOOP ( 'NONE', ( #11345, #19320, #22058, #8652 ) ) ;
#19486=CARTESIAN_POINT ( 'NONE',  ( 17.99999999999999645, 0.000000000000000000, 0.000000000000000000 ) ) ;
#19491=DIRECTION ( 'NONE',  ( 0.000000000000000000, 0.000000000000000000, 1.000000000000000000 ) ) ;
#19536=ADVANCED_FACE ( 'NONE', ( #37774 ), #11623, .T. ) ;
#19537=VERTEX_POINT ( 'NONE', #37991 ) ;
#19538=CARTESIAN_POINT ( 'NONE',  ( 17.99999999999999645, -29.03409033315590904, 12.21509719675380623 ) ) ;
#19548=ORIENTED_EDGE ( 'NONE', *, *, #19150, .F. ) ;
#19582=EDGE_CURVE ( 'NONE', #38585, #16643, #43111, .T. ) ;
#19596=DIRECTION ( 'NONE',  ( 0.000000000000000000, 0.000000000000000000, -1.000000000000000000 ) ) ;
#19606=CYLINDRICAL_SURFACE ( 'NONE', #3684, 36.00000000000000000 ) ;
#19624=VERTEX_POINT ( 'NONE', #31471 ) ;
#19625=DIRECTION ( 'NONE',  ( -1.000000000000000000, 0.000000000000000000, -0.000000000000000000 ) ) ;
#19634=ORIENTED_EDGE ( 'NONE', *, *, #36140, .T. ) ;
#19636=ADVANCED_FACE ( 'NONE', ( #4614 ), #38630, .T. ) ;
#19653=EDGE_CURVE ( 'NONE', #40785, #42378, #34093, .T. ) ;
#19664=AXIS2_PLACEMENT_3D ( 'NONE', #2301, #39177, #12396 ) ;
#19672=CARTESIAN_POINT ( 'NONE',  ( 17.99999999999999645, 19.69434969228073484, 24.58291258574055860 ) ) ;
#19678=DIRECTION ( 'NONE',  ( 0.000000000000000000, 0.000000000000000000, 1.000000000000000000 ) ) ;
#19685=VECTOR ( 'NONE', #4309, 1000.000000000000000 ) ;
#19689=VECTOR ( 'NONE', #12734, 1000.000000000000000 ) ;
#19692=CARTESIAN_POINT ( 'NONE',  ( 0.000000000000000000, -26.29521155129837595, -17.34211205339375184 ) ) ;
#19693=VECTOR ( 'NONE', #18806, 1000.000000000000000 ) ;
#19703=DIRECTION ( 'NONE',  ( -1.000000000000000000, -0.000000000000000000, -0.000000000000000000 ) ) ;
#19712=CARTESIAN_POINT ( 'NONE',  ( 0.000000000000000000, 0.000000000000000000, 0.000000000000000000 ) ) ;
#19714=ADVANCED_FACE ( 'NONE', ( #15127 ), #28432, .T. ) ;
#19719=ORIENTED_EDGE ( 'NONE', *, *, #8988, .F. ) ;
#19726=CARTESIAN_POINT ( 'NONE',  ( 17.99999999999999645, 25.52601536738592358, 19.21447964122706509 ) ) ;
#19729=ORIENTED_EDGE ( 'NONE', *, *, #24596, .T. ) ;
#19745=ORIENTED_EDGE ( 'NONE', *, *, #23857, .F. ) ;
#19749=VERTEX_POINT ( 'NONE', #5269 ) ;
#19761=PRESENTATION_STYLE_ASSIGNMENT (( #9901 ) ) ;
#19768=CARTESIAN_POINT ( 'NONE',  ( 9.000000000000000000, -34.45183346761142928, 10.44371441202643247 ) ) ;
#19770=EDGE_CURVE ( 'NONE', #41289, #10692, #22302, .T. ) ;
#19786=DIRECTION ( 'NONE',  ( -1.000000000000000000, 0.000000000000000000, 0.000000000000000000 ) ) ;
#19788=DIRECTION ( 'NONE',  ( -1.000000000000000000, -0.000000000000000000, -0.000000000000000000 ) ) ;
#19789=CARTESIAN_POINT ( 'NONE',  ( 17.99999999999999645, 0.000000000000000000, 0.000000000000000000 ) ) ;
#19796=VECTOR ( 'NONE', #32589, 1000.000000000000000 ) ;
#19805=DIRECTION ( 'NONE',  ( 0.000000000000000000, 0.3612416661871537538, -0.9324722294043554793 ) ) ;
#19817=DIRECTION ( 'NONE',  ( -1.000000000000000000, -0.000000000000000000, -0.000000000000000000 ) ) ;
#19833=ORIENTED_EDGE ( 'NONE', *, *, #356, .T. ) ;
#19849=ORIENTED_EDGE ( 'NONE', *, *, #10236, .F. ) ;
#19861=DIRECTION ( 'NONE',  ( 0.000000000000000000, -0.9618256431728219313, 0.2736629900720729536 ) ) ;
#19874=LINE ( 'NONE', #6308, #27235 ) ;
#19889=VECTOR ( 'NONE', #13676, 1000.000000000000000 ) ;
#19922=CARTESIAN_POINT ( 'NONE',  ( 0.000000000000000000, 0.000000000000000000, 0.000000000000000000 ) ) ;
#19931=ORIENTED_EDGE ( 'NONE', *, *, #2655, .F. ) ;
#19935=DIRECTION ( 'NONE',  ( -1.000000000000000000, 0.000000000000000000, -0.000000000000000000 ) ) ;
#19942=ORIENTED_EDGE ( 'NONE', *, *, #16760, .F. ) ;
#19951=FACE_OUTER_BOUND ( 'NONE', #28977, .T. ) ;
#19958=EDGE_CURVE ( 'NONE', #21901, #20287, #24027, .T. ) ;
#19963=EDGE_LOOP ( 'NONE', ( #35391, #38967, #23446, #39056 ) ) ;
#19964=VECTOR ( 'NONE', #17458, 1000.000000000000000 ) ;
#19974=AXIS2_PLACEMENT_3D ( 'NONE', #25745, #18144, #31841 ) ;
#19982=DIRECTION ( 'NONE',  ( -1.000000000000000000, 0.000000000000000000, 0.000000000000000000 ) ) ;
#20015=DIRECTION ( 'NONE',  ( -1.000000000000000000, -0.000000000000000000, -0.000000000000000000 ) ) ;
#20016=ORIENTED_EDGE ( 'NONE', *, *, #16437, .T. ) ;
#20019=CARTESIAN_POINT ( 'NONE',  ( 17.99999999999999645, 31.81777574834302058, 2.898764365605871696 ) ) ;
#20030=ORIENTED_EDGE ( 'NONE', *, *, #12645, .F. ) ;
#20032=CARTESIAN_POINT ( 'NONE',  ( 0.000000000000000000, 0.000000000000000000, 0.000000000000000000 ) ) ;
#20047=FACE_OUTER_BOUND ( 'NONE', #1701, .T. ) ;
#20051=CARTESIAN_POINT ( 'NONE',  ( 17.99999999999999645, 30.74337109795219547, -8.695908345466218492 ) ) ;
#20052=ORIENTED_EDGE ( 'NONE', *, *, #18739, .T. ) ;
#20063=ORIENTED_EDGE ( 'NONE', *, *, #5961, .T. ) ;
#20073=DIRECTION ( 'NONE',  ( -1.000000000000000000, 0.000000000000000000, 0.000000000000000000 ) ) ;
#20074=ORIENTED_EDGE ( 'NONE', *, *, #1469, .F. ) ;
#20080=ORIENTED_EDGE ( 'NONE', *, *, #23616, .T. ) ;
#20081=DIRECTION ( 'NONE',  ( 0.000000000000000000, -0.9618256431728160472, -0.2736629900720938813 ) ) ;
#20083=EDGE_CURVE ( 'NONE', #40347, #6169, #38907, .T. ) ;
#20085=ADVANCED_FACE ( 'NONE', ( #20540 ), #33810, .T. ) ;
#20090=CARTESIAN_POINT ( 'NONE',  ( 17.99999999999999645, 31.80866420683990725, 2.997093558041416195 ) ) ;
#20091=CARTESIAN_POINT ( 'NONE',  ( 17.99999999999999645, 0.000000000000000000, 0.000000000000000000 ) ) ;
#20094=DIRECTION ( 'NONE',  ( 0.000000000000000000, 0.000000000000000000, 1.000000000000000000 ) ) ;
#20105=AXIS2_PLACEMENT_3D ( 'NONE', #26047, #16450, #36055 ) ;
#20106=DIRECTION ( 'NONE',  ( -1.000000000000000000, 0.000000000000000000, -0.000000000000000000 ) ) ;
#20116=ORIENTED_EDGE ( 'NONE', *, *, #11129, .F. ) ;
#20117=DIRECTION ( 'NONE',  ( -1.000000000000000000, 0.000000000000000000, -0.000000000000000000 ) ) ;
#20131=CARTESIAN_POINT ( 'NONE',  ( 17.99999999999999645, -31.80866420683992857, 2.997093558041182160 ) ) ;
#20161=DIRECTION ( 'NONE',  ( 0.000000000000000000, 0.000000000000000000, 1.000000000000000000 ) ) ;
#20176=AXIS2_PLACEMENT_3D ( 'NONE', #40458, #40245, #7088 ) ;
#20179=CARTESIAN_POINT ( 'NONE',  ( 0.000000000000000000, 0.000000000000000000, 0.000000000000000000 ) ) ;
#20184=DIRECTION ( 'NONE',  ( 0.000000000000000000, 0.000000000000000000, -1.000000000000000000 ) ) ;
#20194=CARTESIAN_POINT ( 'NONE',  ( 17.99999999999999645, 2.007101075700415738, -31.43498920425966858 ) ) ;
#20208=DIRECTION ( 'NONE',  ( 0.000000000000000000, 0.000000000000000000, 1.000000000000000000 ) ) ;
#20211=ADVANCED_FACE ( 'NONE', ( #25953 ), #19209, .T. ) ;
#20215=VERTEX_POINT ( 'NONE', #19007 ) ;
#20220=ORIENTED_EDGE ( 'NONE', *, *, #4554, .F. ) ;
#20226=EDGE_LOOP ( 'NONE', ( #3984, #4830, #5306, #26849 ) ) ;
#20231=CARTESIAN_POINT ( 'NONE',  ( 0.000000000000000000, 13.57797752207971520, -33.34124362422459598 ) ) ;
#20233=FACE_OUTER_BOUND ( 'NONE', #7729, .T. ) ;
#20234=ORIENTED_EDGE ( 'NONE', *, *, #42958, .F. ) ;
#20241=ORIENTED_EDGE ( 'NONE', *, *, #22301, .T. ) ;
#20253=ADVANCED_FACE ( 'NONE', ( #33546 ), #39434, .T. ) ;
#20265=CIRCLE ( 'NONE', #4200, 31.49899999999999878 ) ;
#20276=DIRECTION ( 'NONE',  ( 0.000000000000000000, 0.000000000000000000, 1.000000000000000000 ) ) ;
#20280=CARTESIAN_POINT ( 'NONE',  ( 17.99999999999999645, -27.24480646643618442, 15.80846360676574669 ) ) ;
#20287=VERTEX_POINT ( 'NONE', #22694 ) ;
#20291=DIRECTION ( 'NONE',  ( -1.000000000000000000, 0.000000000000000000, 0.000000000000000000 ) ) ;
#20295=CARTESIAN_POINT ( 'NONE',  ( 17.99999999999999645, 0.000000000000000000, 0.000000000000000000 ) ) ;
#20301=DIRECTION ( 'NONE',  ( 0.000000000000000000, 0.3612416661871471479, 0.9324722294043581439 ) ) ;
#20308=ORIENTED_EDGE ( 'NONE', *, *, #33563, .T. ) ;
#20318=CIRCLE ( 'NONE', #18250, 13.60000000000000142 ) ;
#20338=DIRECTION ( 'NONE',  ( 0.000000000000000000, 0.000000000000000000, 1.000000000000000000 ) ) ;
#20341=DIRECTION ( 'NONE',  ( -1.000000000000000000, 0.000000000000000000, 0.000000000000000000 ) ) ;
#20344=CYLINDRICAL_SURFACE ( 'NONE', #30081, 31.49899999999999878 ) ;
#20350=AXIS2_PLACEMENT_3D ( 'NONE', #20032, #26978, #33940 ) ;
#20351=CARTESIAN_POINT ( 'NONE',  ( 0.000000000000000000, -31.94619804602753277, -16.59639811537390131 ) ) ;
#20352=DIRECTION ( 'NONE',  ( -1.000000000000000000, -0.000000000000000000, -0.000000000000000000 ) ) ;
#20354=CIRCLE ( 'NONE', #5679, 36.00000000000000000 ) ;
#20365=CYLINDRICAL_SURFACE ( 'NONE', #2028, 36.00000000000000000 ) ;
#20374=VERTEX_POINT ( 'NONE', #13939 ) ;
#20389=ADVANCED_FACE ( 'NONE', ( #30515 ), #30927, .T. ) ;
#20399=ORIENTED_EDGE ( 'NONE', *, *, #52, .T. ) ;
#20401=PRODUCT_DEFINITION_SHAPE ( 'NONE', 'NONE',  #3027 ) ;
#20404=CARTESIAN_POINT ( 'NONE',  ( 17.99999999999999645, 30.71634675606053833, 8.790889055186667633 ) ) ;
#20420=EDGE_CURVE ( 'NONE', #14987, #28874, #27676, .T. ) ;
#20435=VERTEX_POINT ( 'NONE', #7139 ) ;
#20449=VERTEX_POINT ( 'NONE', #14363 ) ;
#20452=LINE ( 'NONE', #40465, #28752 ) ;
#20455=CARTESIAN_POINT ( 'NONE',  ( 0.000000000000000000, 0.000000000000000000, 0.000000000000000000 ) ) ;
#20462=ADVANCED_FACE ( 'NONE', ( #40946 ), #31155, .T. ) ;
#20469=EDGE_LOOP ( 'NONE', ( #34120, #17949, #26480, #20399 ) ) ;
#20473=ORIENTED_EDGE ( 'NONE', *, *, #18344, .T. ) ;
#20482=DIRECTION ( 'NONE',  ( 0.000000000000000000, -0.7980172272802448230, 0.6026346363792492999 ) ) ;
#20485=CARTESIAN_POINT ( 'NONE',  ( 0.000000000000000000, -32.49609705003715732, 15.49205204337262920 ) ) ;
#20509=DIRECTION ( 'NONE',  ( 0.000000000000000000, 0.000000000000000000, 1.000000000000000000 ) ) ;
#20512=CARTESIAN_POINT ( 'NONE',  ( 17.99999999999999645, 30.78424799127067502, 6.672111855473287001 ) ) ;
#20516=EDGE_LOOP ( 'NONE', ( #24179, #22335, #14392, #28632 ) ) ;
#20531=DIRECTION ( 'NONE',  ( -1.000000000000000000, -0.000000000000000000, -0.000000000000000000 ) ) ;
#20538=VERTEX_POINT ( 'NONE', #4956 ) ;
#20540=FACE_OUTER_BOUND ( 'NONE', #38767, .T. ) ;
#20574=DIRECTION ( 'NONE',  ( -1.000000000000000000, 0.000000000000000000, -0.000000000000000000 ) ) ;
#20575=CARTESIAN_POINT ( 'NONE',  ( 17.99999999999999645, 14.84191762912315049, 27.78316904333131276 ) ) ;
#20591=ORIENTED_EDGE ( 'NONE', *, *, #21061, .T. ) ;
#20594=DIRECTION ( 'NONE',  ( 0.000000000000000000, 0.000000000000000000, 1.000000000000000000 ) ) ;
#20626=ORIENTED_EDGE ( 'NONE', *, *, #588, .T. ) ;
#20632=CARTESIAN_POINT ( 'NONE',  ( 0.000000000000000000, 0.000000000000000000, 0.000000000000000000 ) ) ;
#20635=ORIENTED_EDGE ( 'NONE', *, *, #27809, .F. ) ;
#20642=AXIS2_PLACEMENT_3D ( 'NONE', #24994, #1801, #14933 ) ;
#20651=CARTESIAN_POINT ( 'NONE',  ( 17.99999999999999645, -23.87611429743677505, 20.54551452399611478 ) ) ;
#20655=DIRECTION ( 'NONE',  ( -1.000000000000000000, -0.000000000000000000, 0.000000000000000000 ) ) ;
#20658=EDGE_LOOP ( 'NONE', ( #33256, #22285, #29495, #22404 ) ) ;
#20666=ORIENTED_EDGE ( 'NONE', *, *, #14034, .F. ) ;
#20673=DIRECTION ( 'NONE',  ( -1.000000000000000000, 0.000000000000000000, 0.000000000000000000 ) ) ;
#20693=ORIENTED_EDGE ( 'NONE', *, *, #18836, .T. ) ;
#20702=VECTOR ( 'NONE', #33032, 1000.000000000000000 ) ;
#20704=VERTEX_POINT ( 'NONE', #23077 ) ;
#20705=DIRECTION ( 'NONE',  ( 0.000000000000000000, 0.000000000000000000, 1.000000000000000000 ) ) ;
#20724=ORIENTED_EDGE ( 'NONE', *, *, #16992, .T. ) ;
#20728=ORIENTED_EDGE ( 'NONE', *, *, #5044, .F. ) ;
#20730=VERTEX_POINT ( 'NONE', #20231 ) ;
#20731=CARTESIAN_POINT ( 'NONE',  ( -10.00000000000000000, 0.000000000000000000, 0.000000000000000000 ) ) ;
#20739=CARTESIAN_POINT ( 'NONE',  ( 17.99999999999999645, -9.484061862023704492, -30.03730300138991538 ) ) ;
#20764=VECTOR ( 'NONE', #42767, 1000.000000000000000 ) ;
#20771=ORIENTED_EDGE ( 'NONE', *, *, #19653, .F. ) ;
#20776=AXIS2_PLACEMENT_3D ( 'NONE', #30617, #26268, #39539 ) ;
#20783=AXIS2_PLACEMENT_3D ( 'NONE', #37086, #13558, #26855 ) ;
#20786=ORIENTED_EDGE ( 'NONE', *, *, #4310, .T. ) ;
#20788=DIRECTION ( 'NONE',  ( 0.000000000000000000, -0.7980172272802321665, -0.6026346363792660643 ) ) ;
#20797=DIRECTION ( 'NONE',  ( 0.000000000000000000, 0.000000000000000000, 1.000000000000000000 ) ) ;
#20814=AXIS2_PLACEMENT_3D ( 'NONE', #39047, #1978, #5683 ) ;
#20828=ORIENTED_EDGE ( 'NONE', *, *, #22930, .T. ) ;
#20837=ORIENTED_EDGE ( 'NONE', *, *, #2534, .F. ) ;
#20840=CARTESIAN_POINT ( 'NONE',  ( 0.000000000000000000, 34.78944633786291973, -9.257128253673256424 ) ) ;
#20845=EDGE_CURVE ( 'NONE', #14556, #4975, #17171, .T. ) ;
#20864=DIRECTION ( 'NONE',  ( -1.000000000000000000, -0.000000000000000000, -0.000000000000000000 ) ) ;
#20868=EDGE_LOOP ( 'NONE', ( #34557, #32111, #6980, #39013 ) ) ;
#20883=CARTESIAN_POINT ( 'NONE',  ( 0.000000000000000000, -3.803237743092135581, 31.26855263151013276 ) ) ;
#20891=EDGE_LOOP ( 'NONE', ( #321, #43, #16311, #12568 ) ) ;
#20892=DIRECTION ( 'NONE',  ( -1.000000000000000000, -0.000000000000000000, -0.000000000000000000 ) ) ;
#20896=CARTESIAN_POINT ( 'NONE',  ( 17.99999999999999645, 11.58753559615485251, 29.77419532459266449 ) ) ;
#20906=AXIS2_PLACEMENT_3D ( 'NONE', #7234, #36470, #20594 ) ;
#20915=EDGE_CURVE ( 'NONE', #27491, #23539, #22298, .T. ) ;
#20924=FACE_OUTER_BOUND ( 'NONE', #36061, .T. ) ;
#20929=AXIS2_PLACEMENT_3D ( 'NONE', #12316, #2658, #38679 ) ;
#20941=DIRECTION ( 'NONE',  ( -1.000000000000000000, 0.000000000000000000, 0.000000000000000000 ) ) ;
#20944=DIRECTION ( 'NONE',  ( 0.000000000000000000, 0.000000000000000000, 1.000000000000000000 ) ) ;
#20955=CARTESIAN_POINT ( 'NONE',  ( 0.000000000000000000, -31.80866420683992857, 2.997093558041182160 ) ) ;
#20984=CARTESIAN_POINT ( 'NONE',  ( 8.999999999999998224, -28.35267316522767445, -22.18391138608739155 ) ) ;
#20988=CIRCLE ( 'NONE', #17490, 31.49899999999999878 ) ;
#20995=FACE_OUTER_BOUND ( 'NONE', #22594, .T. ) ;
#21007=EDGE_CURVE ( 'NONE', #26154, #29573, #218, .T. ) ;
#21008=ADVANCED_FACE ( 'NONE', ( #32978 ), #20365, .T. ) ;
#21012=DIRECTION ( 'NONE',  ( -1.000000000000000000, -0.000000000000000000, 0.000000000000000000 ) ) ;
#21021=AXIS2_PLACEMENT_3D ( 'NONE', #33015, #26490, #29774 ) ;
#21024=LINE ( 'NONE', #24947, #35798 ) ;
#21034=CARTESIAN_POINT ( 'NONE',  ( 0.000000000000000000, 0.000000000000000000, 0.000000000000000000 ) ) ;
#21044=ORIENTED_EDGE ( 'NONE', *, *, #40138, .T. ) ;
#21052=CARTESIAN_POINT ( 'NONE',  ( 0.000000000000000000, 0.000000000000000000, 0.000000000000000000 ) ) ;
#21059=EDGE_CURVE ( 'NONE', #6599, #40723, #3710, .T. ) ;
#21061=EDGE_CURVE ( 'NONE', #31789, #4637, #3418, .T. ) ;
#21082=VERTEX_POINT ( 'NONE', #13376 ) ;
#21083=AXIS2_PLACEMENT_3D ( 'NONE', #22656, #26123, #2523 ) ;
#21108=EDGE_CURVE ( 'NONE', #43124, #25635, #12724, .T. ) ;
#21118=CYLINDRICAL_SURFACE ( 'NONE', #22021, 31.49899999999999878 ) ;
#21138=DIRECTION ( 'NONE',  ( 0.000000000000000000, 0.000000000000000000, 1.000000000000000000 ) ) ;
#21141=DIRECTION ( 'NONE',  ( -1.000000000000000000, 0.000000000000000000, -0.000000000000000000 ) ) ;
#21144=DIRECTION ( 'NONE',  ( -1.000000000000000000, 0.000000000000000000, 0.000000000000000000 ) ) ;
#21145=AXIS2_PLACEMENT_3D ( 'NONE', #14366, #16798, #27681 ) ;
#21155=CARTESIAN_POINT ( 'NONE',  ( -10.00000000000000000, 0.000000000000000000, 0.000000000000000000 ) ) ;
#21178=CARTESIAN_POINT ( 'NONE',  ( 0.000000000000000000, 32.49609705003727100, -15.49205204337240005 ) ) ;
#21191=ADVANCED_FACE ( 'NONE', ( #34490 ), #11176, .T. ) ;
#21192=DIRECTION ( 'NONE',  ( -1.000000000000000000, 0.000000000000000000, 0.000000000000000000 ) ) ;
#21202=ORIENTED_EDGE ( 'NONE', *, *, #23934, .F. ) ;
#21210=AXIS2_PLACEMENT_3D ( 'NONE', #17635, #27647, #7323 ) ;
#21212=CARTESIAN_POINT ( 'NONE',  ( 17.99999999999999645, -31.81777574834308098, 2.898764365605205562 ) ) ;
#21218=VERTEX_POINT ( 'NONE', #40812 ) ;
#21220=ADVANCED_FACE ( 'NONE', ( #10964 ), #14460, .T. ) ;
#21235=DIRECTION ( 'NONE',  ( -1.000000000000000000, 0.000000000000000000, -0.000000000000000000 ) ) ;
#21236=ORIENTED_EDGE ( 'NONE', *, *, #6275, .T. ) ;
#21253=ORIENTED_EDGE ( 'NONE', *, *, #737, .F. ) ;
#21258=EDGE_CURVE ( 'NONE', #27491, #12909, #29207, .T. ) ;
#21280=FACE_OUTER_BOUND ( 'NONE', #38432, .T. ) ;
#21286=FACE_OUTER_BOUND ( 'NONE', #9097, .T. ) ;
#21296=CIRCLE ( 'NONE', #37960, 13.60000000000000142 ) ;
#21297=EDGE_LOOP ( 'NONE', ( #20308, #36985, #3073, #10309 ) ) ;
#21302=EDGE_CURVE ( 'NONE', #10153, #32077, #15043, .T. ) ;
#21334=CARTESIAN_POINT ( 'NONE',  ( 17.99999999999999645, -26.29521155129837595, -17.34211205339375184 ) ) ;
#21338=ORIENTED_EDGE ( 'NONE', *, *, #5000, .F. ) ;
#21339=AXIS2_PLACEMENT_3D ( 'NONE', #32764, #42368, #9651 ) ;
#21358=AXIS2_PLACEMENT_3D ( 'NONE', #17016, #30301, #374 ) ;
#21361=CIRCLE ( 'NONE', #38024, 36.00000000000000000 ) ;
#21402=CARTESIAN_POINT ( 'NONE',  ( 9.000000000000000000, 7.220349212960960550, -35.26849241522656087 ) ) ;
#21411=ADVANCED_FACE ( 'NONE', ( #8324 ), #24957, .T. ) ;
#21426=EDGE_CURVE ( 'NONE', #17650, #17796, #21683, .T. ) ;
#21429=CARTESIAN_POINT ( 'NONE',  ( 8.999999999999998224, 23.79363200506953291, 27.01597816121656237 ) ) ;
#21433=DIRECTION ( 'NONE',  ( 1.000000000000000000, -0.000000000000000000, -0.000000000000000000 ) ) ;
#21437=DIRECTION ( 'NONE',  ( -1.000000000000000000, 0.000000000000000000, -0.000000000000000000 ) ) ;
#21444=AXIS2_PLACEMENT_3D ( 'NONE', #1444, #8000, #41806 ) ;
#21462=FACE_OUTER_BOUND ( 'NONE', #17356, .T. ) ;
#21464=DIRECTION ( 'NONE',  ( 0.000000000000000000, 0.9618256431728199329, -0.2736629900720800590 ) ) ;
#21468=EDGE_CURVE ( 'NONE', #42039, #1458, #5258, .T. ) ;
#21503=EDGE_CURVE ( 'NONE', #38187, #14447, #9310, .T. ) ;
#21524=EDGE_LOOP ( 'NONE', ( #4514, #870, #42287, #20786 ) ) ;
#21534=CARTESIAN_POINT ( 'NONE',  ( 9.000000000000000000, 35.78425302087543969, -3.935382540232422510 ) ) ;
#21537=AXIS2_PLACEMENT_3D ( 'NONE', #28842, #41703, #21895 ) ;
#21542=DIRECTION ( 'NONE',  ( -1.000000000000000000, -0.000000000000000000, 0.000000000000000000 ) ) ;
#21547=ORIENTED_EDGE ( 'NONE', *, *, #18739, .F. ) ;
#21552=CIRCLE ( 'NONE', #15173, 13.59999999999999964 ) ;
#21572=DIRECTION ( 'NONE',  ( 1.000000000000000000, 0.000000000000000000, 0.000000000000000000 ) ) ;
#21575=VECTOR ( 'NONE', #34786, 1000.000000000000000 ) ;
#21608=EDGE_CURVE ( 'NONE', #15182, #20449, #22525, .T. ) ;
#21615=EDGE_CURVE ( 'NONE', #12218, #5335, #28150, .T. ) ;
#21620=EDGE_LOOP ( 'NONE', ( #29353, #20234, #16187, #16102 ) ) ;
#21625=AXIS2_PLACEMENT_3D ( 'NONE', #4300, #811, #11531 ) ;
#21631=ORIENTED_EDGE ( 'NONE', *, *, #8859, .T. ) ;
#21634=DIRECTION ( 'NONE',  ( -1.000000000000000000, 0.000000000000000000, 0.000000000000000000 ) ) ;
#21638=CARTESIAN_POINT ( 'NONE',  ( 17.99999999999999645, 23.79363200506953291, 27.01597816121656237 ) ) ;
#21640=ORIENTED_EDGE ( 'NONE', *, *, #8276, .F. ) ;
#21648=ORIENTED_EDGE ( 'NONE', *, *, #21907, .F. ) ;
#21650=ORIENTED_EDGE ( 'NONE', *, *, #17742, .F. ) ;
#21657=DIRECTION ( 'NONE',  ( -1.000000000000000000, -0.000000000000000000, -0.000000000000000000 ) ) ;
#21665=DIRECTION ( 'NONE',  ( -1.000000000000000000, -0.000000000000000000, -0.000000000000000000 ) ) ;
#21683=LINE ( 'NONE', #14466, #2455 ) ;
#21694=DIRECTION ( 'NONE',  ( 0.000000000000000000, 0.8951632913550635617, -0.4457383557765359772 ) ) ;
#21701=CARTESIAN_POINT ( 'NONE',  ( 0.000000000000000000, 0.000000000000000000, 0.000000000000000000 ) ) ;
#21703=CIRCLE ( 'NONE', #29329, 31.49899999999999878 ) ;
#21704=CARTESIAN_POINT ( 'NONE',  ( 17.99999999999999645, 0.000000000000000000, 0.000000000000000000 ) ) ;
#21710=CIRCLE ( 'NONE', #23067, 13.59999999999999964 ) ;
#21714=DIRECTION ( 'NONE',  ( 0.000000000000000000, 0.000000000000000000, 1.000000000000000000 ) ) ;
#21717=DIRECTION ( 'NONE',  ( -1.000000000000000000, -0.000000000000000000, -0.000000000000000000 ) ) ;
#21718=ORIENTED_EDGE ( 'NONE', *, *, #36641, .F. ) ;
#21727=CARTESIAN_POINT ( 'NONE',  ( 0.000000000000000000, -19.47322409167291113, 30.27859877001393230 ) ) ;
#21754=AXIS2_PLACEMENT_3D ( 'NONE', #10770, #27151, #46 ) ;
#21757=VERTEX_POINT ( 'NONE', #408 ) ;
#21767=DIRECTION ( 'NONE',  ( -1.000000000000000000, 0.000000000000000000, 0.000000000000000000 ) ) ;
#21768=DIRECTION ( 'NONE',  ( 0.000000000000000000, 0.000000000000000000, -1.000000000000000000 ) ) ;
#21773=ADVANCED_FACE ( 'NONE', ( #17484 ), #27278, .T. ) ;
#21786=ORIENTED_EDGE ( 'NONE', *, *, #25577, .F. ) ;
#21795=DIRECTION ( 'NONE',  ( -1.000000000000000000, 0.000000000000000000, 0.000000000000000000 ) ) ;
#21799=ORIENTED_EDGE ( 'NONE', *, *, #29641, .F. ) ;
#21807=FACE_OUTER_BOUND ( 'NONE', #24906, .T. ) ;
#21817=AXIS2_PLACEMENT_3D ( 'NONE', #12078, #15364, #28234 ) ;
#21842=CARTESIAN_POINT ( 'NONE',  ( 17.99999999999999645, 0.000000000000000000, 0.000000000000000000 ) ) ;
#21850=ORIENTED_EDGE ( 'NONE', *, *, #12645, .T. ) ;
#21853=ORIENTED_EDGE ( 'NONE', *, *, #13459, .T. ) ;
#21856=ORIENTED_EDGE ( 'NONE', *, *, #40467, .F. ) ;
#21864=ORIENTED_EDGE ( 'NONE', *, *, #28509, .T. ) ;
#21879=DIRECTION ( 'NONE',  ( 0.000000000000000000, 0.000000000000000000, 1.000000000000000000 ) ) ;
#21880=LINE ( 'NONE', #1971, #13623 ) ;
#21889=DIRECTION ( 'NONE',  ( 0.000000000000000000, 0.000000000000000000, 1.000000000000000000 ) ) ;
#21895=DIRECTION ( 'NONE',  ( 0.000000000000000000, 0.000000000000000000, 1.000000000000000000 ) ) ;
#21901=VERTEX_POINT ( 'NONE', #21638 ) ;
#21907=EDGE_CURVE ( 'NONE', #19127, #12837, #10021, .T. ) ;
#21909=AXIS2_PLACEMENT_3D ( 'NONE', #15790, #5930, #32342 ) ;
#21913=FACE_OUTER_BOUND ( 'NONE', #22545, .T. ) ;
#21920=DIRECTION ( 'NONE',  ( -1.000000000000000000, -0.000000000000000000, -0.000000000000000000 ) ) ;
#21927=ORIENTED_EDGE ( 'NONE', *, *, #5658, .T. ) ;
#21932=CIRCLE ( 'NONE', #30273, 31.49899999999999878 ) ;
#21935=VERTEX_POINT ( 'NONE', #1060 ) ;
#21962=ORIENTED_EDGE ( 'NONE', *, *, #41200, .F. ) ;
#21969=LINE ( 'NONE', #4464, #7445 ) ;
#21971=FACE_OUTER_BOUND ( 'NONE', #14669, .T. ) ;
#21984=ORIENTED_EDGE ( 'NONE', *, *, #32220, .F. ) ;
#21989=DIRECTION ( 'NONE',  ( 0.000000000000000000, 0.000000000000000000, 1.000000000000000000 ) ) ;
#21997=AXIS2_PLACEMENT_3D ( 'NONE', #37667, #21144, #37024 ) ;
#22003=ORIENTED_EDGE ( 'NONE', *, *, #4702, .F. ) ;
#22007=AXIS2_PLACEMENT_3D ( 'NONE', #13663, #20015, #13021 ) ;
#22012=ADVANCED_FACE ( 'NONE', ( #18149 ), #4333, .T. ) ;
#22013=CARTESIAN_POINT ( 'NONE',  ( 17.99999999999999645, -31.80866420683992857, 2.997093558041182160 ) ) ;
#22021=AXIS2_PLACEMENT_3D ( 'NONE', #30251, #10829, #33946 ) ;
#22025=AXIS2_PLACEMENT_3D ( 'NONE', #19486, #1792, #15149 ) ;
#22034=CIRCLE ( 'NONE', #26885, 13.59999999999999964 ) ;
#22036=EDGE_CURVE ( 'NONE', #27845, #28707, #37210, .T. ) ;
#22047=EDGE_LOOP ( 'NONE', ( #35803, #35844 ) ) ;
#22048=DIRECTION ( 'NONE',  ( 0.000000000000000000, 0.000000000000000000, 1.000000000000000000 ) ) ;
#22058=ORIENTED_EDGE ( 'NONE', *, *, #34704, .F. ) ;
#22063=CYLINDRICAL_SURFACE ( 'NONE', #15525, 31.49899999999999878 ) ;
#22080=CYLINDRICAL_SURFACE ( 'NONE', #28749, 13.59999999999999787 ) ;
#22084=ORIENTED_EDGE ( 'NONE', *, *, #32690, .F. ) ;
#22097=AXIS2_PLACEMENT_3D ( 'NONE', #2653, #16015, #29312 ) ;
#22098=DIRECTION ( 'NONE',  ( -1.000000000000000000, 0.000000000000000000, 0.000000000000000000 ) ) ;
#22100=ORIENTED_EDGE ( 'NONE', *, *, #2209, .T. ) ;
#22106=DIRECTION ( 'NONE',  ( -1.000000000000000000, -0.000000000000000000, 0.000000000000000000 ) ) ;
#22115=AXIS2_PLACEMENT_3D ( 'NONE', #7133, #30074, #13715 ) ;
#22154=AXIS2_PLACEMENT_3D ( 'NONE', #1230, #21141, #37873 ) ;
#22157=ADVANCED_FACE ( 'NONE', ( #36164 ), #6278, .T. ) ;
#22160=DIRECTION ( 'NONE',  ( -1.000000000000000000, 0.000000000000000000, 0.000000000000000000 ) ) ;
#22161=DIRECTION ( 'NONE',  ( -1.000000000000000000, 0.000000000000000000, -0.000000000000000000 ) ) ;
#22173=ORIENTED_EDGE ( 'NONE', *, *, #37583, .T. ) ;
#22177=ORIENTED_EDGE ( 'NONE', *, *, #24012, .F. ) ;
#22182=CARTESIAN_POINT ( 'NONE',  ( 17.99999999999999645, 0.000000000000000000, 0.000000000000000000 ) ) ;
#22185=DIRECTION ( 'NONE',  ( 0.000000000000000000, 0.5264321628773570572, -0.8502171357296134380 ) ) ;
#22199=DIRECTION ( 'NONE',  ( 0.000000000000000000, 0.000000000000000000, 1.000000000000000000 ) ) ;
#22210=DIRECTION ( 'NONE',  ( -1.000000000000000000, 0.000000000000000000, -0.000000000000000000 ) ) ;
#22215=ADVANCED_FACE ( 'NONE', ( #16576 ), #29875, .T. ) ;
#22216=CARTESIAN_POINT ( 'NONE',  ( 17.99999999999999645, 0.000000000000000000, 0.000000000000000000 ) ) ;
#22230=DIRECTION ( 'NONE',  ( -1.000000000000000000, 0.000000000000000000, 0.000000000000000000 ) ) ;
#22233=ORIENTED_EDGE ( 'NONE', *, *, #25492, .T. ) ;
#22239=CARTESIAN_POINT ( 'NONE',  ( 0.000000000000000000, -7.749090474611723067, 30.53094492177210384 ) ) ;
#22251=EDGE_CURVE ( 'NONE', #40285, #31747, #26795, .T. ) ;
#22253=LINE ( 'NONE', #2315, #4346 ) ;
#22268=CARTESIAN_POINT ( 'NONE',  ( 17.99999999999999645, 7.749090474611950441, -30.53094492177204700 ) ) ;
#22280=EDGE_CURVE ( 'NONE', #1458, #42747, #10053, .T. ) ;
#22282=ADVANCED_FACE ( 'NONE', ( #3838 ), #9772, .T. ) ;
#22285=ORIENTED_EDGE ( 'NONE', *, *, #35665, .T. ) ;
#22294=ORIENTED_EDGE ( 'NONE', *, *, #1017, .F. ) ;
#22298=CIRCLE ( 'NONE', #41745, 31.49899999999999878 ) ;
#22301=EDGE_CURVE ( 'NONE', #33164, #2232, #353, .T. ) ;
#22302=CIRCLE ( 'NONE', #27861, 13.59999999999999787 ) ;
#22316=CARTESIAN_POINT ( 'NONE',  ( 18.00000000000000355, 0.000000000000000000, 0.000000000000000000 ) ) ;
#22330=CARTESIAN_POINT ( 'NONE',  ( 0.000000000000000000, -19.69434969228056787, -24.58291258574069360 ) ) ;
#22333=CARTESIAN_POINT ( 'NONE',  ( 0.000000000000000000, 14.84191762912354839, -27.78316904333109960 ) ) ;
#22335=ORIENTED_EDGE ( 'NONE', *, *, #3451, .T. ) ;
#22337=CARTESIAN_POINT ( 'NONE',  ( 17.99999999999999645, 0.000000000000000000, 0.000000000000000000 ) ) ;
#22355=CIRCLE ( 'NONE', #27922, 13.59999999999999964 ) ;
#22358=CIRCLE ( 'NONE', #2785, 15.00000000000000000 ) ;
#22363=ORIENTED_EDGE ( 'NONE', *, *, #30085, .T. ) ;
#22397=ORIENTED_EDGE ( 'NONE', *, *, #6275, .F. ) ;
#22404=ORIENTED_EDGE ( 'NONE', *, *, #17600, .T. ) ;
#22409=DIRECTION ( 'NONE',  ( 0.000000000000000000, 0.000000000000000000, 1.000000000000000000 ) ) ;
#22419=LINE ( 'NONE', #25472, #33715 ) ;
#22422=ORIENTED_EDGE ( 'NONE', *, *, #39473, .F. ) ;
#22428=EDGE_CURVE ( 'NONE', #19624, #3495, #14150, .T. ) ;
#22441=VERTEX_POINT ( 'NONE', #35046 ) ;
#22442=ORIENTED_EDGE ( 'NONE', *, *, #25834, .F. ) ;
#22467=CARTESIAN_POINT ( 'NONE',  ( 17.99999999999999645, -29.03409033315573851, -12.21509719675420946 ) ) ;
#22475=VECTOR ( 'NONE', #2940, 1000.000000000000000 ) ;
#22477=CARTESIAN_POINT ( 'NONE',  ( 50.00005079999999680, 0.000000000000000000, 15.00000000000000000 ) ) ;
#22491=ORIENTED_EDGE ( 'NONE', *, *, #1469, .T. ) ;
#22493=VERTEX_POINT ( 'NONE', #28955 ) ;
#22500=DIRECTION ( 'NONE',  ( -1.000000000000000000, -0.000000000000000000, -0.000000000000000000 ) ) ;
#22525=LINE ( 'NONE', #19672, #35072 ) ;
#22526=DIRECTION ( 'NONE',  ( -1.000000000000000000, 0.000000000000000000, -0.000000000000000000 ) ) ;
#22542=ORIENTED_EDGE ( 'NONE', *, *, #26374, .F. ) ;
#22545=EDGE_LOOP ( 'NONE', ( #32035, #18104, #39901, #36671 ) ) ;
#22552=CARTESIAN_POINT ( 'NONE',  ( 17.99999999999999645, -35.78425302087536153, -3.935382540233173465 ) ) ;
#22553=DIRECTION ( 'NONE',  ( 0.000000000000000000, 0.000000000000000000, 1.000000000000000000 ) ) ;
#22560=ORIENTED_EDGE ( 'NONE', *, *, #23258, .F. ) ;
#22563=CARTESIAN_POINT ( 'NONE',  ( 18.00000000000000355, 0.000000000000000000, 15.00000000000000000 ) ) ;
#22576=CARTESIAN_POINT ( 'NONE',  ( 9.000000000000000000, -32.49609705003694415, -15.49205204337308217 ) ) ;
#22579=ORIENTED_EDGE ( 'NONE', *, *, #17101, .T. ) ;
#22586=AXIS2_PLACEMENT_3D ( 'NONE', #37544, #33027, #17520 ) ;
#22594=EDGE_LOOP ( 'NONE', ( #8585, #9059, #1577, #4613 ) ) ;
#22596=ORIENTED_EDGE ( 'NONE', *, *, #38011, .F. ) ;
#22600=DIRECTION ( 'NONE',  ( -1.000000000000000000, -0.000000000000000000, -0.000000000000000000 ) ) ;
#22612=ORIENTED_EDGE ( 'NONE', *, *, #16506, .F. ) ;
#22616=ADVANCED_FACE ( 'NONE', ( #32208 ), #16080, .T. ) ;
#22620=DIRECTION ( 'NONE',  ( 0.000000000000000000, -0.1837495178165777232, 0.9829730996839003421 ) ) ;
#22622=EDGE_CURVE ( 'NONE', #12218, #7715, #5384, .T. ) ;
#22623=EDGE_CURVE ( 'NONE', #39574, #41473, #25274, .T. ) ;
#22631=FACE_OUTER_BOUND ( 'NONE', #19210, .T. ) ;
#22642=CIRCLE ( 'NONE', #42081, 13.59999999999999787 ) ;
#22656=CARTESIAN_POINT ( 'NONE',  ( 17.99999999999999645, 0.000000000000000000, 0.000000000000000000 ) ) ;
#22668=EDGE_LOOP ( 'NONE', ( #39174, #9416, #23055, #36945 ) ) ;
#22675=CIRCLE ( 'NONE', #7299, 31.49899999999999878 ) ;
#22677=ORIENTED_EDGE ( 'NONE', *, *, #14321, .T. ) ;
#22681=CARTESIAN_POINT ( 'NONE',  ( 0.000000000000000000, 22.66088087769211157, -21.87856208362532939 ) ) ;
#22683=ORIENTED_EDGE ( 'NONE', *, *, #39954, .F. ) ;
#22692=EDGE_LOOP ( 'NONE', ( #9559, #39968, #2764, #18990 ) ) ;
#22694=CARTESIAN_POINT ( 'NONE',  ( 0.000000000000000000, 23.79363200506953291, 27.01597816121656237 ) ) ;
#22703=CIRCLE ( 'NONE', #12893, 36.00000000000000000 ) ;
#22708=AXIS2_PLACEMENT_3D ( 'NONE', #41413, #21634, #31614 ) ;
#22733=ADVANCED_FACE ( 'NONE', ( #23493 ), #27179, .T. ) ;
#22744=LINE ( 'NONE', #32738, #36339 ) ;
#22748=ORIENTED_EDGE ( 'NONE', *, *, #963, .F. ) ;
#22758=AXIS2_PLACEMENT_3D ( 'NONE', #16814, #23144, #20094 ) ;
#22761=VECTOR ( 'NONE', #9494, 1000.000000000000000 ) ;
#22768=CIRCLE ( 'NONE', #19974, 13.59999999999999964 ) ;
#22771=EDGE_CURVE ( 'NONE', #9051, #18562, #27520, .T. ) ;
#22787=CARTESIAN_POINT ( 'NONE',  ( 17.99999999999999645, 7.220349212960452512, 35.26849241522666745 ) ) ;
#22802=CIRCLE ( 'NONE', #10205, 31.49899999999999878 ) ;
#22818=EDGE_CURVE ( 'NONE', #18138, #37185, #6436, .T. ) ;
#22820=ORIENTED_EDGE ( 'NONE', *, *, #21059, .T. ) ;
#22832=EDGE_CURVE ( 'NONE', #10211, #17650, #35190, .T. ) ;
#22834=CIRCLE ( 'NONE', #3949, 13.59999999999999964 ) ;
#22842=CIRCLE ( 'NONE', #37424, 31.49899999999999878 ) ;
#22861=CARTESIAN_POINT ( 'NONE',  ( 17.99999999999999645, -5.822172717930484964, 31.41458249383138934 ) ) ;
#22866=DIRECTION ( 'NONE',  ( 0.000000000000000000, 0.000000000000000000, 1.000000000000000000 ) ) ;
#22890=EDGE_LOOP ( 'NONE', ( #15648, #28589, #31133, #31809 ) ) ;
#22896=CIRCLE ( 'NONE', #4010, 13.59999999999999964 ) ;
#22905=ADVANCED_FACE ( 'NONE', ( #14962 ), #34134, .T. ) ;
#22915=CARTESIAN_POINT ( 'NONE',  ( 17.99999999999999645, 13.22719389141978930, 28.58720592780601066 ) ) ;
#22917=CARTESIAN_POINT ( 'NONE',  ( 17.99999999999999645, 16.86122981692017930, 27.13802899033298388 ) ) ;
#22920=DIRECTION ( 'NONE',  ( 1.000000000000000000, -0.000000000000000000, 0.000000000000000000 ) ) ;
#22925=CARTESIAN_POINT ( 'NONE',  ( 17.99999999999999645, 0.000000000000000000, 0.000000000000000000 ) ) ;
#22930=EDGE_CURVE ( 'NONE', #12909, #33094, #21296, .T. ) ;
#22936=DIRECTION ( 'NONE',  ( -1.000000000000000000, -0.000000000000000000, 0.000000000000000000 ) ) ;
#22951=CARTESIAN_POINT ( 'NONE',  ( 0.000000000000000000, 34.45183346761150034, -10.44371441202619621 ) ) ;
#22953=VECTOR ( 'NONE', #29926, 1000.000000000000000 ) ;
#22968=CARTESIAN_POINT ( 'NONE',  ( 17.99999999999999645, 31.81777574834305966, 10.70123563439457293 ) ) ;
#22976=EDGE_LOOP ( 'NONE', ( #22397, #36092, #9216, #27574 ) ) ;
#22977=LINE ( 'NONE', #6341, #23719 ) ;
#22983=DIRECTION ( 'NONE',  ( 0.000000000000000000, 0.000000000000000000, 1.000000000000000000 ) ) ;
#22987=DIRECTION ( 'NONE',  ( -1.000000000000000000, -0.000000000000000000, -0.000000000000000000 ) ) ;
#22992=CARTESIAN_POINT ( 'NONE',  ( 17.99999999999999645, 3.803237743091921974, 31.26855263151016828 ) ) ;
#22994=AXIS2_PLACEMENT_3D ( 'NONE', #3118, #12997, #22409 ) ;
#23000=DIRECTION ( 'NONE',  ( -1.000000000000000000, -0.000000000000000000, -0.000000000000000000 ) ) ;
#23003=VECTOR ( 'NONE', #18691, 1000.000000000000000 ) ;
#23006=CARTESIAN_POINT ( 'NONE',  ( 17.99999999999999645, 0.000000000000000000, 0.000000000000000000 ) ) ;
#23009=CARTESIAN_POINT ( 'NONE',  ( 17.99999999999999645, 0.000000000000000000, 0.000000000000000000 ) ) ;
#23011=FACE_OUTER_BOUND ( 'NONE', #32452, .T. ) ;
#23019=CARTESIAN_POINT ( 'NONE',  ( 17.99999999999999645, -2.007101075699733173, -31.43498920425971832 ) ) ;
#23029=ORIENTED_EDGE ( 'NONE', *, *, #3582, .T. ) ;
#23039=CARTESIAN_POINT ( 'NONE',  ( 17.99999999999999645, 0.000000000000000000, 0.000000000000000000 ) ) ;
#23050=DIRECTION ( 'NONE',  ( -1.000000000000000000, 0.000000000000000000, 0.000000000000000000 ) ) ;
#23055=ORIENTED_EDGE ( 'NONE', *, *, #2257, .T. ) ;
#23065=CARTESIAN_POINT ( 'NONE',  ( 0.000000000000000000, 0.000000000000000000, 0.000000000000000000 ) ) ;
#23067=AXIS2_PLACEMENT_3D ( 'NONE', #20896, #544, #30679 ) ;
#23077=CARTESIAN_POINT ( 'NONE',  ( 17.99999999999999645, 9.484061862024356415, -30.03730300138970932 ) ) ;
#23084=VERTEX_POINT ( 'NONE', #18468 ) ;
#23086=CARTESIAN_POINT ( 'NONE',  ( 17.99999999999999645, 0.000000000000000000, 0.000000000000000000 ) ) ;
#23093=EDGE_CURVE ( 'NONE', #13228, #16681, #18560, .T. ) ;
#23104=DIRECTION ( 'NONE',  ( -1.000000000000000000, -0.000000000000000000, -0.000000000000000000 ) ) ;
#23107=DIRECTION ( 'NONE',  ( 0.000000000000000000, 0.1837495178165637344, 0.9829730996839030066 ) ) ;
#23112=ORIENTED_EDGE ( 'NONE', *, *, #18639, .T. ) ;
#23121=DIRECTION ( 'NONE',  ( 0.000000000000000000, -0.5264321628773627193, 0.8502171357296098853 ) ) ;
#23125=CARTESIAN_POINT ( 'NONE',  ( 0.000000000000000000, 28.62203781743003717, 14.19692359621465094 ) ) ;
#23129=CIRCLE ( 'NONE', #41862, 36.00000000000000000 ) ;
#23133=CIRCLE ( 'NONE', #14747, 13.59999999999999787 ) ;
#23141=FACE_OUTER_BOUND ( 'NONE', #26955, .T. ) ;
#23144=DIRECTION ( 'NONE',  ( -1.000000000000000000, -0.000000000000000000, 0.000000000000000000 ) ) ;
#23165=AXIS2_PLACEMENT_3D ( 'NONE', #40368, #39924, #13365 ) ;
#23173=DIRECTION ( 'NONE',  ( 0.000000000000000000, 0.000000000000000000, 1.000000000000000000 ) ) ;
#23183=CARTESIAN_POINT ( 'NONE',  ( -10.00000000000000000, 0.000000000000000000, 0.000000000000000000 ) ) ;
#23206=EDGE_CURVE ( 'NONE', #35006, #35211, #33821, .T. ) ;
#23213=ORIENTED_EDGE ( 'NONE', *, *, #27809, .T. ) ;
#23232=ORIENTED_EDGE ( 'NONE', *, *, #12405, .F. ) ;
#23236=VERTEX_POINT ( 'NONE', #23019 ) ;
#23258=EDGE_CURVE ( 'NONE', #16681, #14052, #19228, .T. ) ;
#23261=DIRECTION ( 'NONE',  ( -1.000000000000000000, 0.000000000000000000, 0.000000000000000000 ) ) ;
#23265=AXIS2_PLACEMENT_3D ( 'NONE', #17315, #14225, #27528 ) ;
#23294=DIRECTION ( 'NONE',  ( 0.000000000000000000, 0.9618256431728199329, -0.2736629900720799480 ) ) ;
#23295=DIRECTION ( 'NONE',  ( 1.000000000000000000, 0.000000000000000000, 0.000000000000000000 ) ) ;
#23305=ORIENTED_EDGE ( 'NONE', *, *, #23206, .F. ) ;
#23328=DIRECTION ( 'NONE',  ( 0.000000000000000000, 0.000000000000000000, 1.000000000000000000 ) ) ;
#23356=VERTEX_POINT ( 'NONE', #34300 ) ;
#23369=AXIS2_PLACEMENT_3D ( 'NONE', #36882, #33400, #15990 ) ;
#23378=VERTEX_POINT ( 'NONE', #27555 ) ;
#23383=DIRECTION ( 'NONE',  ( 0.000000000000000000, 0.000000000000000000, -1.000000000000000000 ) ) ;
#23384=ORIENTED_EDGE ( 'NONE', *, *, #37683, .T. ) ;
#23386=ORIENTED_EDGE ( 'NONE', *, *, #26445, .F. ) ;
#23390=EDGE_LOOP ( 'NONE', ( #1921, #28203, #21850, #28497 ) ) ;
#23402=LINE ( 'NONE', #36664, #25981 ) ;
#23405=AXIS2_PLACEMENT_3D ( 'NONE', #6554, #9635, #22983 ) ;
#23406=ORIENTED_EDGE ( 'NONE', *, *, #9929, .F. ) ;
#23429=ORIENTED_EDGE ( 'NONE', *, *, #737, .T. ) ;
#23438=DIRECTION ( 'NONE',  ( 0.000000000000000000, 0.000000000000000000, 1.000000000000000000 ) ) ;
#23443=VERTEX_POINT ( 'NONE', #37780 ) ;
#23444=CIRCLE ( 'NONE', #8094, 13.59999999999999787 ) ;
#23446=ORIENTED_EDGE ( 'NONE', *, *, #21608, .F. ) ;
#23457=ADVANCED_FACE ( 'NONE', ( #38219 ), #36380, .T. ) ;
#23458=AXIS2_PLACEMENT_3D ( 'NONE', #17506, #27513, #37952 ) ;
#23472=AXIS2_PLACEMENT_3D ( 'NONE', #33105, #2335, #5847 ) ;
#23480=CARTESIAN_POINT ( 'NONE',  ( 17.99999999999999645, 6.007673836298004666, 35.49518073029998533 ) ) ;
#23493=FACE_OUTER_BOUND ( 'NONE', #24635, .T. ) ;
#23499=DIRECTION ( 'NONE',  ( -1.000000000000000000, 0.000000000000000000, 0.000000000000000000 ) ) ;
#23502=DIRECTION ( 'NONE',  ( -1.000000000000000000, 0.000000000000000000, -0.000000000000000000 ) ) ;
#23532=CARTESIAN_POINT ( 'NONE',  ( 0.000000000000000000, 0.000000000000000000, 0.000000000000000000 ) ) ;
#23539=VERTEX_POINT ( 'NONE', #6285 ) ;
#23595=EDGE_CURVE ( 'NONE', #21901, #26484, #21361, .T. ) ;
#23612=DIRECTION ( 'NONE',  ( 0.000000000000000000, 0.000000000000000000, 1.000000000000000000 ) ) ;
#23614=FACE_OUTER_BOUND ( 'NONE', #27906, .T. ) ;
#23616=EDGE_CURVE ( 'NONE', #24001, #23236, #19251, .T. ) ;
#23627=LINE ( 'NONE', #652, #38733 ) ;
#23632=CARTESIAN_POINT ( 'NONE',  ( 17.99999999999999645, 31.11570115861502828, -4.898994019976315784 ) ) ;
#23648=CARTESIAN_POINT ( 'NONE',  ( 0.000000000000000000, 13.22719389142019608, -28.58720592780581882 ) ) ;
#23665=AXIS2_PLACEMENT_3D ( 'NONE', #30818, #18412, #14246 ) ;
#23676=EDGE_CURVE ( 'NONE', #28489, #637, #39412, .T. ) ;
#23687=DIRECTION ( 'NONE',  ( 0.000000000000000000, 0.000000000000000000, 1.000000000000000000 ) ) ;
#23694=EDGE_CURVE ( 'NONE', #36592, #33164, #42900, .T. ) ;
#23698=EDGE_CURVE ( 'NONE', #31287, #20730, #3844, .T. ) ;
#23705=VERTEX_POINT ( 'NONE', #13941 ) ;
#23712=DIRECTION ( 'NONE',  ( -1.000000000000000000, -0.000000000000000000, -0.000000000000000000 ) ) ;
#23715=CYLINDRICAL_SURFACE ( 'NONE', #12495, 13.60000000000000142 ) ;
#23719=VECTOR ( 'NONE', #1078, 1000.000000000000000 ) ;
#23723=ORIENTED_EDGE ( 'NONE', *, *, #42433, .T. ) ;
#23736=VERTEX_POINT ( 'NONE', #33987 ) ;
#23742=EDGE_LOOP ( 'NONE', ( #33436, #930, #23429, #36520 ) ) ;
#23756=CYLINDRICAL_SURFACE ( 'NONE', #21997, 31.49899999999999878 ) ;
#23757=CARTESIAN_POINT ( 'NONE',  ( 8.999999999999998224, 24.70533337038260413, -26.18485254986667243 ) ) ;
#23759=DIRECTION ( 'NONE',  ( -1.000000000000000000, -0.000000000000000000, 0.000000000000000000 ) ) ;
#23779=AXIS2_PLACEMENT_3D ( 'NONE', #20090, #10442, #16806 ) ;
#23790=ORIENTED_EDGE ( 'NONE', *, *, #26488, .T. ) ;
#23792=AXIS2_PLACEMENT_3D ( 'NONE', #16665, #19935, #10295 ) ;
#23801=AXIS2_PLACEMENT_3D ( 'NONE', #42406, #26065, #43047 ) ;
#23826=FACE_OUTER_BOUND ( 'NONE', #6306, .T. ) ;
#23844=CARTESIAN_POINT ( 'NONE',  ( 17.99999999999999645, 24.70533337038223110, 26.18485254986702060 ) ) ;
#23857=EDGE_CURVE ( 'NONE', #18138, #3911, #40847, .T. ) ;
#23868=VECTOR ( 'NONE', #2983, 1000.000000000000000 ) ;
#23876=ORIENTED_EDGE ( 'NONE', *, *, #40622, .F. ) ;
#23880=ORIENTED_EDGE ( 'NONE', *, *, #36111, .F. ) ;
#23895=CIRCLE ( 'NONE', #37804, 36.00000000000000000 ) ;
#23911=DIRECTION ( 'NONE',  ( 0.000000000000000000, 0.6736956436465584286, -0.7390089172206579793 ) ) ;
#23912=ORIENTED_EDGE ( 'NONE', *, *, #35388, .F. ) ;
#23919=CARTESIAN_POINT ( 'NONE',  ( 17.99999999999999645, 23.79363200506992015, -27.01597816121622486 ) ) ;
#23934=EDGE_CURVE ( 'NONE', #8291, #26427, #41546, .T. ) ;
#23935=ADVANCED_FACE ( 'NONE', ( #21807 ), #37677, .T. ) ;
#23956=CARTESIAN_POINT ( 'NONE',  ( 17.99999999999999645, -31.11570115861491814, -4.898994019976963266 ) ) ;
#23966=CIRCLE ( 'NONE', #6477, 31.49899999999999878 ) ;
#23971=VERTEX_POINT ( 'NONE', #2723 ) ;
#23972=DIRECTION ( 'NONE',  ( 0.000000000000000000, 0.9618256431728180456, 0.2736629900720866648 ) ) ;
#23975=CARTESIAN_POINT ( 'NONE',  ( 17.99999999999999645, 21.56073507908678977, -23.57770962728541875 ) ) ;
#23981=CIRCLE ( 'NONE', #9303, 13.59999999999999964 ) ;
#23989=EDGE_LOOP ( 'NONE', ( #26662, #20771, #38271, #11726 ) ) ;
#24001=VERTEX_POINT ( 'NONE', #41007 ) ;
#24012=EDGE_CURVE ( 'NONE', #22493, #41473, #26922, .T. ) ;
#24024=CIRCLE ( 'NONE', #41389, 31.49900000000000233 ) ;
#24027=LINE ( 'NONE', #21429, #8252 ) ;
#24032=CARTESIAN_POINT ( 'NONE',  ( -10.00000000000000000, 0.000000000000000000, 0.000000000000000000 ) ) ;
#24034=CARTESIAN_POINT ( 'NONE',  ( 17.99999999999999645, -35.78425302087541837, 3.935382540232670312 ) ) ;
#24050=DIRECTION ( 'NONE',  ( -1.000000000000000000, 0.000000000000000000, 0.000000000000000000 ) ) ;
#24060=DIRECTION ( 'NONE',  ( 0.000000000000000000, -0.8951632913550664483, 0.4457383557765300930 ) ) ;
#24109=FACE_OUTER_BOUND ( 'NONE', #594, .T. ) ;
#24111=EDGE_CURVE ( 'NONE', #606, #23443, #1079, .T. ) ;
#24116=CARTESIAN_POINT ( 'NONE',  ( 17.99999999999999645, 19.47322409167312429, -30.27859877001380084 ) ) ;
#24136=CARTESIAN_POINT ( 'NONE',  ( 0.000000000000000000, -21.56073507908629594, -23.57770962728587705 ) ) ;
#24142=CARTESIAN_POINT ( 'NONE',  ( 17.99999999999999645, 0.000000000000000000, 0.000000000000000000 ) ) ;
#24160=ORIENTED_EDGE ( 'NONE', *, *, #24667, .T. ) ;
#24175=CARTESIAN_POINT ( 'NONE',  ( 0.000000000000000000, -34.78944633786284868, 9.257128253673496232 ) ) ;
#24179=ORIENTED_EDGE ( 'NONE', *, *, #38884, .T. ) ;
#24184=CIRCLE ( 'NONE', #7419, 36.00000000000000000 ) ;
#24186=ORIENTED_EDGE ( 'NONE', *, *, #11057, .T. ) ;
#24191=CARTESIAN_POINT ( 'NONE',  ( 17.99999999999999645, 3.803237743091921974, 31.26855263151016828 ) ) ;
#24192=ADVANCED_FACE ( 'NONE', ( #5230 ), #35537, .T. ) ;
#24205=CIRCLE ( 'NONE', #42270, 13.59999999999999787 ) ;
#24213=ORIENTED_EDGE ( 'NONE', *, *, #21108, .T. ) ;
#24220=CARTESIAN_POINT ( 'NONE',  ( 0.000000000000000000, -32.49609705003694415, -15.49205204337308395 ) ) ;
#24223=DIRECTION ( 'NONE',  ( 1.000000000000000000, -0.000000000000000000, -0.000000000000000000 ) ) ;
#24259=VERTEX_POINT ( 'NONE', #8297 ) ;
#24260=VECTOR ( 'NONE', #17341, 1000.000000000000000 ) ;
#24269=EDGE_LOOP ( 'NONE', ( #33692, #8818, #8924, #21864 ) ) ;
#24289=VERTEX_POINT ( 'NONE', #3437 ) ;
#24290=DIRECTION ( 'NONE',  ( -1.000000000000000000, -0.000000000000000000, 0.000000000000000000 ) ) ;
#24293=VECTOR ( 'NONE', #19258, 1000.000000000000000 ) ;
#24317=ORIENTED_EDGE ( 'NONE', *, *, #28578, .T. ) ;
#24320=ADVANCED_FACE ( 'NONE', ( #23141 ), #39662, .T. ) ;
#24328=AXIS2_PLACEMENT_3D ( 'NONE', #1505, #11571, #24914 ) ;
#24339=EDGE_CURVE ( 'NONE', #34983, #17035, #18662, .T. ) ;
#24350=CARTESIAN_POINT ( 'NONE',  ( 17.99999999999999645, 21.48775762007893420, -23.64423737150114135 ) ) ;
#24355=CARTESIAN_POINT ( 'NONE',  ( 17.99999999999999645, 31.48608500567870294, 0.9019157472705636724 ) ) ;
#24358=ORIENTED_EDGE ( 'NONE', *, *, #16992, .F. ) ;
#24365=ORIENTED_EDGE ( 'NONE', *, *, #1409, .T. ) ;
#24376=DIRECTION ( 'NONE',  ( 1.000000000000000000, 0.000000000000000000, 0.000000000000000000 ) ) ;
#24377=DIRECTION ( 'NONE',  ( -1.000000000000000000, 0.000000000000000000, -0.000000000000000000 ) ) ;
#24385=ORIENTED_EDGE ( 'NONE', *, *, #29530, .F. ) ;
#24421=CARTESIAN_POINT ( 'NONE',  ( 17.99999999999999645, 0.000000000000000000, 0.000000000000000000 ) ) ;
#24442=CIRCLE ( 'NONE', #23779, 13.59999999999999787 ) ;
#24445=ORIENTED_EDGE ( 'NONE', *, *, #5272, .F. ) ;
#24447=AXIS2_PLACEMENT_3D ( 'NONE', #25791, #2608, #9612 ) ;
#24472=ORIENTED_EDGE ( 'NONE', *, *, #9218, .T. ) ;
#24477=VECTOR ( 'NONE', #19205, 1000.000000000000000 ) ;
#24483=DIRECTION ( 'NONE',  ( -1.000000000000000000, -0.000000000000000000, 0.000000000000000000 ) ) ;
#24492=EDGE_CURVE ( 'NONE', #17035, #34983, #26200, .T. ) ;
#24496=EDGE_CURVE ( 'NONE', #3911, #22441, #13763, .T. ) ;
#24502=DIRECTION ( 'NONE',  ( -1.000000000000000000, -0.000000000000000000, -0.000000000000000000 ) ) ;
#24538=CARTESIAN_POINT ( 'NONE',  ( 9.000000000000000000, -35.78425302087536863, -3.935382540233169912 ) ) ;
#24541=ORIENTED_EDGE ( 'NONE', *, *, #30213, .F. ) ;
#24553=ADVANCED_FACE ( 'NONE', ( #29579 ), #36519, .T. ) ;
#24562=EDGE_CURVE ( 'NONE', #21218, #15532, #30377, .T. ) ;
#24565=CARTESIAN_POINT ( 'NONE',  ( 0.000000000000000000, -13.22719389141998469, 28.58720592780591474 ) ) ;
#24573=AXIS2_PLACEMENT_3D ( 'NONE', #5294, #2008, #21714 ) ;
#24591=CARTESIAN_POINT ( 'NONE',  ( 17.99999999999999645, 0.000000000000000000, 0.000000000000000000 ) ) ;
#24596=EDGE_CURVE ( 'NONE', #38106, #30670, #30478, .T. ) ;
#24619=AXIS2_PLACEMENT_3D ( 'NONE', #8673, #34648, #38136 ) ;
#24624=CARTESIAN_POINT ( 'NONE',  ( 17.99999999999999645, -27.24480646643618442, 15.80846360676574669 ) ) ;
#24635=EDGE_LOOP ( 'NONE', ( #28576, #26057, #42523, #18904 ) ) ;
#24646=CARTESIAN_POINT ( 'NONE',  ( 17.99999999999999645, -31.94619804602776725, 16.59639811537345366 ) ) ;
#24647=LINE ( 'NONE', #7376, #19964 ) ;
#24657=EDGE_LOOP ( 'NONE', ( #11759, #6437, #4312, #6664 ) ) ;
#24667=EDGE_CURVE ( 'NONE', #21935, #27712, #26989, .T. ) ;
#24672=CIRCLE ( 'NONE', #27448, 31.49899999999999523 ) ;
#24676=VERTEX_POINT ( 'NONE', #14035 ) ;
#24687=DIRECTION ( 'NONE',  ( 0.000000000000000000, 0.000000000000000000, 1.000000000000000000 ) ) ;
#24697=DIRECTION ( 'NONE',  ( 0.000000000000000000, -0.7980172272802447120, 0.6026346363792492999 ) ) ;
#24713=ORIENTED_EDGE ( 'NONE', *, *, #34794, .F. ) ;
#24719=EDGE_CURVE ( 'NONE', #8862, #13944, #11577, .T. ) ;
#24729=CARTESIAN_POINT ( 'NONE',  ( 17.99999999999999645, 0.000000000000000000, 0.000000000000000000 ) ) ;
#24735=CYLINDRICAL_SURFACE ( 'NONE', #2593, 13.59999999999999787 ) ;
#24754=DIRECTION ( 'NONE',  ( -1.000000000000000000, 0.000000000000000000, 0.000000000000000000 ) ) ;
#24756=VERTEX_POINT ( 'NONE', #22552 ) ;
#24757=DIRECTION ( 'NONE',  ( -1.000000000000000000, 0.000000000000000000, 0.000000000000000000 ) ) ;
#24763=PLANE ( 'NONE',  #15187 ) ;
#24771=CARTESIAN_POINT ( 'NONE',  ( 0.000000000000000000, -30.74337109795225942, 8.695908345466005329 ) ) ;
#24779=ORIENTED_EDGE ( 'NONE', *, *, #16506, .T. ) ;
#24790=EDGE_CURVE ( 'NONE', #23539, #39668, #19280, .T. ) ;
#24793=ADVANCED_FACE ( 'NONE', ( #39277 ), #35592, .T. ) ;
#24796=VERTEX_POINT ( 'NONE', #5712 ) ;
#24800=CIRCLE ( 'NONE', #22025, 36.00000000000000000 ) ;
#24809=CARTESIAN_POINT ( 'NONE',  ( 0.000000000000000000, 11.49545354908979888, -29.80986809967247453 ) ) ;
#24812=LINE ( 'NONE', #11916, #5220 ) ;
#24818=CARTESIAN_POINT ( 'NONE',  ( 0.000000000000000000, -29.68570942776479527, 10.53307442156924267 ) ) ;
#24823=CARTESIAN_POINT ( 'NONE',  ( 0.000000000000000000, 25.52601536738592358, 19.21447964122706509 ) ) ;
#24827=AXIS2_PLACEMENT_3D ( 'NONE', #17135, #5076, #8782 ) ;
#24834=VECTOR ( 'NONE', #27226, 1000.000000000000000 ) ;
#24850=DIRECTION ( 'NONE',  ( -1.000000000000000000, -0.000000000000000000, -0.000000000000000000 ) ) ;
#24855=CARTESIAN_POINT ( 'NONE',  ( 17.99999999999999645, 0.000000000000000000, 0.000000000000000000 ) ) ;
#24856=EDGE_CURVE ( 'NONE', #24796, #35008, #14382, .T. ) ;
#24859=EDGE_LOOP ( 'NONE', ( #33654, #25552, #31720, #10980 ) ) ;
#24906=EDGE_LOOP ( 'NONE', ( #8415, #30621, #23232, #35329 ) ) ;
#24910=EDGE_CURVE ( 'NONE', #27725, #40723, #32484, .T. ) ;
#24914=DIRECTION ( 'NONE',  ( 0.000000000000000000, 0.8951632913550604531, 0.4457383557765420834 ) ) ;
#24918=DIRECTION ( 'NONE',  ( -1.000000000000000000, 0.000000000000000000, -0.000000000000000000 ) ) ;
#24919=ORIENTED_EDGE ( 'NONE', *, *, #13122, .T. ) ;
#24925=CYLINDRICAL_SURFACE ( 'NONE', #36240, 31.49899999999999878 ) ;
#24928=VECTOR ( 'NONE', #40288, 1000.000000000000000 ) ;
#24944=EDGE_CURVE ( 'NONE', #28703, #11424, #23627, .T. ) ;
#24947=CARTESIAN_POINT ( 'NONE',  ( 9.000000000000000000, 34.78944633786279184, 9.257128253673750251 ) ) ;
#24957=CYLINDRICAL_SURFACE ( 'NONE', #26168, 13.59999999999999964 ) ;
#24976=ADVANCED_FACE ( 'NONE', ( #7205 ), #37317, .T. ) ;
#24978=DIRECTION ( 'NONE',  ( -1.000000000000000000, 0.000000000000000000, 0.000000000000000000 ) ) ;
#24979=CIRCLE ( 'NONE', #41641, 13.60000000000000142 ) ;
#24994=CARTESIAN_POINT ( 'NONE',  ( 17.99999999999999645, -30.74337109795225942, 8.695908345466005329 ) ) ;
#24995=CYLINDRICAL_SURFACE ( 'NONE', #4768, 36.00000000000000000 ) ;
#24998=AXIS2_PLACEMENT_3D ( 'NONE', #190, #30985, #1073 ) ;
#24999=DIRECTION ( 'NONE',  ( 0.000000000000000000, 0.000000000000000000, -1.000000000000000000 ) ) ;
#25001=CARTESIAN_POINT ( 'NONE',  ( 0.000000000000000000, 0.000000000000000000, 0.000000000000000000 ) ) ;
#25004=DIRECTION ( 'NONE',  ( 0.000000000000000000, 0.000000000000000000, 1.000000000000000000 ) ) ;
#25006=VERTEX_POINT ( 'NONE', #20351 ) ;
#25007=EDGE_CURVE ( 'NONE', #41335, #42394, #11609, .T. ) ;
#25021=CARTESIAN_POINT ( 'NONE',  ( 0.000000000000000000, -28.57802095670097131, 14.28532136906662586 ) ) ;
#25041=CYLINDRICAL_SURFACE ( 'NONE', #35171, 13.60000000000000142 ) ;
#25045=DIRECTION ( 'NONE',  ( 0.000000000000000000, 0.000000000000000000, 1.000000000000000000 ) ) ;
#25065=DIRECTION ( 'NONE',  ( -1.000000000000000000, -0.000000000000000000, 0.000000000000000000 ) ) ;
#25070=VERTEX_POINT ( 'NONE', #15522 ) ;
#25073=CYLINDRICAL_SURFACE ( 'NONE', #13043, 31.49899999999999878 ) ;
#25074=DIRECTION ( 'NONE',  ( 0.000000000000000000, 0.000000000000000000, 1.000000000000000000 ) ) ;
#25090=CARTESIAN_POINT ( 'NONE',  ( 17.99999999999999645, -16.86122981692000167, -27.13802899033310112 ) ) ;
#25096=CARTESIAN_POINT ( 'NONE',  ( 0.000000000000000000, -29.68570942776464960, -10.53307442156965656 ) ) ;
#25099=ORIENTED_EDGE ( 'NONE', *, *, #23206, .T. ) ;
#25106=ADVANCED_FACE ( 'NONE', ( #12034 ), #22080, .T. ) ;
#25124=DIRECTION ( 'NONE',  ( -1.000000000000000000, 0.000000000000000000, 0.000000000000000000 ) ) ;
#25135=CIRCLE ( 'NONE', #5561, 13.59999999999999964 ) ;
#25152=FACE_OUTER_BOUND ( 'NONE', #4043, .T. ) ;
#25166=CARTESIAN_POINT ( 'NONE',  ( 17.99999999999999645, 31.80866420683990725, 2.997093558041416195 ) ) ;
#25171=DIRECTION ( 'NONE',  ( -1.000000000000000000, 0.000000000000000000, -0.000000000000000000 ) ) ;
#25187=DIRECTION ( 'NONE',  ( 0.000000000000000000, -0.9618256431728219313, 0.2736629900720728981 ) ) ;
#25206=DIRECTION ( 'NONE',  ( 0.000000000000000000, -0.1837495178165777232, 0.9829730996839003421 ) ) ;
#25212=VERTEX_POINT ( 'NONE', #16606 ) ;
#25217=CARTESIAN_POINT ( 'NONE',  ( 0.000000000000000000, 18.42432724429473012, 30.92804820216009176 ) ) ;
#25218=LINE ( 'NONE', #26042, #23003 ) ;
#25222=DIRECTION ( 'NONE',  ( 1.000000000000000000, 0.000000000000000000, 0.000000000000000000 ) ) ;
#25227=VECTOR ( 'NONE', #28102, 1000.000000000000000 ) ;
#25240=DIRECTION ( 'NONE',  ( -1.000000000000000000, -0.000000000000000000, 0.000000000000000000 ) ) ;
#25241=DIRECTION ( 'NONE',  ( -1.000000000000000000, 0.000000000000000000, -0.000000000000000000 ) ) ;
#25243=ORIENTED_EDGE ( 'NONE', *, *, #12106, .F. ) ;
#25247=ORIENTED_EDGE ( 'NONE', *, *, #6928, .T. ) ;
#25248=DIRECTION ( 'NONE',  ( 1.000000000000000000, -0.000000000000000000, -0.000000000000000000 ) ) ;
#25254=CARTESIAN_POINT ( 'NONE',  ( 0.000000000000000000, 0.000000000000000000, 0.000000000000000000 ) ) ;
#25265=CARTESIAN_POINT ( 'NONE',  ( 17.99999999999999645, 28.57802095670086828, 14.28532136906683370 ) ) ;
#25271=CARTESIAN_POINT ( 'NONE',  ( 17.99999999999999645, 29.03409033315581667, 12.21509719675401051 ) ) ;
#25272=LINE ( 'NONE', #1661, #13750 ) ;
#25274=LINE ( 'NONE', #8644, #17800 ) ;
#25284=DIRECTION ( 'NONE',  ( 0.000000000000000000, 0.3612416661871471479, 0.9324722294043580328 ) ) ;
#25301=CARTESIAN_POINT ( 'NONE',  ( 17.99999999999999645, 11.58753559615527529, -29.77419532459249751 ) ) ;
#25318=AXIS2_PLACEMENT_3D ( 'NONE', #8036, #18556, #4774 ) ;
#25324=DIRECTION ( 'NONE',  ( 0.000000000000000000, 0.000000000000000000, 1.000000000000000000 ) ) ;
#25338=AXIS2_PLACEMENT_3D ( 'NONE', #1860, #28298, #28076 ) ;
#25339=ORIENTED_EDGE ( 'NONE', *, *, #29962, .F. ) ;
#25342=DIRECTION ( 'NONE',  ( 1.000000000000000000, -0.000000000000000000, 0.000000000000000000 ) ) ;
#25344=DIRECTION ( 'NONE',  ( -1.000000000000000000, 0.000000000000000000, 0.000000000000000000 ) ) ;
#25345=CARTESIAN_POINT ( 'NONE',  ( 17.99999999999999645, -3.803237743092135581, 31.26855263151013276 ) ) ;
#25360=ORIENTED_EDGE ( 'NONE', *, *, #38687, .T. ) ;
#25386=ORIENTED_EDGE ( 'NONE', *, *, #19582, .F. ) ;
#25388=CIRCLE ( 'NONE', #30933, 31.49899999999999523 ) ;
#25389=DIRECTION ( 'NONE',  ( -1.000000000000000000, 0.000000000000000000, 0.000000000000000000 ) ) ;
#25392=CARTESIAN_POINT ( 'NONE',  ( 0.000000000000000000, -7.749090474611287860, -30.53094492177221397 ) ) ;
#25425=ORIENTED_EDGE ( 'NONE', *, *, #8884, .F. ) ;
#25429=EDGE_CURVE ( 'NONE', #2013, #3440, #34216, .T. ) ;
#25457=DIRECTION ( 'NONE',  ( -1.000000000000000000, -0.000000000000000000, -0.000000000000000000 ) ) ;
#25472=CARTESIAN_POINT ( 'NONE',  ( 17.99999999999999645, -9.484061862024134371, 30.03730300138978038 ) ) ;
#25477=DIRECTION ( 'NONE',  ( 0.000000000000000000, 0.000000000000000000, 1.000000000000000000 ) ) ;
#25487=AXIS2_PLACEMENT_3D ( 'NONE', #19102, #8590, #2449 ) ;
#25492=EDGE_CURVE ( 'NONE', #28980, #8515, #23895, .T. ) ;
#25496=DIRECTION ( 'NONE',  ( 1.000000000000000000, -0.000000000000000000, 0.000000000000000000 ) ) ;
#25503=DIRECTION ( 'NONE',  ( -1.000000000000000000, -0.000000000000000000, 0.000000000000000000 ) ) ;
#25509=CARTESIAN_POINT ( 'NONE',  ( 0.000000000000000000, 0.000000000000000000, 0.000000000000000000 ) ) ;
#25512=VECTOR ( 'NONE', #21795, 1000.000000000000000 ) ;
#25531=DIRECTION ( 'NONE',  ( -1.000000000000000000, 0.000000000000000000, 0.000000000000000000 ) ) ;
#25552=ORIENTED_EDGE ( 'NONE', *, *, #3259, .F. ) ;
#25571=DIRECTION ( 'NONE',  ( 1.000000000000000000, 0.000000000000000000, 0.000000000000000000 ) ) ;
#25577=EDGE_CURVE ( 'NONE', #15863, #39379, #14141, .T. ) ;
#25608=AXIS2_PLACEMENT_3D ( 'NONE', #40232, #36966, #526 ) ;
#25625=EDGE_CURVE ( 'NONE', #17206, #1617, #18336, .T. ) ;
#25632=AXIS2_PLACEMENT_3D ( 'NONE', #785, #8225, #20705 ) ;
#25635=VERTEX_POINT ( 'NONE', #41622 ) ;
#25648=CIRCLE ( 'NONE', #36739, 13.60000000000000142 ) ;
#25671=CARTESIAN_POINT ( 'NONE',  ( 17.99999999999999645, -24.70533337038204635, -26.18485254986720179 ) ) ;
#25675=APPLICATION_CONTEXT ( 'automotive_design' ) ;
#25686=DIRECTION ( 'NONE',  ( 0.000000000000000000, 0.8951632913550634507, -0.4457383557765359217 ) ) ;
#25699=VECTOR ( 'NONE', #16690, 1000.000000000000000 ) ;
#25703=FACE_OUTER_BOUND ( 'NONE', #23390, .T. ) ;
#25719=CARTESIAN_POINT ( 'NONE',  ( 17.99999999999999645, 35.78425302087538995, 3.935382540232922111 ) ) ;
#25744=ORIENTED_EDGE ( 'NONE', *, *, #26488, .F. ) ;
#25745=CARTESIAN_POINT ( 'NONE',  ( 17.99999999999999645, -28.62203781742993414, -14.19692359621484989 ) ) ;
#25767=CARTESIAN_POINT ( 'NONE',  ( 17.99999999999999645, 31.94619804602764290, 16.59639811537368814 ) ) ;
#25791=CARTESIAN_POINT ( 'NONE',  ( 17.99999999999999645, -11.58753559615464290, -29.77419532459275331 ) ) ;
#25801=FACE_OUTER_BOUND ( 'NONE', #6688, .T. ) ;
#25805=ORIENTED_EDGE ( 'NONE', *, *, #32834, .T. ) ;
#25808=EDGE_CURVE ( 'NONE', #4714, #39379, #22253, .T. ) ;
#25815=FACE_OUTER_BOUND ( 'NONE', #41317, .T. ) ;
#25834=EDGE_CURVE ( 'NONE', #27591, #9615, #12052, .T. ) ;
#25842=CARTESIAN_POINT ( 'NONE',  ( 17.99999999999999645, 30.78424799127077804, -6.672111855472861563 ) ) ;
#25846=EDGE_LOOP ( 'NONE', ( #42581, #4692, #35380, #31209 ) ) ;
#25847=DIRECTION ( 'NONE',  ( 0.000000000000000000, 0.000000000000000000, 1.000000000000000000 ) ) ;
#25849=VECTOR ( 'NONE', #8308, 1000.000000000000000 ) ;
#25865=LINE ( 'NONE', #26062, #11243 ) ;
#25868=CIRCLE ( 'NONE', #35566, 36.00000000000000000 ) ;
#25869=CARTESIAN_POINT ( 'NONE',  ( 0.000000000000000000, -27.24480646643618442, 15.80846360676574669 ) ) ;
#25871=ORIENTED_EDGE ( 'NONE', *, *, #8356, .F. ) ;
#25880=DIRECTION ( 'NONE',  ( -1.000000000000000000, 0.000000000000000000, -0.000000000000000000 ) ) ;
#25895=AXIS2_PLACEMENT_3D ( 'NONE', #13449, #29817, #10145 ) ;
#25896=DIRECTION ( 'NONE',  ( -1.000000000000000000, 0.000000000000000000, 0.000000000000000000 ) ) ;
#25899=ORIENTED_EDGE ( 'NONE', *, *, #31288, .F. ) ;
#25915=DIRECTION ( 'NONE',  ( -1.000000000000000000, -0.000000000000000000, -0.000000000000000000 ) ) ;
#25919=AXIS2_PLACEMENT_3D ( 'NONE', #8890, #28342, #1681 ) ;
#25924=DIRECTION ( 'NONE',  ( 1.000000000000000000, 0.000000000000000000, 0.000000000000000000 ) ) ;
#25926=EDGE_LOOP ( 'NONE', ( #9736, #39263, #3095, #27038 ) ) ;
#25936=EDGE_LOOP ( 'NONE', ( #41419, #153, #2541, #21631 ) ) ;
#25950=DIRECTION ( 'NONE',  ( 0.000000000000000000, 0.000000000000000000, 1.000000000000000000 ) ) ;
#25953=FACE_OUTER_BOUND ( 'NONE', #42876, .T. ) ;
#25963=DIRECTION ( 'NONE',  ( -1.000000000000000000, 0.000000000000000000, 0.000000000000000000 ) ) ;
#25977=CYLINDRICAL_SURFACE ( 'NONE', #6284, 31.49899999999999878 ) ;
#25981=VECTOR ( 'NONE', #7436, 1000.000000000000000 ) ;
#26001=CARTESIAN_POINT ( 'NONE',  ( 0.000000000000000000, 31.81777574834305966, -2.898764365605425830 ) ) ;
#26002=VERTEX_POINT ( 'NONE', #17632 ) ;
#26009=DIRECTION ( 'NONE',  ( -1.000000000000000000, 0.000000000000000000, 0.000000000000000000 ) ) ;
#26015=EDGE_CURVE ( 'NONE', #33247, #37148, #27394, .T. ) ;
#26016=CARTESIAN_POINT ( 'NONE',  ( 0.000000000000000000, 0.6168405712491942250, -35.99471499692226217 ) ) ;
#26017=CARTESIAN_POINT ( 'NONE',  ( 9.000000000000000000, -34.78944633786284868, 9.257128253673498008 ) ) ;
#26025=LINE ( 'NONE', #2219, #5135 ) ;
#26038=EDGE_CURVE ( 'NONE', #4027, #25070, #884, .T. ) ;
#26042=CARTESIAN_POINT ( 'NONE',  ( 8.999999999999998224, 18.42432724429518487, -30.92804820215982531 ) ) ;
#26047=CARTESIAN_POINT ( 'NONE',  ( 0.000000000000000000, 0.000000000000000000, 0.000000000000000000 ) ) ;
#26050=CIRCLE ( 'NONE', #23265, 13.60000000000000142 ) ;
#26053=CARTESIAN_POINT ( 'NONE',  ( 17.99999999999999645, -31.81777574834303124, -2.898764365605651427 ) ) ;
#26057=ORIENTED_EDGE ( 'NONE', *, *, #36159, .F. ) ;
#26062=CARTESIAN_POINT ( 'NONE',  ( 17.99999999999999645, 9.484061862023926537, 30.03730300138984433 ) ) ;
#26065=DIRECTION ( 'NONE',  ( -1.000000000000000000, 0.000000000000000000, 0.000000000000000000 ) ) ;
#26070=DIRECTION ( 'NONE',  ( -1.000000000000000000, 0.000000000000000000, -0.000000000000000000 ) ) ;
#26072=CARTESIAN_POINT ( 'NONE',  ( 0.000000000000000000, 0.000000000000000000, 0.000000000000000000 ) ) ;
#26073=ORIENTED_EDGE ( 'NONE', *, *, #7843, .T. ) ;
#26079=CIRCLE ( 'NONE', #2364, 36.00000000000000000 ) ;
#26090=DIRECTION ( 'NONE',  ( -1.000000000000000000, 0.000000000000000000, 0.000000000000000000 ) ) ;
#26123=DIRECTION ( 'NONE',  ( -1.000000000000000000, 0.000000000000000000, -0.000000000000000000 ) ) ;
#26130=CIRCLE ( 'NONE', #17082, 36.00000000000000000 ) ;
#26133=DIRECTION ( 'NONE',  ( -1.000000000000000000, 0.000000000000000000, -0.000000000000000000 ) ) ;
#26154=VERTEX_POINT ( 'NONE', #14992 ) ;
#26162=DIRECTION ( 'NONE',  ( 0.000000000000000000, 0.000000000000000000, 1.000000000000000000 ) ) ;
#26164=AXIS2_PLACEMENT_3D ( 'NONE', #18279, #4704, #5352 ) ;
#26168=AXIS2_PLACEMENT_3D ( 'NONE', #25166, #38208, #21889 ) ;
#26178=VERTEX_POINT ( 'NONE', #38500 ) ;
#26188=LINE ( 'NONE', #35750, #28974 ) ;
#26197=CARTESIAN_POINT ( 'NONE',  ( 17.99999999999999645, -5.919241748379376666, -31.39643714728462953 ) ) ;
#26200=CIRCLE ( 'NONE', #21358, 15.00000000000000000 ) ;
#26203=EDGE_CURVE ( 'NONE', #6169, #3495, #29474, .T. ) ;
#26211=CARTESIAN_POINT ( 'NONE',  ( 0.000000000000000000, 26.29521155129873122, -17.34211205339320117 ) ) ;
#26214=DIRECTION ( 'NONE',  ( 1.000000000000000000, 0.000000000000000000, 0.000000000000000000 ) ) ;
#26220=CARTESIAN_POINT ( 'NONE',  ( 17.99999999999999645, 18.25486108452625089, 25.66996392254279868 ) ) ;
#26223=CYLINDRICAL_SURFACE ( 'NONE', #23405, 13.59999999999999964 ) ;
#26226=DIRECTION ( 'NONE',  ( -1.000000000000000000, -0.000000000000000000, 0.000000000000000000 ) ) ;
#26229=CARTESIAN_POINT ( 'NONE',  ( 17.99999999999999645, 31.81777574834305966, -2.898764365605425830 ) ) ;
#26233=CARTESIAN_POINT ( 'NONE',  ( 17.99999999999999645, -3.803237743091689715, -31.26855263151018960 ) ) ;
#26234=AXIS2_PLACEMENT_3D ( 'NONE', #7174, #20531, #30552 ) ;
#26245=CARTESIAN_POINT ( 'NONE',  ( 8.999999999999998224, 12.42760411676038146, 33.78690065568429191 ) ) ;
#26250=ORIENTED_EDGE ( 'NONE', *, *, #33819, .T. ) ;
#26257=CIRCLE ( 'NONE', #10234, 13.59999999999999964 ) ;
#26262=ORIENTED_EDGE ( 'NONE', *, *, #42821, .T. ) ;
#26267=CIRCLE ( 'NONE', #26950, 13.60000000000000320 ) ;
#26268=DIRECTION ( 'NONE',  ( -1.000000000000000000, 0.000000000000000000, -0.000000000000000000 ) ) ;
#26271=FACE_OUTER_BOUND ( 'NONE', #20868, .T. ) ;
#26279=ORIENTED_EDGE ( 'NONE', *, *, #8496, .F. ) ;
#26310=ORIENTED_EDGE ( 'NONE', *, *, #11365, .T. ) ;
#26312=FACE_OUTER_BOUND ( 'NONE', #34829, .T. ) ;
#26315=DIRECTION ( 'NONE',  ( 0.000000000000000000, 0.000000000000000000, 1.000000000000000000 ) ) ;
#26322=EDGE_CURVE ( 'NONE', #32556, #10881, #35231, .T. ) ;
#26323=CIRCLE ( 'NONE', #6797, 13.59999999999999964 ) ;
#26324=CARTESIAN_POINT ( 'NONE',  ( 0.000000000000000000, -24.70533337038242294, 26.18485254986683586 ) ) ;
#26327=CARTESIAN_POINT ( 'NONE',  ( 9.000000000000000000, 34.45183346761150034, -10.44371441202619621 ) ) ;
#26328=DIRECTION ( 'NONE',  ( 0.000000000000000000, 0.000000000000000000, 1.000000000000000000 ) ) ;
#26332=ORIENTED_EDGE ( 'NONE', *, *, #29641, .T. ) ;
#26349=EDGE_CURVE ( 'NONE', #7683, #25070, #40616, .T. ) ;
#26351=ORIENTED_EDGE ( 'NONE', *, *, #6640, .T. ) ;
#26370=ORIENTED_EDGE ( 'NONE', *, *, #23676, .F. ) ;
#26374=EDGE_CURVE ( 'NONE', #1401, #51, #15596, .T. ) ;
#26394=DIRECTION ( 'NONE',  ( 0.000000000000000000, 0.000000000000000000, -1.000000000000000000 ) ) ;
#26399=EDGE_LOOP ( 'NONE', ( #22820, #19444, #36476, #30658 ) ) ;
#26405=VERTEX_POINT ( 'NONE', #7656 ) ;
#26407=DIRECTION ( 'NONE',  ( 0.000000000000000000, -0.8951632913550570114, -0.4457383557765488558 ) ) ;
#26418=DIRECTION ( 'NONE',  ( 0.000000000000000000, 0.5264321628773570572, -0.8502171357296134380 ) ) ;
#26425=DIRECTION ( 'NONE',  ( 0.000000000000000000, -0.5264321628773450668, -0.8502171357296208765 ) ) ;
#26427=VERTEX_POINT ( 'NONE', #27107 ) ;
#26434=DIRECTION ( 'NONE',  ( -1.000000000000000000, 0.000000000000000000, 0.000000000000000000 ) ) ;
#26445=EDGE_CURVE ( 'NONE', #24259, #24001, #12991, .T. ) ;
#26451=EDGE_LOOP ( 'NONE', ( #27968, #39908 ) ) ;
#26460=VERTEX_POINT ( 'NONE', #6412 ) ;
#26479=CYLINDRICAL_SURFACE ( 'NONE', #8941, 36.00000000000000000 ) ;
#26480=ORIENTED_EDGE ( 'NONE', *, *, #8495, .T. ) ;
#26484=VERTEX_POINT ( 'NONE', #23844 ) ;
#26488=EDGE_CURVE ( 'NONE', #17450, #11761, #26050, .T. ) ;
#26490=DIRECTION ( 'NONE',  ( -1.000000000000000000, 0.000000000000000000, 0.000000000000000000 ) ) ;
#26523=CARTESIAN_POINT ( 'NONE',  ( 17.99999999999999645, 24.70533337038261124, -26.18485254986667954 ) ) ;
#26529=DIRECTION ( 'NONE',  ( -1.000000000000000000, -0.000000000000000000, 0.000000000000000000 ) ) ;
#26532=CYLINDRICAL_SURFACE ( 'NONE', #36801, 36.00000000000000000 ) ;
#26535=EDGE_LOOP ( 'NONE', ( #15983, #17510, #16530, #33986 ) ) ;
#26543=CARTESIAN_POINT ( 'NONE',  ( 17.99999999999999645, 0.000000000000000000, 0.000000000000000000 ) ) ;
#26550=VERTEX_POINT ( 'NONE', #8520 ) ;
#26558=EDGE_CURVE ( 'NONE', #17666, #14830, #5104, .T. ) ;
#26562=VECTOR ( 'NONE', #35474, 1000.000000000000000 ) ;
#26564=ORIENTED_EDGE ( 'NONE', *, *, #34873, .T. ) ;
#26578=EDGE_CURVE ( 'NONE', #13372, #5751, #42702, .T. ) ;
#26581=LINE ( 'NONE', #23757, #10230 ) ;
#26594=CIRCLE ( 'NONE', #37007, 36.00000000000000000 ) ;
#26595=ORIENTED_EDGE ( 'NONE', *, *, #42187, .T. ) ;
#26622=AXIS2_PLACEMENT_3D ( 'NONE', #28457, #4864, #37799 ) ;
#26633=ORIENTED_EDGE ( 'NONE', *, *, #15778, .F. ) ;
#26654=VERTEX_POINT ( 'NONE', #22951 ) ;
#26662=ORIENTED_EDGE ( 'NONE', *, *, #39347, .T. ) ;
#26666=CARTESIAN_POINT ( 'NONE',  ( 17.99999999999999645, 0.000000000000000000, 0.000000000000000000 ) ) ;
#26674=VERTEX_POINT ( 'NONE', #36195 ) ;
#26680=DIRECTION ( 'NONE',  ( -1.000000000000000000, 0.000000000000000000, 0.000000000000000000 ) ) ;
#26685=DIRECTION ( 'NONE',  ( 0.000000000000000000, -0.5264321628773627193, 0.8502171357296098853 ) ) ;
#26696=ORIENTED_EDGE ( 'NONE', *, *, #8443, .T. ) ;
#26698=ORIENTED_EDGE ( 'NONE', *, *, #8884, .T. ) ;
#26704=FACE_OUTER_BOUND ( 'NONE', #7363, .T. ) ;
#26708=CARTESIAN_POINT ( 'NONE',  ( 0.000000000000000000, 29.03409033315581667, 12.21509719675401051 ) ) ;
#26719=ORIENTED_EDGE ( 'NONE', *, *, #34716, .T. ) ;
#26727=AXIS2_PLACEMENT_3D ( 'NONE', #5033, #25571, #15529 ) ;
#26731=AXIS2_PLACEMENT_3D ( 'NONE', #19249, #32302, #26418 ) ;
#26732=ORIENTED_EDGE ( 'NONE', *, *, #30580, .T. ) ;
#26742=DIRECTION ( 'NONE',  ( -1.000000000000000000, -0.000000000000000000, -0.000000000000000000 ) ) ;
#26772=EDGE_LOOP ( 'NONE', ( #1996, #22233, #37403, #35527 ) ) ;
#26790=ORIENTED_EDGE ( 'NONE', *, *, #26322, .F. ) ;
#26795=CIRCLE ( 'NONE', #14990, 31.49900000000000588 ) ;
#26801=FACE_OUTER_BOUND ( 'NONE', #30892, .T. ) ;
#26807=EDGE_LOOP ( 'NONE', ( #16815, #18289, #660, #12455 ) ) ;
#26826=CARTESIAN_POINT ( 'NONE',  ( 17.99999999999999645, -21.56073507908629594, -23.57770962728587705 ) ) ;
#26844=ORIENTED_EDGE ( 'NONE', *, *, #26015, .T. ) ;
#26849=ORIENTED_EDGE ( 'NONE', *, *, #30962, .T. ) ;
#26852=FACE_OUTER_BOUND ( 'NONE', #2377, .T. ) ;
#26855=DIRECTION ( 'NONE',  ( 0.000000000000000000, 0.000000000000000000, 1.000000000000000000 ) ) ;
#26871=VECTOR ( 'NONE', #3595, 1000.000000000000000 ) ;
#26873=CYLINDRICAL_SURFACE ( 'NONE', #39333, 31.49899999999999878 ) ;
#26877=DIRECTION ( 'NONE',  ( -1.000000000000000000, 0.000000000000000000, 0.000000000000000000 ) ) ;
#26885=AXIS2_PLACEMENT_3D ( 'NONE', #3394, #6046, #30052 ) ;
#26890=CARTESIAN_POINT ( 'NONE',  ( 17.99999999999999645, 29.68570942776472066, 10.53307442156944873 ) ) ;
#26901=FACE_OUTER_BOUND ( 'NONE', #37245, .T. ) ;
#26903=VECTOR ( 'NONE', #35647, 1000.000000000000000 ) ;
#26913=STYLED_ITEM ( 'NONE', ( #13872 ), #13741 ) ;
#26919=AXIS2_PLACEMENT_3D ( 'NONE', #27097, #30587, #6994 ) ;
#26921=CARTESIAN_POINT ( 'NONE',  ( 8.999999999999998224, -24.70533337038242294, 26.18485254986683586 ) ) ;
#26922=CIRCLE ( 'NONE', #23458, 13.59999999999999964 ) ;
#26925=LINE ( 'NONE', #40205, #17569 ) ;
#26934=DIRECTION ( 'NONE',  ( 0.000000000000000000, -0.9957341762950334685, -0.09226835946331299332 ) ) ;
#26950=AXIS2_PLACEMENT_3D ( 'NONE', #31357, #42005, #18516 ) ;
#26955=EDGE_LOOP ( 'NONE', ( #33059, #33977, #14996, #41086 ) ) ;
#26956=CYLINDRICAL_SURFACE ( 'NONE', #25608, 36.00000000000000000 ) ;
#26958=CIRCLE ( 'NONE', #27660, 13.60000000000000320 ) ;
#26962=EDGE_CURVE ( 'NONE', #13115, #19749, #25388, .T. ) ;
#26976=ORIENTED_EDGE ( 'NONE', *, *, #34246, .F. ) ;
#26978=DIRECTION ( 'NONE',  ( 1.000000000000000000, 0.000000000000000000, 0.000000000000000000 ) ) ;
#26989=CIRCLE ( 'NONE', #34631, 31.49899999999999523 ) ;
#26997=EDGE_CURVE ( 'NONE', #3495, #16072, #3762, .T. ) ;
#27016=CIRCLE ( 'NONE', #22154, 13.59999999999999964 ) ;
#27024=DIRECTION ( 'NONE',  ( -1.000000000000000000, 0.000000000000000000, -0.000000000000000000 ) ) ;
#27025=EDGE_CURVE ( 'NONE', #39668, #18842, #1917, .T. ) ;
#27038=ORIENTED_EDGE ( 'NONE', *, *, #3995, .T. ) ;
#27052=DIRECTION ( 'NONE',  ( 0.000000000000000000, 0.000000000000000000, 1.000000000000000000 ) ) ;
#27070=DIRECTION ( 'NONE',  ( -1.000000000000000000, -0.000000000000000000, 0.000000000000000000 ) ) ;
#27082=ORIENTED_EDGE ( 'NONE', *, *, #21108, .F. ) ;
#27095=DIRECTION ( 'NONE',  ( 0.000000000000000000, 0.000000000000000000, -1.000000000000000000 ) ) ;
#27097=CARTESIAN_POINT ( 'NONE',  ( 0.000000000000000000, 5.919241748380035695, -31.39643714728450163 ) ) ;
#27098=AXIS2_PLACEMENT_3D ( 'NONE', #8290, #9515, #29824 ) ;
#27107=CARTESIAN_POINT ( 'NONE',  ( 17.99999999999999645, -35.89808275599447285, 2.706964063997103764 ) ) ;
#27110=FACE_OUTER_BOUND ( 'NONE', #20891, .T. ) ;
#27114=CIRCLE ( 'NONE', #36983, 31.49900000000000233 ) ;
#27118=EDGE_LOOP ( 'NONE', ( #14384, #39228, #38479, #30059 ) ) ;
#27145=VERTEX_POINT ( 'NONE', #43119 ) ;
#27151=DIRECTION ( 'NONE',  ( -1.000000000000000000, 0.000000000000000000, 0.000000000000000000 ) ) ;
#27154=ORIENTED_EDGE ( 'NONE', *, *, #32054, .F. ) ;
#27158=CARTESIAN_POINT ( 'NONE',  ( 9.000000000000000000, -13.57797752207901532, -33.34124362422488730 ) ) ;
#27166=CARTESIAN_POINT ( 'NONE',  ( 0.000000000000000000, 28.35267316522783432, 22.18391138608718549 ) ) ;
#27168=SURFACE_SIDE_STYLE ('',( #40642 ) ) ;
#27176=DIRECTION ( 'NONE',  ( 0.000000000000000000, 0.000000000000000000, 1.000000000000000000 ) ) ;
#27179=CYLINDRICAL_SURFACE ( 'NONE', #39342, 31.49899999999999878 ) ;
#27210=EDGE_CURVE ( 'NONE', #16104, #10372, #5199, .T. ) ;
#27226=DIRECTION ( 'NONE',  ( 1.000000000000000000, 0.000000000000000000, -0.000000000000000000 ) ) ;
#27230=DIRECTION ( 'NONE',  ( -1.000000000000000000, 0.000000000000000000, 0.000000000000000000 ) ) ;
#27235=VECTOR ( 'NONE', #20106, 1000.000000000000000 ) ;
#27243=DIRECTION ( 'NONE',  ( 0.000000000000000000, 0.000000000000000000, 1.000000000000000000 ) ) ;
#27252=ORIENTED_EDGE ( 'NONE', *, *, #35697, .F. ) ;
#27261=VECTOR ( 'NONE', #216, 1000.000000000000000 ) ;
#27267=ORIENTED_EDGE ( 'NONE', *, *, #32091, .T. ) ;
#27278=CYLINDRICAL_SURFACE ( 'NONE', #2986, 13.60000000000000142 ) ;
#27287=CARTESIAN_POINT ( 'NONE',  ( 17.99999999999999645, 31.80866420683990725, 2.997093558041416195 ) ) ;
#27291=ORIENTED_EDGE ( 'NONE', *, *, #16011, .T. ) ;
#27295=CYLINDRICAL_SURFACE ( 'NONE', #39690, 13.59999999999999787 ) ;
#27310=ORIENTED_EDGE ( 'NONE', *, *, #21907, .T. ) ;
#27324=ORIENTED_EDGE ( 'NONE', *, *, #9647, .T. ) ;
#27326=CARTESIAN_POINT ( 'NONE',  ( 17.99999999999999645, 0.000000000000000000, 0.000000000000000000 ) ) ;
#27330=ORIENTED_EDGE ( 'NONE', *, *, #39410, .F. ) ;
#27333=DIRECTION ( 'NONE',  ( -1.000000000000000000, -0.000000000000000000, -0.000000000000000000 ) ) ;
#27337=VERTEX_POINT ( 'NONE', #24175 ) ;
#27342=CYLINDRICAL_SURFACE ( 'NONE', #11044, 31.49899999999999878 ) ;
#27368=EDGE_CURVE ( 'NONE', #12013, #11159, #38605, .T. ) ;
#27376=CARTESIAN_POINT ( 'NONE',  ( 17.99999999999999645, 5.822172717930266472, 31.41458249383143198 ) ) ;
#27379=FILL_AREA_STYLE ('',( #10573 ) ) ;
#27394=CIRCLE ( 'NONE', #25338, 36.00000000000000000 ) ;
#27405=CIRCLE ( 'NONE', #31577, 31.49900000000000233 ) ;
#27418=ORIENTED_EDGE ( 'NONE', *, *, #13528, .F. ) ;
#27443=AXIS2_PLACEMENT_3D ( 'NONE', #35633, #39317, #3316 ) ;
#27448=AXIS2_PLACEMENT_3D ( 'NONE', #929, #41514, #8365 ) ;
#27464=LINE ( 'NONE', #20739, #6708 ) ;
#27474=AXIS2_PLACEMENT_3D ( 'NONE', #32066, #31861, #41872 ) ;
#27479=VECTOR ( 'NONE', #27601, 1000.000000000000000 ) ;
#27486=DIRECTION ( 'NONE',  ( -1.000000000000000000, -0.000000000000000000, 0.000000000000000000 ) ) ;
#27491=VERTEX_POINT ( 'NONE', #31129 ) ;
#27499=ORIENTED_EDGE ( 'NONE', *, *, #3259, .T. ) ;
#27503=EDGE_LOOP ( 'NONE', ( #40095, #3919, #10502, #25360 ) ) ;
#27505=ORIENTED_EDGE ( 'NONE', *, *, #32960, .T. ) ;
#27507=VECTOR ( 'NONE', #42711, 1000.000000000000000 ) ;
#27513=DIRECTION ( 'NONE',  ( -1.000000000000000000, -0.000000000000000000, 0.000000000000000000 ) ) ;
#27517=LINE ( 'NONE', #30996, #33120 ) ;
#27520=CIRCLE ( 'NONE', #22007, 36.00000000000000000 ) ;
#27522=CARTESIAN_POINT ( 'NONE',  ( 17.99999999999999645, 0.000000000000000000, 0.000000000000000000 ) ) ;
#27527=AXIS2_PLACEMENT_3D ( 'NONE', #24771, #41512, #25206 ) ;
#27528=DIRECTION ( 'NONE',  ( 0.000000000000000000, -0.8951632913550663373, 0.4457383557765300375 ) ) ;
#27536=VECTOR ( 'NONE', #430, 1000.000000000000000 ) ;
#27553=EDGE_LOOP ( 'NONE', ( #4152, #15764, #18293, #12756 ) ) ;
#27555=CARTESIAN_POINT ( 'NONE',  ( 17.99999999999999645, -23.79363200506973186, 27.01597816121639184 ) ) ;
#27567=EDGE_CURVE ( 'NONE', #34450, #14228, #11725, .T. ) ;
#27574=ORIENTED_EDGE ( 'NONE', *, *, #15494, .T. ) ;
#27578=DIRECTION ( 'NONE',  ( 0.000000000000000000, 0.6736956436465584286, -0.7390089172206580903 ) ) ;
#27583=EDGE_CURVE ( 'NONE', #3911, #33690, #14339, .T. ) ;
#27587=DIRECTION ( 'NONE',  ( 1.000000000000000000, 0.000000000000000000, -0.000000000000000000 ) ) ;
#27591=VERTEX_POINT ( 'NONE', #14782 ) ;
#27594=ORIENTED_EDGE ( 'NONE', *, *, #326, .F. ) ;
#27601=DIRECTION ( 'NONE',  ( -1.000000000000000000, 0.000000000000000000, 0.000000000000000000 ) ) ;
#27609=MECHANICAL_DESIGN_GEOMETRIC_PRESENTATION_REPRESENTATION('',(#26913),#5290);
#27615=ORIENTED_EDGE ( 'NONE', *, *, #36349, .T. ) ;
#27622=CARTESIAN_POINT ( 'NONE',  ( 17.99999999999999645, 0.000000000000000000, 0.000000000000000000 ) ) ;
#27623=ORIENTED_EDGE ( 'NONE', *, *, #15076, .T. ) ;
#27629=DIRECTION ( 'NONE',  ( 0.000000000000000000, 0.9957341762950341346, 0.09226835946330559646 ) ) ;
#27630=VERTEX_POINT ( 'NONE', #9709 ) ;
#27635=CIRCLE ( 'NONE', #3917, 31.49900000000000588 ) ;
#27640=ORIENTED_EDGE ( 'NONE', *, *, #39627, .F. ) ;
#27647=DIRECTION ( 'NONE',  ( 1.000000000000000000, 0.000000000000000000, 0.000000000000000000 ) ) ;
#27650=AXIS2_PLACEMENT_3D ( 'NONE', #8444, #1015, #1671 ) ;
#27660=AXIS2_PLACEMENT_3D ( 'NONE', #32821, #23050, #22620 ) ;
#27663=ORIENTED_EDGE ( 'NONE', *, *, #42527, .T. ) ;
#27676=LINE ( 'NONE', #10644, #6175 ) ;
#27681=DIRECTION ( 'NONE',  ( 0.000000000000000000, 0.000000000000000000, 1.000000000000000000 ) ) ;
#27699=CARTESIAN_POINT ( 'NONE',  ( 17.99999999999999645, 3.803237743092368284, -31.26855263151010789 ) ) ;
#27702=ORIENTED_EDGE ( 'NONE', *, *, #7199, .T. ) ;
#27704=CARTESIAN_POINT ( 'NONE',  ( 17.99999999999999645, -13.22719389141960100, -28.58720592780609593 ) ) ;
#27707=CIRCLE ( 'NONE', #18681, 13.59999999999999964 ) ;
#27712=VERTEX_POINT ( 'NONE', #42202 ) ;
#27718=AXIS2_PLACEMENT_3D ( 'NONE', #15365, #11869, #5295 ) ;
#27723=DIRECTION ( 'NONE',  ( 0.000000000000000000, 0.000000000000000000, 1.000000000000000000 ) ) ;
#27725=VERTEX_POINT ( 'NONE', #12363 ) ;
#27742=CYLINDRICAL_SURFACE ( 'NONE', #31608, 13.59999999999999964 ) ;
#27743=ORIENTED_EDGE ( 'NONE', *, *, #22623, .T. ) ;
#27745=DIRECTION ( 'NONE',  ( 0.000000000000000000, -0.1837495178165775012, 0.9829730996839004531 ) ) ;
#27750=CARTESIAN_POINT ( 'NONE',  ( 0.000000000000000000, -23.79363200506972476, 27.01597816121638829 ) ) ;
#27758=ORIENTED_EDGE ( 'NONE', *, *, #20083, .F. ) ;
#27763=DIRECTION ( 'NONE',  ( 0.000000000000000000, 0.000000000000000000, 1.000000000000000000 ) ) ;
#27768=CARTESIAN_POINT ( 'NONE',  ( -10.00000000000000000, 0.000000000000000000, 0.000000000000000000 ) ) ;
#27784=CARTESIAN_POINT ( 'NONE',  ( 17.99999999999999645, 28.62203781743003717, 14.19692359621465094 ) ) ;
#27799=CIRCLE ( 'NONE', #4787, 13.59999999999999787 ) ;
#27803=CIRCLE ( 'NONE', #29886, 13.59999999999999964 ) ;
#27809=EDGE_CURVE ( 'NONE', #6403, #31369, #42145, .T. ) ;
#27814=VERTEX_POINT ( 'NONE', #27166 ) ;
#27819=VERTEX_POINT ( 'NONE', #17371 ) ;
#27821=ADVANCED_FACE ( 'NONE', ( #720 ), #14079, .T. ) ;
#27823=ORIENTED_EDGE ( 'NONE', *, *, #6025, .T. ) ;
#27825=DIRECTION ( 'NONE',  ( -1.000000000000000000, -0.000000000000000000, 0.000000000000000000 ) ) ;
#27845=VERTEX_POINT ( 'NONE', #16931 ) ;
#27850=CARTESIAN_POINT ( 'NONE',  ( 17.99999999999999645, 30.71634675606066267, -8.790889055186230649 ) ) ;
#27860=VERTEX_POINT ( 'NONE', #6631 ) ;
#27861=AXIS2_PLACEMENT_3D ( 'NONE', #5897, #33593, #16846 ) ;
#27880=DIRECTION ( 'NONE',  ( -1.000000000000000000, 0.000000000000000000, 0.000000000000000000 ) ) ;
#27887=CARTESIAN_POINT ( 'NONE',  ( -10.00000000000000000, 0.000000000000000000, 0.000000000000000000 ) ) ;
#27896=DIRECTION ( 'NONE',  ( 0.000000000000000000, 0.000000000000000000, 1.000000000000000000 ) ) ;
#27906=EDGE_LOOP ( 'NONE', ( #20116, #41493, #2214, #22579 ) ) ;
#27915=DIRECTION ( 'NONE',  ( 0.000000000000000000, 0.000000000000000000, -1.000000000000000000 ) ) ;
#27922=AXIS2_PLACEMENT_3D ( 'NONE', #11153, #24483, #20788 ) ;
#27937=CYLINDRICAL_SURFACE ( 'NONE', #13694, 13.60000000000000142 ) ;
#27938=VECTOR ( 'NONE', #30317, 1000.000000000000000 ) ;
#27949=ORIENTED_EDGE ( 'NONE', *, *, #13641, .F. ) ;
#27959=ORIENTED_EDGE ( 'NONE', *, *, #19066, .F. ) ;
#27964=CARTESIAN_POINT ( 'NONE',  ( 17.99999999999999645, 29.03409033315599075, -12.21509719675360373 ) ) ;
#27966=DIRECTION ( 'NONE',  ( -1.000000000000000000, 0.000000000000000000, 0.000000000000000000 ) ) ;
#27967=DIRECTION ( 'NONE',  ( -1.000000000000000000, 0.000000000000000000, 0.000000000000000000 ) ) ;
#27968=ORIENTED_EDGE ( 'NONE', *, *, #10204, .F. ) ;
#27981=CARTESIAN_POINT ( 'NONE',  ( 0.000000000000000000, 0.000000000000000000, 0.000000000000000000 ) ) ;
#27986=DIRECTION ( 'NONE',  ( -1.000000000000000000, 0.000000000000000000, 0.000000000000000000 ) ) ;
#27997=ORIENTED_EDGE ( 'NONE', *, *, #37930, .T. ) ;
#28021=CARTESIAN_POINT ( 'NONE',  ( 17.99999999999999645, -9.484061862023704492, -30.03730300138991538 ) ) ;
#28024=ORIENTED_EDGE ( 'NONE', *, *, #33563, .F. ) ;
#28037=CIRCLE ( 'NONE', #19664, 31.49899999999999878 ) ;
#28063=CARTESIAN_POINT ( 'NONE',  ( 17.99999999999999645, -7.220349212960190499, -35.26849241522671718 ) ) ;
#28072=ORIENTED_EDGE ( 'NONE', *, *, #17600, .F. ) ;
#28076=DIRECTION ( 'NONE',  ( 0.000000000000000000, 0.000000000000000000, 1.000000000000000000 ) ) ;
#28101=ORIENTED_EDGE ( 'NONE', *, *, #42207, .F. ) ;
#28102=DIRECTION ( 'NONE',  ( -1.000000000000000000, -0.000000000000000000, 0.000000000000000000 ) ) ;
#28110=LINE ( 'NONE', #41375, #40794 ) ;
#28111=ORIENTED_EDGE ( 'NONE', *, *, #20, .F. ) ;
#28112=DIRECTION ( 'NONE',  ( 1.000000000000000000, 0.000000000000000000, 0.000000000000000000 ) ) ;
#28119=DIRECTION ( 'NONE',  ( 0.000000000000000000, -0.5264321628773449557, -0.8502171357296209875 ) ) ;
#28130=FACE_OUTER_BOUND ( 'NONE', #42198, .T. ) ;
#28140=EDGE_LOOP ( 'NONE', ( #17213, #32808, #37832, #9350 ) ) ;
#28146=CARTESIAN_POINT ( 'NONE',  ( 9.000000000000000000, -6.007673836298252468, 35.49518073029994980 ) ) ;
#28150=CIRCLE ( 'NONE', #26731, 31.49899999999999523 ) ;
#28160=ORIENTED_EDGE ( 'NONE', *, *, #15251, .T. ) ;
#28173=CARTESIAN_POINT ( 'NONE',  ( 17.99999999999999645, 0.000000000000000000, 0.000000000000000000 ) ) ;
#28203=ORIENTED_EDGE ( 'NONE', *, *, #14629, .T. ) ;
#28215=DIRECTION ( 'NONE',  ( 0.000000000000000000, 0.000000000000000000, 1.000000000000000000 ) ) ;
#28219=LINE ( 'NONE', #41486, #4166 ) ;
#28224=EDGE_CURVE ( 'NONE', #43124, #8862, #10886, .T. ) ;
#28227=CARTESIAN_POINT ( 'NONE',  ( 8.999999999999998224, 35.89808275599445153, -2.706964063997355119 ) ) ;
#28234=DIRECTION ( 'NONE',  ( 0.000000000000000000, 0.000000000000000000, 1.000000000000000000 ) ) ;
#28235=CARTESIAN_POINT ( 'NONE',  ( 17.99999999999999645, 0.000000000000000000, 0.000000000000000000 ) ) ;
#28236=CIRCLE ( 'NONE', #4521, 13.59999999999999964 ) ;
#28247=CARTESIAN_POINT ( 'NONE',  ( 17.99999999999999645, -19.47322409167291113, 30.27859877001394295 ) ) ;
#28255=DIRECTION ( 'NONE',  ( 1.000000000000000000, 0.000000000000000000, 0.000000000000000000 ) ) ;
#28267=DIRECTION ( 'NONE',  ( 0.000000000000000000, 0.000000000000000000, -1.000000000000000000 ) ) ;
#28277=DIRECTION ( 'NONE',  ( -1.000000000000000000, -0.000000000000000000, 0.000000000000000000 ) ) ;
#28282=CARTESIAN_POINT ( 'NONE',  ( 17.99999999999999645, 18.42432724429518842, -30.92804820215982886 ) ) ;
#28290=ORIENTED_EDGE ( 'NONE', *, *, #34136, .T. ) ;
#28298=DIRECTION ( 'NONE',  ( -1.000000000000000000, -0.000000000000000000, -0.000000000000000000 ) ) ;
#28312=DIRECTION ( 'NONE',  ( -1.000000000000000000, -0.000000000000000000, 0.000000000000000000 ) ) ;
#28319=ORIENTED_EDGE ( 'NONE', *, *, #19653, .T. ) ;
#28335=AXIS2_PLACEMENT_3D ( 'NONE', #35962, #6941, #20301 ) ;
#28340=CARTESIAN_POINT ( 'NONE',  ( 17.99999999999999645, -34.78944633786285578, 9.257128253673503337 ) ) ;
#28342=DIRECTION ( 'NONE',  ( -1.000000000000000000, 0.000000000000000000, 0.000000000000000000 ) ) ;
#28345=FACE_OUTER_BOUND ( 'NONE', #9251, .T. ) ;
#28354=ORIENTED_EDGE ( 'NONE', *, *, #41282, .F. ) ;
#28360=DIRECTION ( 'NONE',  ( -1.000000000000000000, 0.000000000000000000, 0.000000000000000000 ) ) ;
#28370=ORIENTED_EDGE ( 'NONE', *, *, #33158, .F. ) ;
#28388=ORIENTED_EDGE ( 'NONE', *, *, #42958, .T. ) ;
#28401=EDGE_CURVE ( 'NONE', #18333, #4714, #8780, .T. ) ;
#28402=CIRCLE ( 'NONE', #9558, 13.59999999999999787 ) ;
#28403=AXIS2_PLACEMENT_3D ( 'NONE', #6323, #10414, #13709 ) ;
#28420=ADVANCED_FACE ( 'NONE', ( #619 ), #27937, .T. ) ;
#28432=CYLINDRICAL_SURFACE ( 'NONE', #21537, 13.59999999999999964 ) ;
#28457=CARTESIAN_POINT ( 'NONE',  ( 17.99999999999999645, 0.000000000000000000, 0.000000000000000000 ) ) ;
#28472=AXIS2_PLACEMENT_3D ( 'NONE', #12057, #15757, #39055 ) ;
#28473=ORIENTED_EDGE ( 'NONE', *, *, #13122, .F. ) ;
#28486=CARTESIAN_POINT ( 'NONE',  ( 17.99999999999999645, 35.89808275599445153, 2.706964063997355119 ) ) ;
#28488=CARTESIAN_POINT ( 'NONE',  ( 17.99999999999999645, 19.69434969228073484, 24.58291258574055860 ) ) ;
#28489=VERTEX_POINT ( 'NONE', #22268 ) ;
#28497=ORIENTED_EDGE ( 'NONE', *, *, #1749, .T. ) ;
#28498=DIRECTION ( 'NONE',  ( 0.000000000000000000, 0.000000000000000000, 1.000000000000000000 ) ) ;
#28507=DIRECTION ( 'NONE',  ( 0.000000000000000000, -0.6736956436465479925, -0.7390089172206675272 ) ) ;
#28509=EDGE_CURVE ( 'NONE', #30296, #3075, #40843, .T. ) ;
#28513=CYLINDRICAL_SURFACE ( 'NONE', #8141, 13.59999999999999787 ) ;
#28516=DIRECTION ( 'NONE',  ( 0.000000000000000000, 0.000000000000000000, -1.000000000000000000 ) ) ;
#28529=ADVANCED_FACE ( 'NONE', ( #15063 ), #9122, .T. ) ;
#28540=LINE ( 'NONE', #25271, #10138 ) ;
#28541=LINE ( 'NONE', #31794, #17218 ) ;
#28551=CIRCLE ( 'NONE', #9702, 31.49900000000000588 ) ;
#28576=ORIENTED_EDGE ( 'NONE', *, *, #14600, .F. ) ;
#28578=EDGE_CURVE ( 'NONE', #6694, #14987, #22768, .T. ) ;
#28589=ORIENTED_EDGE ( 'NONE', *, *, #4009, .F. ) ;
#28608=ORIENTED_EDGE ( 'NONE', *, *, #23258, .T. ) ;
#28611=ORIENTED_EDGE ( 'NONE', *, *, #18780, .T. ) ;
#28612=DIRECTION ( 'NONE',  ( 0.000000000000000000, 0.000000000000000000, 1.000000000000000000 ) ) ;
#28630=CARTESIAN_POINT ( 'NONE',  ( 17.99999999999999645, -26.29521155129837595, -17.34211205339375184 ) ) ;
#28632=ORIENTED_EDGE ( 'NONE', *, *, #31800, .T. ) ;
#28642=CARTESIAN_POINT ( 'NONE',  ( 17.99999999999999645, 0.000000000000000000, 0.000000000000000000 ) ) ;
#28643=VERTEX_POINT ( 'NONE', #3413 ) ;
#28650=AXIS2_PLACEMENT_3D ( 'NONE', #36500, #43058, #6622 ) ;
#28655=CIRCLE ( 'NONE', #34202, 31.49900000000000233 ) ;
#28657=AXIS2_PLACEMENT_3D ( 'NONE', #21701, #1139, #5067 ) ;
#28678=ORIENTED_EDGE ( 'NONE', *, *, #2558, .T. ) ;
#28681=CYLINDRICAL_SURFACE ( 'NONE', #5356, 13.59999999999999964 ) ;
#28703=VERTEX_POINT ( 'NONE', #33537 ) ;
#28707=VERTEX_POINT ( 'NONE', #20485 ) ;
#28708=DIRECTION ( 'NONE',  ( 1.000000000000000000, 0.000000000000000000, 0.000000000000000000 ) ) ;
#28722=VECTOR ( 'NONE', #7045, 1000.000000000000000 ) ;
#28724=CARTESIAN_POINT ( 'NONE',  ( 17.99999999999999645, 0.000000000000000000, 0.000000000000000000 ) ) ;
#28728=DIRECTION ( 'NONE',  ( 0.000000000000000000, 0.000000000000000000, -1.000000000000000000 ) ) ;
#28738=ORIENTED_EDGE ( 'NONE', *, *, #23676, .T. ) ;
#28744=ORIENTED_EDGE ( 'NONE', *, *, #16655, .T. ) ;
#28749=AXIS2_PLACEMENT_3D ( 'NONE', #35343, #27967, #11161 ) ;
#28752=VECTOR ( 'NONE', #20673, 1000.000000000000000 ) ;
#28763=DIRECTION ( 'NONE',  ( -1.000000000000000000, 0.000000000000000000, 0.000000000000000000 ) ) ;
#28782=AXIS2_PLACEMENT_3D ( 'NONE', #4037, #30051, #33517 ) ;
#28807=ORIENTED_EDGE ( 'NONE', *, *, #24944, .F. ) ;
#28811=EDGE_CURVE ( 'NONE', #5335, #26178, #40497, .T. ) ;
#28837=DIRECTION ( 'NONE',  ( -1.000000000000000000, -0.000000000000000000, -0.000000000000000000 ) ) ;
#28842=CARTESIAN_POINT ( 'NONE',  ( 17.99999999999999645, 16.77727049691149475, -27.19001440037526862 ) ) ;
#28855=DIRECTION ( 'NONE',  ( -1.000000000000000000, 0.000000000000000000, 0.000000000000000000 ) ) ;
#28860=CARTESIAN_POINT ( 'NONE',  ( -10.00000000000000000, 0.000000000000000000, 0.000000000000000000 ) ) ;
#28870=ADVANCED_FACE ( 'NONE', ( #32000 ), #25073, .T. ) ;
#28874=VERTEX_POINT ( 'NONE', #7996 ) ;
#28887=DIRECTION ( 'NONE',  ( 0.000000000000000000, 0.000000000000000000, 1.000000000000000000 ) ) ;
#28889=AXIS2_PLACEMENT_3D ( 'NONE', #9549, #19405, #23107 ) ;
#28891=EDGE_CURVE ( 'NONE', #3075, #35838, #26267, .T. ) ;
#28899=CARTESIAN_POINT ( 'NONE',  ( 17.99999999999999645, 19.69434969228107946, -24.58291258574028504 ) ) ;
#28918=VECTOR ( 'NONE', #38899, 1000.000000000000000 ) ;
#28925=VERTEX_POINT ( 'NONE', #36110 ) ;
#28931=CARTESIAN_POINT ( 'NONE',  ( 17.99999999999999645, 22.66088087769211157, -21.87856208362532939 ) ) ;
#28932=DIRECTION ( 'NONE',  ( 1.000000000000000000, -0.000000000000000000, -0.000000000000000000 ) ) ;
#28946=DIRECTION ( 'NONE',  ( -1.000000000000000000, -0.000000000000000000, 0.000000000000000000 ) ) ;
#28949=DIRECTION ( 'NONE',  ( -1.000000000000000000, 0.000000000000000000, -0.000000000000000000 ) ) ;
#28955=CARTESIAN_POINT ( 'NONE',  ( 0.000000000000000000, 2.007101075700416182, -31.43498920425967569 ) ) ;
#28974=VECTOR ( 'NONE', #2171, 1000.000000000000000 ) ;
#28977=EDGE_LOOP ( 'NONE', ( #18308, #24317, #32829, #5039 ) ) ;
#28980=VERTEX_POINT ( 'NONE', #26523 ) ;
#28982=AXIS2_PLACEMENT_3D ( 'NONE', #41143, #8229, #25074 ) ;
#29011=CIRCLE ( 'NONE', #38044, 36.00000000000000000 ) ;
#29014=EDGE_LOOP ( 'NONE', ( #19331, #11195, #41357, #40862 ) ) ;
#29020=AXIS2_PLACEMENT_3D ( 'NONE', #18792, #35309, #11558 ) ;
#29023=ORIENTED_EDGE ( 'NONE', *, *, #29202, .F. ) ;
#29024=DIRECTION ( 'NONE',  ( -1.000000000000000000, 0.000000000000000000, -0.000000000000000000 ) ) ;
#29030=EDGE_LOOP ( 'NONE', ( #16352, #23213, #25871, #2730 ) ) ;
#29054=EDGE_CURVE ( 'NONE', #40989, #7683, #42986, .T. ) ;
#29067=ORIENTED_EDGE ( 'NONE', *, *, #21426, .T. ) ;
#29093=CARTESIAN_POINT ( 'NONE',  ( 0.000000000000000000, -3.803237743091689715, -31.26855263151018960 ) ) ;
#29100=CIRCLE ( 'NONE', #17986, 31.49899999999999523 ) ;
#29119=DIRECTION ( 'NONE',  ( 1.000000000000000000, 0.000000000000000000, 0.000000000000000000 ) ) ;
#29128=EDGE_LOOP ( 'NONE', ( #35680, #28111, #28807, #17313 ) ) ;
#29129=EDGE_CURVE ( 'NONE', #34690, #12201, #37613, .T. ) ;
#29132=DIRECTION ( 'NONE',  ( 0.000000000000000000, 0.000000000000000000, 1.000000000000000000 ) ) ;
#29187=DIRECTION ( 'NONE',  ( 0.000000000000000000, -0.8951632913550663373, 0.4457383557765300375 ) ) ;
#29191=AXIS2_PLACEMENT_3D ( 'NONE', #37467, #587, #27896 ) ;
#29195=AXIS2_PLACEMENT_3D ( 'NONE', #6172, #16026, #19097 ) ;
#29202=EDGE_CURVE ( 'NONE', #25212, #21757, #13881, .T. ) ;
#29207=LINE ( 'NONE', #22467, #17155 ) ;
#29215=LINE ( 'NONE', #22477, #37980 ) ;
#29226=ORIENTED_EDGE ( 'NONE', *, *, #24492, .T. ) ;
#29228=EDGE_CURVE ( 'NONE', #7044, #4975, #22842, .T. ) ;
#29232=ORIENTED_EDGE ( 'NONE', *, *, #3084, .T. ) ;
#29245=CIRCLE ( 'NONE', #10453, 31.49899999999999523 ) ;
#29250=ADVANCED_FACE ( 'NONE', ( #13658 ), #26956, .T. ) ;
#29259=ORIENTED_EDGE ( 'NONE', *, *, #15817, .F. ) ;
#29270=CARTESIAN_POINT ( 'NONE',  ( 0.000000000000000000, 14.84191762912315049, 27.78316904333131276 ) ) ;
#29276=CARTESIAN_POINT ( 'NONE',  ( 9.000000000000000000, -34.78944633786272789, -9.257128253673986507 ) ) ;
#29288=DIRECTION ( 'NONE',  ( 0.000000000000000000, 0.000000000000000000, 1.000000000000000000 ) ) ;
#29294=EDGE_CURVE ( 'NONE', #42378, #37373, #12361, .T. ) ;
#29307=CARTESIAN_POINT ( 'NONE',  ( 8.999999999999998224, 19.47322409167312429, -30.27859877001379374 ) ) ;
#29312=DIRECTION ( 'NONE',  ( 0.000000000000000000, 0.000000000000000000, 1.000000000000000000 ) ) ;
#29320=CARTESIAN_POINT ( 'NONE',  ( 17.99999999999999645, 31.80866420683995699, -2.997093558040963224 ) ) ;
#29329=AXIS2_PLACEMENT_3D ( 'NONE', #16309, #29614, #32444 ) ;
#29336=CIRCLE ( 'NONE', #39045, 13.59999999999999787 ) ;
#29341=AXIS2_PLACEMENT_3D ( 'NONE', #32053, #12433, #19003 ) ;
#29346=CIRCLE ( 'NONE', #37012, 13.59999999999999787 ) ;
#29353=ORIENTED_EDGE ( 'NONE', *, *, #23698, .T. ) ;
#29375=CARTESIAN_POINT ( 'NONE',  ( 0.000000000000000000, -13.57797752207946829, 33.34124362422470256 ) ) ;
#29380=DIRECTION ( 'NONE',  ( 0.000000000000000000, 0.000000000000000000, 1.000000000000000000 ) ) ;
#29385=FACE_OUTER_BOUND ( 'NONE', #30922, .T. ) ;
#29393=AXIS2_PLACEMENT_3D ( 'NONE', #36934, #3330, #700 ) ;
#29397=CIRCLE ( 'NONE', #34263, 13.59999999999999787 ) ;
#29399=AXIS2_PLACEMENT_3D ( 'NONE', #29481, #9182, #35771 ) ;
#29411=ADVANCED_FACE ( 'NONE', ( #31521 ), #1608, .T. ) ;
#29441=ORIENTED_EDGE ( 'NONE', *, *, #7287, .F. ) ;
#29466=EDGE_CURVE ( 'NONE', #30185, #10881, #5425, .T. ) ;
#29474=CIRCLE ( 'NONE', #30900, 36.00000000000000000 ) ;
#29481=CARTESIAN_POINT ( 'NONE',  ( 17.99999999999999645, -11.49545354908914518, -29.80986809967271967 ) ) ;
#29491=ORIENTED_EDGE ( 'NONE', *, *, #36502, .F. ) ;
#29492=CARTESIAN_POINT ( 'NONE',  ( 17.99999999999999645, 0.000000000000000000, 0.000000000000000000 ) ) ;
#29495=ORIENTED_EDGE ( 'NONE', *, *, #22622, .T. ) ;
#29515=VERTEX_POINT ( 'NONE', #5950 ) ;
#29517=DIRECTION ( 'NONE',  ( 0.000000000000000000, 0.000000000000000000, -1.000000000000000000 ) ) ;
#29530=EDGE_CURVE ( 'NONE', #21935, #3796, #32581, .T. ) ;
#29537=ORIENTED_EDGE ( 'NONE', *, *, #12324, .F. ) ;
#29540=CYLINDRICAL_SURFACE ( 'NONE', #27443, 13.60000000000000142 ) ;
#29549=ORIENTED_EDGE ( 'NONE', *, *, #36715, .F. ) ;
#29561=( NAMED_UNIT ( * ) SI_UNIT ( $, .STERADIAN. ) SOLID_ANGLE_UNIT ( ) );
#29572=AXIS2_PLACEMENT_3D ( 'NONE', #8282, #14849, #27723 ) ;
#29573=VERTEX_POINT ( 'NONE', #233 ) ;
#29578=DIRECTION ( 'NONE',  ( -1.000000000000000000, -0.000000000000000000, -0.000000000000000000 ) ) ;
#29579=FACE_OUTER_BOUND ( 'NONE', #29014, .T. ) ;
#29583=AXIS2_PLACEMENT_3D ( 'NONE', #11605, #5249, #21879 ) ;
#29605=FACE_OUTER_BOUND ( 'NONE', #27553, .T. ) ;
#29614=DIRECTION ( 'NONE',  ( -1.000000000000000000, 0.000000000000000000, 0.000000000000000000 ) ) ;
#29616=ORIENTED_EDGE ( 'NONE', *, *, #1170, .T. ) ;
#29628=DIRECTION ( 'NONE',  ( 0.000000000000000000, 0.000000000000000000, 1.000000000000000000 ) ) ;
#29640=ORIENTED_EDGE ( 'NONE', *, *, #2174, .F. ) ;
#29641=EDGE_CURVE ( 'NONE', #4444, #8807, #10085, .T. ) ;
#29651=AXIS2_PLACEMENT_3D ( 'NONE', #15218, #38073, #21768 ) ;
#29657=AXIS2_PLACEMENT_3D ( 'NONE', #18407, #1768, #18631 ) ;
#29661=AXIS2_PLACEMENT_3D ( 'NONE', #7711, #13865, #26934 ) ;
#29680=AXIS2_PLACEMENT_3D ( 'NONE', #26072, #19982, #9694 ) ;
#29698=ORIENTED_EDGE ( 'NONE', *, *, #28401, .F. ) ;
#29705=ORIENTED_EDGE ( 'NONE', *, *, #32051, .F. ) ;
#29722=CARTESIAN_POINT ( 'NONE',  ( 17.99999999999999645, 0.000000000000000000, 0.000000000000000000 ) ) ;
#29727=AXIS2_PLACEMENT_3D ( 'NONE', #21155, #15258, #11304 ) ;
#29732=ADVANCED_FACE ( 'NONE', ( #26901 ), #16895, .T. ) ;
#29754=CIRCLE ( 'NONE', #28403, 36.00000000000000000 ) ;
#29760=FACE_OUTER_BOUND ( 'NONE', #37484, .T. ) ;
#29765=ORIENTED_EDGE ( 'NONE', *, *, #8356, .T. ) ;
#29774=DIRECTION ( 'NONE',  ( 0.000000000000000000, 0.7980172272802363853, 0.6026346363792605132 ) ) ;
#29788=CARTESIAN_POINT ( 'NONE',  ( 17.99999999999999645, 0.000000000000000000, 0.000000000000000000 ) ) ;
#29793=ADVANCED_FACE ( 'NONE', ( #1986 ), #24735, .T. ) ;
#29794=DIRECTION ( 'NONE',  ( 0.000000000000000000, -0.8951632913550571224, -0.4457383557765488002 ) ) ;
#29801=CARTESIAN_POINT ( 'NONE',  ( 17.99999999999999645, 0.000000000000000000, 0.000000000000000000 ) ) ;
#29814=DIRECTION ( 'NONE',  ( 0.000000000000000000, -0.9618256431728160472, -0.2736629900720938813 ) ) ;
#29817=DIRECTION ( 'NONE',  ( -1.000000000000000000, 0.000000000000000000, 0.000000000000000000 ) ) ;
#29824=DIRECTION ( 'NONE',  ( 0.000000000000000000, 0.000000000000000000, 1.000000000000000000 ) ) ;
#29835=DIRECTION ( 'NONE',  ( 0.000000000000000000, 0.6736956436465532105, 0.7390089172206629753 ) ) ;
#29839=CARTESIAN_POINT ( 'NONE',  ( 0.000000000000000000, 0.000000000000000000, 0.000000000000000000 ) ) ;
#29853=AXIS2_PLACEMENT_3D ( 'NONE', #41852, #6479, #3188 ) ;
#29867=ORIENTED_EDGE ( 'NONE', *, *, #25834, .T. ) ;
#29872=DIRECTION ( 'NONE',  ( 0.000000000000000000, 0.000000000000000000, 1.000000000000000000 ) ) ;
#29875=CYLINDRICAL_SURFACE ( 'NONE', #35158, 13.59999999999999964 ) ;
#29879=DIRECTION ( 'NONE',  ( 0.000000000000000000, 0.000000000000000000, 1.000000000000000000 ) ) ;
#29886=AXIS2_PLACEMENT_3D ( 'NONE', #25021, #38049, #41307 ) ;
#29893=DIRECTION ( 'NONE',  ( -1.000000000000000000, 0.000000000000000000, 0.000000000000000000 ) ) ;
#29894=DIRECTION ( 'NONE',  ( -1.000000000000000000, 0.000000000000000000, -0.000000000000000000 ) ) ;
#29899=ADVANCED_FACE ( 'NONE', ( #19255 ), #32108, .T. ) ;
#29908=AXIS2_PLACEMENT_3D ( 'NONE', #13669, #23499, #36978 ) ;
#29909=ORIENTED_EDGE ( 'NONE', *, *, #41352, .T. ) ;
#29912=AXIS2_PLACEMENT_3D ( 'NONE', #39253, #19254, #2613 ) ;
#29913=EDGE_CURVE ( 'NONE', #26002, #18694, #1274, .T. ) ;
#29926=DIRECTION ( 'NONE',  ( -1.000000000000000000, -0.000000000000000000, 0.000000000000000000 ) ) ;
#29927=ORIENTED_EDGE ( 'NONE', *, *, #24790, .T. ) ;
#29939=EDGE_LOOP ( 'NONE', ( #12674, #28608, #6653, #38396 ) ) ;
#29952=VERTEX_POINT ( 'NONE', #29270 ) ;
#29953=DIRECTION ( 'NONE',  ( -1.000000000000000000, 0.000000000000000000, 0.000000000000000000 ) ) ;
#29962=EDGE_CURVE ( 'NONE', #3796, #38173, #34013, .T. ) ;
#29973=CARTESIAN_POINT ( 'NONE',  ( 17.99999999999999645, 0.000000000000000000, 0.000000000000000000 ) ) ;
#29984=ORIENTED_EDGE ( 'NONE', *, *, #16930, .T. ) ;
#30017=CARTESIAN_POINT ( 'NONE',  ( 17.99999999999999645, 26.29521155129848964, 17.34211205339357065 ) ) ;
#30031=CYLINDRICAL_SURFACE ( 'NONE', #13757, 13.59999999999999964 ) ;
#30051=DIRECTION ( 'NONE',  ( -1.000000000000000000, 0.000000000000000000, 0.000000000000000000 ) ) ;
#30052=DIRECTION ( 'NONE',  ( 0.000000000000000000, 0.5264321628773507289, 0.8502171357296173237 ) ) ;
#30057=VECTOR ( 'NONE', #16948, 1000.000000000000000 ) ;
#30059=ORIENTED_EDGE ( 'NONE', *, *, #10617, .T. ) ;
#30062=AXIS2_PLACEMENT_3D ( 'NONE', #5662, #12456, #8948 ) ;
#30074=DIRECTION ( 'NONE',  ( -1.000000000000000000, 0.000000000000000000, 0.000000000000000000 ) ) ;
#30081=AXIS2_PLACEMENT_3D ( 'NONE', #16860, #26434, #9835 ) ;
#30085=EDGE_CURVE ( 'NONE', #38633, #29515, #15913, .T. ) ;
#30092=CARTESIAN_POINT ( 'NONE',  ( 17.99999999999999645, 5.919241748380035695, -31.39643714728450163 ) ) ;
#30100=ORIENTED_EDGE ( 'NONE', *, *, #1053, .F. ) ;
#30103=VERTEX_POINT ( 'NONE', #39904 ) ;
#30118=AXIS2_PLACEMENT_3D ( 'NONE', #34967, #1798, #4642 ) ;
#30131=DIRECTION ( 'NONE',  ( -1.000000000000000000, 0.000000000000000000, 0.000000000000000000 ) ) ;
#30141=VECTOR ( 'NONE', #36465, 1000.000000000000000 ) ;
#30145=AXIS2_PLACEMENT_3D ( 'NONE', #11962, #8446, #18317 ) ;
#30149=ORIENTED_EDGE ( 'NONE', *, *, #8640, .T. ) ;
#30155=DIRECTION ( 'NONE',  ( -1.000000000000000000, 0.000000000000000000, 0.000000000000000000 ) ) ;
#30178=CARTESIAN_POINT ( 'NONE',  ( 17.99999999999999645, 0.000000000000000000, 0.000000000000000000 ) ) ;
#30182=CARTESIAN_POINT ( 'NONE',  ( -10.00000000000000000, 0.000000000000000000, 0.000000000000000000 ) ) ;
#30185=VERTEX_POINT ( 'NONE', #42011 ) ;
#30190=CARTESIAN_POINT ( 'NONE',  ( 0.000000000000000000, 0.000000000000000000, 0.000000000000000000 ) ) ;
#30200=CARTESIAN_POINT ( 'NONE',  ( 0.000000000000000000, -27.24480646643596415, -15.80846360676612505 ) ) ;
#30211=ORIENTED_EDGE ( 'NONE', *, *, #6788, .T. ) ;
#30213=EDGE_CURVE ( 'NONE', #19383, #13115, #21552, .T. ) ;
#30223=DIRECTION ( 'NONE',  ( -1.000000000000000000, -0.000000000000000000, 0.000000000000000000 ) ) ;
#30226=CARTESIAN_POINT ( 'NONE',  ( 17.99999999999999645, -30.71634675606047793, -8.790889055186887902 ) ) ;
#30247=AXIS2_PLACEMENT_3D ( 'NONE', #22216, #29578, #5582 ) ;
#30251=CARTESIAN_POINT ( 'NONE',  ( 17.99999999999999645, 0.000000000000000000, 0.000000000000000000 ) ) ;
#30267=ORIENTED_EDGE ( 'NONE', *, *, #20915, .F. ) ;
#30272=CARTESIAN_POINT ( 'NONE',  ( 17.99999999999999645, 0.000000000000000000, 0.000000000000000000 ) ) ;
#30273=AXIS2_PLACEMENT_3D ( 'NONE', #14863, #41431, #5654 ) ;
#30284=ORIENTED_EDGE ( 'NONE', *, *, #18639, .F. ) ;
#30296=VERTEX_POINT ( 'NONE', #10924 ) ;
#30300=DIRECTION ( 'NONE',  ( -1.000000000000000000, -0.000000000000000000, -0.000000000000000000 ) ) ;
#30301=DIRECTION ( 'NONE',  ( -1.000000000000000000, -0.000000000000000000, -0.000000000000000000 ) ) ;
#30302=ADVANCED_FACE ( 'NONE', ( #34242 ), #30031, .T. ) ;
#30310=ORIENTED_EDGE ( 'NONE', *, *, #18023, .T. ) ;
#30316=VECTOR ( 'NONE', #18502, 1000.000000000000000 ) ;
#30317=DIRECTION ( 'NONE',  ( 1.000000000000000000, 0.000000000000000000, -0.000000000000000000 ) ) ;
#30328=DIRECTION ( 'NONE',  ( 0.000000000000000000, 0.000000000000000000, 1.000000000000000000 ) ) ;
#30333=AXIS2_PLACEMENT_3D ( 'NONE', #23086, #12809, #36332 ) ;
#30341=DIRECTION ( 'NONE',  ( -1.000000000000000000, 0.000000000000000000, 0.000000000000000000 ) ) ;
#30375=EDGE_CURVE ( 'NONE', #6807, #27591, #32537, .T. ) ;
#30377=CIRCLE ( 'NONE', #12364, 36.00000000000000000 ) ;
#30386=ADVANCED_FACE ( 'NONE', ( #6017 ), #26532, .T. ) ;
#30391=DIRECTION ( 'NONE',  ( -1.000000000000000000, 0.000000000000000000, 0.000000000000000000 ) ) ;
#30402=CIRCLE ( 'NONE', #28335, 13.59999999999999964 ) ;
#30443=ORIENTED_EDGE ( 'NONE', *, *, #29054, .F. ) ;
#30444=CARTESIAN_POINT ( 'NONE',  ( 0.000000000000000000, 0.000000000000000000, 0.000000000000000000 ) ) ;
#30466=ORIENTED_EDGE ( 'NONE', *, *, #34780, .F. ) ;
#30471=CIRCLE ( 'NONE', #34624, 13.59999999999999787 ) ;
#30478=CIRCLE ( 'NONE', #39409, 13.59999999999999787 ) ;
#30481=DIRECTION ( 'NONE',  ( -1.000000000000000000, -0.000000000000000000, 0.000000000000000000 ) ) ;
#30483=DIRECTION ( 'NONE',  ( 0.000000000000000000, 0.000000000000000000, 1.000000000000000000 ) ) ;
#30515=FACE_OUTER_BOUND ( 'NONE', #25926, .T. ) ;
#30534=CARTESIAN_POINT ( 'NONE',  ( 17.99999999999999645, 11.49545354908936545, 29.80986809967263085 ) ) ;
#30537=VECTOR ( 'NONE', #6409, 1000.000000000000000 ) ;
#30552=DIRECTION ( 'NONE',  ( 0.000000000000000000, 0.000000000000000000, 1.000000000000000000 ) ) ;
#30555=DIRECTION ( 'NONE',  ( 0.000000000000000000, 0.000000000000000000, 1.000000000000000000 ) ) ;
#30569=DIRECTION ( 'NONE',  ( -1.000000000000000000, 0.000000000000000000, -0.000000000000000000 ) ) ;
#30574=FACE_OUTER_BOUND ( 'NONE', #34674, .T. ) ;
#30580=EDGE_CURVE ( 'NONE', #36912, #26654, #11709, .T. ) ;
#30587=DIRECTION ( 'NONE',  ( -1.000000000000000000, -0.000000000000000000, 0.000000000000000000 ) ) ;
#30591=CIRCLE ( 'NONE', #29195, 36.00000000000000000 ) ;
#30612=CARTESIAN_POINT ( 'NONE',  ( 0.000000000000000000, 0.000000000000000000, 0.000000000000000000 ) ) ;
#30617=CARTESIAN_POINT ( 'NONE',  ( 0.000000000000000000, 30.74337109795219547, -8.695908345466218492 ) ) ;
#30620=FACE_OUTER_BOUND ( 'NONE', #38707, .T. ) ;
#30621=ORIENTED_EDGE ( 'NONE', *, *, #43051, .F. ) ;
#30632=EDGE_CURVE ( 'NONE', #40062, #38171, #33259, .T. ) ;
#30639=FACE_OUTER_BOUND ( 'NONE', #20516, .T. ) ;
#30643=VERTEX_POINT ( 'NONE', #8594 ) ;
#30647=DIRECTION ( 'NONE',  ( -1.000000000000000000, -0.000000000000000000, -0.000000000000000000 ) ) ;
#30658=ORIENTED_EDGE ( 'NONE', *, *, #31466, .T. ) ;
#30661=CARTESIAN_POINT ( 'NONE',  ( 17.99999999999999645, 31.80866420683990725, 16.59709355804141495 ) ) ;
#30670=VERTEX_POINT ( 'NONE', #2243 ) ;
#30679=DIRECTION ( 'NONE',  ( 0.000000000000000000, 0.6736956436465582065, -0.7390089172206580903 ) ) ;
#30697=ORIENTED_EDGE ( 'NONE', *, *, #33140, .T. ) ;
#30711=FACE_OUTER_BOUND ( 'NONE', #28140, .T. ) ;
#30723=DIRECTION ( 'NONE',  ( 0.000000000000000000, -0.9957341762950354669, 0.09226835946329130234 ) ) ;
#30734=AXIS2_PLACEMENT_3D ( 'NONE', #30190, #3739, #3973 ) ;
#30751=DIRECTION ( 'NONE',  ( -1.000000000000000000, 0.000000000000000000, 0.000000000000000000 ) ) ;
#30764=CYLINDRICAL_SURFACE ( 'NONE', #33454, 13.60000000000000142 ) ;
#30787=FACE_OUTER_BOUND ( 'NONE', #25936, .T. ) ;
#30799=CIRCLE ( 'NONE', #26622, 36.00000000000000000 ) ;
#30818=CARTESIAN_POINT ( 'NONE',  ( 17.99999999999999645, -5.822172717930031993, -31.41458249383147106 ) ) ;
#30827=DIRECTION ( 'NONE',  ( 0.000000000000000000, -0.9957341762950334685, -0.09226835946331299332 ) ) ;
#30829=CARTESIAN_POINT ( 'NONE',  ( 0.000000000000000000, 11.58753559615485251, 29.77419532459266449 ) ) ;
#30833=CYLINDRICAL_SURFACE ( 'NONE', #38317, 36.00000000000000000 ) ;
#30845=CARTESIAN_POINT ( 'NONE',  ( 0.000000000000000000, -5.822172717930484964, 31.41458249383138934 ) ) ;
#30855=ORIENTED_EDGE ( 'NONE', *, *, #7928, .F. ) ;
#30861=CARTESIAN_POINT ( 'NONE',  ( 0.000000000000000000, 16.86122981692017930, 27.13802899033298388 ) ) ;
#30864=EDGE_CURVE ( 'NONE', #28489, #34791, #33234, .T. ) ;
#30875=EDGE_LOOP ( 'NONE', ( #8421, #26844, #36564, #11997 ) ) ;
#30876=DIRECTION ( 'NONE',  ( 0.000000000000000000, -0.1837495178165570453, -0.9829730996839042279 ) ) ;
#30881=CARTESIAN_POINT ( 'NONE',  ( 0.000000000000000000, 0.000000000000000000, 0.000000000000000000 ) ) ;
#30885=CARTESIAN_POINT ( 'NONE',  ( 9.000000000000000000, 6.007673836298004666, 35.49518073029998533 ) ) ;
#30888=CIRCLE ( 'NONE', #39912, 13.59999999999999787 ) ;
#30890=FACE_OUTER_BOUND ( 'NONE', #101, .T. ) ;
#30892=EDGE_LOOP ( 'NONE', ( #38274, #25744, #38140, #32088 ) ) ;
#30900=AXIS2_PLACEMENT_3D ( 'NONE', #28724, #25457, #22199 ) ;
#30911=ADVANCED_FACE ( 'NONE', ( #5749 ), #29540, .T. ) ;
#30920=LINE ( 'NONE', #11085, #24834 ) ;
#30921=CARTESIAN_POINT ( 'NONE',  ( 8.999999999999998224, -23.79363200506972476, 27.01597816121638829 ) ) ;
#30922=EDGE_LOOP ( 'NONE', ( #29067, #40404, #17343, #63 ) ) ;
#30927=CYLINDRICAL_SURFACE ( 'NONE', #29191, 31.49899999999999878 ) ;
#30933=AXIS2_PLACEMENT_3D ( 'NONE', #392, #11121, #17474 ) ;
#30941=CARTESIAN_POINT ( 'NONE',  ( 17.99999999999999645, 34.78944633786279184, 9.257128253673748475 ) ) ;
#30962=EDGE_CURVE ( 'NONE', #15150, #3093, #5840, .T. ) ;
#30970=DIRECTION ( 'NONE',  ( 0.000000000000000000, 0.000000000000000000, 1.000000000000000000 ) ) ;
#30982=CYLINDRICAL_SURFACE ( 'NONE', #18973, 31.49899999999999878 ) ;
#30985=DIRECTION ( 'NONE',  ( -1.000000000000000000, 0.000000000000000000, 0.000000000000000000 ) ) ;
#30991=DIRECTION ( 'NONE',  ( 0.000000000000000000, 0.000000000000000000, 1.000000000000000000 ) ) ;
#30996=CARTESIAN_POINT ( 'NONE',  ( 17.99999999999999645, -18.25486108452607681, -25.66996392254292658 ) ) ;
#31013=ORIENTED_EDGE ( 'NONE', *, *, #22428, .F. ) ;
#31015=DIRECTION ( 'NONE',  ( 0.000000000000000000, 0.000000000000000000, 1.000000000000000000 ) ) ;
#31031=ORIENTED_EDGE ( 'NONE', *, *, #28891, .F. ) ;
#31043=DIRECTION ( 'NONE',  ( 0.000000000000000000, 0.9957341762950341346, 0.09226835946330566585 ) ) ;
#31057=VECTOR ( 'NONE', #30481, 1000.000000000000000 ) ;
#31064=ORIENTED_EDGE ( 'NONE', *, *, #11806, .T. ) ;
#31106=EDGE_LOOP ( 'NONE', ( #30697, #27252, #21547, #40917 ) ) ;
#31126=CYLINDRICAL_SURFACE ( 'NONE', #9318, 36.00000000000000000 ) ;
#31128=ORIENTED_EDGE ( 'NONE', *, *, #21302, .F. ) ;
#31129=CARTESIAN_POINT ( 'NONE',  ( 17.99999999999999645, -29.03409033315573851, -12.21509719675420946 ) ) ;
#31131=EDGE_LOOP ( 'NONE', ( #29023, #27997, #33253, #42004 ) ) ;
#31133=ORIENTED_EDGE ( 'NONE', *, *, #8859, .F. ) ;
#31134=DIRECTION ( 'NONE',  ( -1.000000000000000000, 0.000000000000000000, 0.000000000000000000 ) ) ;
#31135=DIRECTION ( 'NONE',  ( 0.000000000000000000, 0.000000000000000000, 1.000000000000000000 ) ) ;
#31139=CARTESIAN_POINT ( 'NONE',  ( -10.00000000000000000, 0.000000000000000000, 0.000000000000000000 ) ) ;
#31142=CYLINDRICAL_SURFACE ( 'NONE', #25632, 31.49899999999999878 ) ;
#31145=LINE ( 'NONE', #24624, #25512 ) ;
#31146=ADVANCED_FACE ( 'NONE', ( #30574 ), #27742, .T. ) ;
#31155=CYLINDRICAL_SURFACE ( 'NONE', #34057, 31.49899999999999878 ) ;
#31156=AXIS2_PLACEMENT_3D ( 'NONE', #2380, #9376, #12474 ) ;
#31177=DIRECTION ( 'NONE',  ( -1.000000000000000000, -0.000000000000000000, 0.000000000000000000 ) ) ;
#31192=VECTOR ( 'NONE', #39537, 1000.000000000000000 ) ;
#31203=CARTESIAN_POINT ( 'NONE',  ( 0.000000000000000000, -21.56073507908662634, 23.57770962728557151 ) ) ;
#31209=ORIENTED_EDGE ( 'NONE', *, *, #34658, .T. ) ;
#31211=CARTESIAN_POINT ( 'NONE',  ( 17.99999999999999645, -28.57802095670097131, 14.28532136906662586 ) ) ;
#31212=DIRECTION ( 'NONE',  ( -1.000000000000000000, -0.000000000000000000, -0.000000000000000000 ) ) ;
#31215=ORIENTED_EDGE ( 'NONE', *, *, #37793, .F. ) ;
#31220=AXIS2_PLACEMENT_3D ( 'NONE', #19095, #2233, #15393 ) ;
#31223=ORIENTED_EDGE ( 'NONE', *, *, #4702, .T. ) ;
#31225=CARTESIAN_POINT ( 'NONE',  ( 0.000000000000000000, 31.80866420683990725, 2.997093558041416195 ) ) ;
#31240=CARTESIAN_POINT ( 'NONE',  ( 17.99999999999999645, 29.68570942776472066, 10.53307442156944873 ) ) ;
#31270=ORIENTED_EDGE ( 'NONE', *, *, #30213, .T. ) ;
#31287=VERTEX_POINT ( 'NONE', #4803 ) ;
#31288=EDGE_CURVE ( 'NONE', #18067, #32556, #21932, .T. ) ;
#31291=DIRECTION ( 'NONE',  ( -1.000000000000000000, 0.000000000000000000, -0.000000000000000000 ) ) ;
#31292=EDGE_CURVE ( 'NONE', #2013, #1401, #13560, .T. ) ;
#31298=VERTEX_POINT ( 'NONE', #31633 ) ;
#31300=DIRECTION ( 'NONE',  ( 0.000000000000000000, -0.9618256431728160472, -0.2736629900720938813 ) ) ;
#31315=ORIENTED_EDGE ( 'NONE', *, *, #5961, .F. ) ;
#31320=DIRECTION ( 'NONE',  ( 0.000000000000000000, 0.9618256431728180456, 0.2736629900720866093 ) ) ;
#31336=LINE ( 'NONE', #11927, #36268 ) ;
#31342=ADVANCED_FACE ( 'NONE', ( #15719 ), #5860, .T. ) ;
#31357=CARTESIAN_POINT ( 'NONE',  ( 17.99999999999999645, 30.74337109795208178, 8.695908345466650147 ) ) ;
#31362=CARTESIAN_POINT ( 'NONE',  ( 0.000000000000000000, 7.749090474611950441, -30.53094492177204700 ) ) ;
#31369=VERTEX_POINT ( 'NONE', #2153 ) ;
#31382=DIRECTION ( 'NONE',  ( 0.000000000000000000, 0.000000000000000000, 1.000000000000000000 ) ) ;
#31401=ADVANCED_FACE ( 'NONE', ( #1514 ), #8501, .T. ) ;
#31433=EDGE_LOOP ( 'NONE', ( #14160, #1330, #247, #33757 ) ) ;
#31434=CARTESIAN_POINT ( 'NONE',  ( 8.999999999999998224, -18.42432724429495394, 30.92804820215996386 ) ) ;
#31436=EDGE_LOOP ( 'NONE', ( #8635, #37616, #35621, #1008 ) ) ;
#31448=CIRCLE ( 'NONE', #23801, 31.49899999999999878 ) ;
#31456=DIRECTION ( 'NONE',  ( -1.000000000000000000, -0.000000000000000000, 0.000000000000000000 ) ) ;
#31464=CARTESIAN_POINT ( 'NONE',  ( 17.99999999999999645, 25.52601536738592358, 19.21447964122706509 ) ) ;
#31466=EDGE_CURVE ( 'NONE', #27712, #6599, #18448, .T. ) ;
#31471=CARTESIAN_POINT ( 'NONE',  ( 0.000000000000000000, -12.42760411676061949, 33.78690065568420664 ) ) ;
#31480=ORIENTED_EDGE ( 'NONE', *, *, #34246, .T. ) ;
#31495=DIRECTION ( 'NONE',  ( -1.000000000000000000, -0.000000000000000000, -0.000000000000000000 ) ) ;
#31501=ORIENTED_EDGE ( 'NONE', *, *, #7287, .T. ) ;
#31513=AXIS2_PLACEMENT_3D ( 'NONE', #31211, #1722, #4798 ) ;
#31521=FACE_OUTER_BOUND ( 'NONE', #13965, .T. ) ;
#31530=VERTEX_POINT ( 'NONE', #35955 ) ;
#31544=ORIENTED_EDGE ( 'NONE', *, *, #25808, .T. ) ;
#31577=AXIS2_PLACEMENT_3D ( 'NONE', #822, #28360, #37700 ) ;
#31590=CARTESIAN_POINT ( 'NONE',  ( 17.99999999999999645, -22.66088087769196235, 21.87856208362548571 ) ) ;
#31602=DIRECTION ( 'NONE',  ( -1.000000000000000000, -0.000000000000000000, 0.000000000000000000 ) ) ;
#31608=AXIS2_PLACEMENT_3D ( 'NONE', #41004, #3907, #17293 ) ;
#31614=DIRECTION ( 'NONE',  ( 0.000000000000000000, 0.000000000000000000, 1.000000000000000000 ) ) ;
#31633=CARTESIAN_POINT ( 'NONE',  ( 0.000000000000000000, 35.89808275599445153, -2.706964063997353342 ) ) ;
#31648=CYLINDRICAL_SURFACE ( 'NONE', #13433, 13.59999999999999787 ) ;
#31659=DIRECTION ( 'NONE',  ( -1.000000000000000000, 0.000000000000000000, -0.000000000000000000 ) ) ;
#31678=VERTEX_POINT ( 'NONE', #33993 ) ;
#31686=ORIENTED_EDGE ( 'NONE', *, *, #1189, .F. ) ;
#31691=DIRECTION ( 'NONE',  ( -1.000000000000000000, -0.000000000000000000, 0.000000000000000000 ) ) ;
#31700=ADVANCED_FACE ( 'NONE', ( #33556 ), #17670, .T. ) ;
#31710=AXIS2_PLACEMENT_3D ( 'NONE', #35936, #6704, #33334 ) ;
#31720=ORIENTED_EDGE ( 'NONE', *, *, #13170, .F. ) ;
#31726=ORIENTED_EDGE ( 'NONE', *, *, #40674, .F. ) ;
#31739=ORIENTED_EDGE ( 'NONE', *, *, #6314, .F. ) ;
#31746=DIRECTION ( 'NONE',  ( -1.000000000000000000, 0.000000000000000000, -0.000000000000000000 ) ) ;
#31747=VERTEX_POINT ( 'NONE', #22239 ) ;
#31759=EDGE_CURVE ( 'NONE', #38173, #8515, #37896, .T. ) ;
#31761=ORIENTED_EDGE ( 'NONE', *, *, #17545, .F. ) ;
#31773=ADVANCED_FACE ( 'NONE', ( #11760 ), #8017, .T. ) ;
#31789=VERTEX_POINT ( 'NONE', #28340 ) ;
#31793=DIRECTION ( 'NONE',  ( 1.000000000000000000, 0.000000000000000000, 0.000000000000000000 ) ) ;
#31794=CARTESIAN_POINT ( 'NONE',  ( 8.999999999999998224, -29.09613215194468339, -21.19941258140352858 ) ) ;
#31800=EDGE_CURVE ( 'NONE', #35367, #12837, #15684, .T. ) ;
#31809=ORIENTED_EDGE ( 'NONE', *, *, #25007, .T. ) ;
#31841=DIRECTION ( 'NONE',  ( 0.000000000000000000, -6.887872625202028030E-15, 1.000000000000000000 ) ) ;
#31852=DIRECTION ( 'NONE',  ( -1.000000000000000000, -0.000000000000000000, -0.000000000000000000 ) ) ;
#31860=ORIENTED_EDGE ( 'NONE', *, *, #32723, .F. ) ;
#31861=DIRECTION ( 'NONE',  ( -1.000000000000000000, 0.000000000000000000, 0.000000000000000000 ) ) ;
#31880=CARTESIAN_POINT ( 'NONE',  ( 0.000000000000000000, -0.04937522221144796664, 31.94951095880159997 ) ) ;
#31883=CARTESIAN_POINT ( 'NONE',  ( 0.000000000000000000, 31.48608500567870294, 0.9019157472705636724 ) ) ;
#31885=AXIS2_PLACEMENT_3D ( 'NONE', #1581, #41727, #15156 ) ;
#31890=CARTESIAN_POINT ( 'NONE',  ( 0.000000000000000000, -29.09613215194497826, 21.19941258140312002 ) ) ;
#31909=DIRECTION ( 'NONE',  ( -1.000000000000000000, 0.000000000000000000, 0.000000000000000000 ) ) ;
#31924=CARTESIAN_POINT ( 'NONE',  ( 17.99999999999999645, -19.69434969228056787, -24.58291258574069360 ) ) ;
#31935=CARTESIAN_POINT ( 'NONE',  ( 17.99999999999999645, -7.749090474611724844, 30.53094492177211094 ) ) ;
#31944=ORIENTED_EDGE ( 'NONE', *, *, #10617, .F. ) ;
#31946=DIRECTION ( 'NONE',  ( -1.000000000000000000, 0.000000000000000000, 0.000000000000000000 ) ) ;
#31959=EDGE_CURVE ( 'NONE', #8862, #40989, #91, .T. ) ;
#31973=DIRECTION ( 'NONE',  ( 0.000000000000000000, 0.000000000000000000, -1.000000000000000000 ) ) ;
#31981=ORIENTED_EDGE ( 'NONE', *, *, #5272, .T. ) ;
#32000=FACE_OUTER_BOUND ( 'NONE', #1431, .T. ) ;
#32001=FACE_OUTER_BOUND ( 'NONE', #9241, .T. ) ;
#32010=ADVANCED_FACE ( 'NONE', ( #29605 ), #39610, .T. ) ;
#32021=ORIENTED_EDGE ( 'NONE', *, *, #3613, .F. ) ;
#32025=DIRECTION ( 'NONE',  ( -1.000000000000000000, 0.000000000000000000, -0.000000000000000000 ) ) ;
#32029=ORIENTED_EDGE ( 'NONE', *, *, #40844, .F. ) ;
#32035=ORIENTED_EDGE ( 'NONE', *, *, #34704, .T. ) ;
#32047=LINE ( 'NONE', #1496, #16626 ) ;
#32051=EDGE_CURVE ( 'NONE', #13471, #41650, #39361, .T. ) ;
#32053=CARTESIAN_POINT ( 'NONE',  ( -10.00000000000000000, 0.000000000000000000, 0.000000000000000000 ) ) ;
#32054=EDGE_CURVE ( 'NONE', #31287, #3430, #22703, .T. ) ;
#32066=CARTESIAN_POINT ( 'NONE',  ( 17.99999999999999645, -16.77727049691090500, -27.19001440037564166 ) ) ;
#32072=EDGE_CURVE ( 'NONE', #32077, #37143, #1028, .T. ) ;
#32074=DIRECTION ( 'NONE',  ( 0.000000000000000000, -0.6736956436465638687, 0.7390089172206529833 ) ) ;
#32077=VERTEX_POINT ( 'NONE', #41056 ) ;
#32079=ORIENTED_EDGE ( 'NONE', *, *, #963, .T. ) ;
#32088=ORIENTED_EDGE ( 'NONE', *, *, #32051, .T. ) ;
#32091=EDGE_CURVE ( 'NONE', #30296, #31298, #16961, .T. ) ;
#32092=ORIENTED_EDGE ( 'NONE', *, *, #21258, .T. ) ;
#32094=AXIS2_PLACEMENT_3D ( 'NONE', #38977, #25924, #19596 ) ;
#32108=CYLINDRICAL_SURFACE ( 'NONE', #6843, 13.60000000000000142 ) ;
#32109=ORIENTED_EDGE ( 'NONE', *, *, #41049, .T. ) ;
#32111=ORIENTED_EDGE ( 'NONE', *, *, #885, .F. ) ;
#32112=DIRECTION ( 'NONE',  ( 1.000000000000000000, 0.000000000000000000, 0.000000000000000000 ) ) ;
#32119=FACE_OUTER_BOUND ( 'NONE', #31131, .T. ) ;
#32155=CIRCLE ( 'NONE', #14773, 36.00000000000000000 ) ;
#32157=AXIS2_PLACEMENT_3D ( 'NONE', #29492, #19266, #32540 ) ;
#32204=ORIENTED_EDGE ( 'NONE', *, *, #3271, .T. ) ;
#32206=CARTESIAN_POINT ( 'NONE',  ( 0.000000000000000000, 1.836970198721029589E-15, -15.00000000000000000 ) ) ;
#32208=FACE_OUTER_BOUND ( 'NONE', #27118, .T. ) ;
#32220=EDGE_CURVE ( 'NONE', #38361, #6792, #38659, .T. ) ;
#32224=CARTESIAN_POINT ( 'NONE',  ( 8.999999999999998224, 23.79363200506992015, -27.01597816121622486 ) ) ;
#32241=EDGE_CURVE ( 'NONE', #7956, #1973, #3815, .T. ) ;
#32242=EDGE_CURVE ( 'NONE', #20215, #41335, #19214, .T. ) ;
#32253=DIRECTION ( 'NONE',  ( -1.000000000000000000, -0.000000000000000000, 0.000000000000000000 ) ) ;
#32268=AXIS2_PLACEMENT_3D ( 'NONE', #24823, #11719, #34157 ) ;
#32270=DIRECTION ( 'NONE',  ( 0.000000000000000000, 0.000000000000000000, 1.000000000000000000 ) ) ;
#32277=( GEOMETRIC_REPRESENTATION_CONTEXT ( 3 ) GLOBAL_UNCERTAINTY_ASSIGNED_CONTEXT ( ( #34368 ) ) GLOBAL_UNIT_ASSIGNED_CONTEXT ( ( #18724, #41567, #11717 ) ) REPRESENTATION_CONTEXT ( 'NONE', 'WORKASPACE' ) );
#32291=CIRCLE ( 'NONE', #38567, 13.59999999999999787 ) ;
#32296=ADVANCED_FACE ( 'NONE', ( #25815 ), #39070, .T. ) ;
#32302=DIRECTION ( 'NONE',  ( -1.000000000000000000, 0.000000000000000000, -0.000000000000000000 ) ) ;
#32324=DIRECTION ( 'NONE',  ( 0.000000000000000000, -0.7980172272802447120, 0.6026346363792492999 ) ) ;
#32342=DIRECTION ( 'NONE',  ( 0.000000000000000000, 0.7980172272802408262, -0.6026346363792547400 ) ) ;
#32346=EDGE_CURVE ( 'NONE', #19537, #15044, #24800, .T. ) ;
#32371=ADVANCED_FACE ( 'NONE', ( #21913 ), #18860, .T. ) ;
#32373=DIRECTION ( 'NONE',  ( 0.000000000000000000, -0.5264321628773450668, -0.8502171357296208765 ) ) ;
#32378=CARTESIAN_POINT ( 'NONE',  ( 18.00000000000000355, 0.000000000000000000, 0.000000000000000000 ) ) ;
#32388=CARTESIAN_POINT ( 'NONE',  ( 9.000000000000000000, -35.78425302087541127, 3.935382540232670312 ) ) ;
#32389=ORIENTED_EDGE ( 'NONE', *, *, #40138, .F. ) ;
#32411=AXIS2_PLACEMENT_3D ( 'NONE', #21704, #31691, #41492 ) ;
#32414=ORIENTED_EDGE ( 'NONE', *, *, #42652, .T. ) ;
#32430=EDGE_CURVE ( 'NONE', #6784, #9051, #38006, .T. ) ;
#32436=CARTESIAN_POINT ( 'NONE',  ( 8.999999999999998224, 35.89808275599445153, 2.706964063997355119 ) ) ;
#32444=DIRECTION ( 'NONE',  ( 0.000000000000000000, -0.3612416661871601375, 0.9324722294043530368 ) ) ;
#32445=ORIENTED_EDGE ( 'NONE', *, *, #30864, .T. ) ;
#32452=EDGE_LOOP ( 'NONE', ( #1969, #37094, #4556, #9659 ) ) ;
#32467=CYLINDRICAL_SURFACE ( 'NONE', #3787, 13.60000000000000142 ) ;
#32481=DIRECTION ( 'NONE',  ( -1.000000000000000000, -0.000000000000000000, 0.000000000000000000 ) ) ;
#32484=CIRCLE ( 'NONE', #26919, 13.59999999999999964 ) ;
#32513=ADVANCED_FACE ( 'NONE', ( #33610 ), #26223, .T. ) ;
#32537=CIRCLE ( 'NONE', #14441, 36.00000000000000000 ) ;
#32540=DIRECTION ( 'NONE',  ( 0.000000000000000000, 0.000000000000000000, 1.000000000000000000 ) ) ;
#32543=ORIENTED_EDGE ( 'NONE', *, *, #6549, .T. ) ;
#32549=DIRECTION ( 'NONE',  ( 0.000000000000000000, -0.3612416661871603596, 0.9324722294043529258 ) ) ;
#32556=VERTEX_POINT ( 'NONE', #27964 ) ;
#32562=CIRCLE ( 'NONE', #38817, 36.00000000000000000 ) ;
#32564=AXIS2_PLACEMENT_3D ( 'NONE', #17344, #32112, #41912 ) ;
#32567=EDGE_LOOP ( 'NONE', ( #1363, #6187, #9908, #14495 ) ) ;
#32571=CARTESIAN_POINT ( 'NONE',  ( 17.99999999999999645, 31.81777574834305966, -2.898764365605425830 ) ) ;
#32575=DIRECTION ( 'NONE',  ( 1.000000000000000000, -0.000000000000000000, -0.000000000000000000 ) ) ;
#32581=LINE ( 'NONE', #28899, #31192 ) ;
#32589=DIRECTION ( 'NONE',  ( -1.000000000000000000, 0.000000000000000000, -0.000000000000000000 ) ) ;
#32598=EDGE_CURVE ( 'NONE', #20215, #36754, #27517, .T. ) ;
#32609=VERTEX_POINT ( 'NONE', #27750 ) ;
#32634=ORIENTED_EDGE ( 'NONE', *, *, #42652, .F. ) ;
#32653=DIRECTION ( 'NONE',  ( -1.000000000000000000, 0.000000000000000000, 0.000000000000000000 ) ) ;
#32668=CARTESIAN_POINT ( 'NONE',  ( 0.000000000000000000, 6.007673836298004666, 35.49518073029998533 ) ) ;
#32685=CARTESIAN_POINT ( 'NONE',  ( 17.99999999999999645, -31.80866420683989304, -2.997093558041628025 ) ) ;
#32688=CARTESIAN_POINT ( 'NONE',  ( 17.99999999999999645, -13.22719389141960100, -28.58720592780609593 ) ) ;
#32690=EDGE_CURVE ( 'NONE', #18694, #36912, #3129, .T. ) ;
#32723=EDGE_CURVE ( 'NONE', #28707, #12063, #29011, .T. ) ;
#32726=CYLINDRICAL_SURFACE ( 'NONE', #31156, 13.59999999999999964 ) ;
#32730=ORIENTED_EDGE ( 'NONE', *, *, #686, .T. ) ;
#32738=CARTESIAN_POINT ( 'NONE',  ( 17.99999999999999645, -19.69434969228056787, -24.58291258574069360 ) ) ;
#32764=CARTESIAN_POINT ( 'NONE',  ( 17.99999999999999645, -16.77727049691128869, 27.19001440037539297 ) ) ;
#32765=CIRCLE ( 'NONE', #16774, 13.59999999999999964 ) ;
#32767=CARTESIAN_POINT ( 'NONE',  ( 0.000000000000000000, 31.80866420683995699, -2.997093558040963224 ) ) ;
#32771=CIRCLE ( 'NONE', #13992, 31.49899999999999878 ) ;
#32781=FACE_OUTER_BOUND ( 'NONE', #6769, .T. ) ;
#32794=VERTEX_POINT ( 'NONE', #25345 ) ;
#32795=CIRCLE ( 'NONE', #3493, 13.60000000000000320 ) ;
#32804=FACE_OUTER_BOUND ( 'NONE', #8213, .T. ) ;
#32807=DIRECTION ( 'NONE',  ( -1.000000000000000000, 0.000000000000000000, 0.000000000000000000 ) ) ;
#32808=ORIENTED_EDGE ( 'NONE', *, *, #12443, .F. ) ;
#32821=CARTESIAN_POINT ( 'NONE',  ( 17.99999999999999645, -30.74337109795225942, 8.695908345466005329 ) ) ;
#32829=ORIENTED_EDGE ( 'NONE', *, *, #20420, .T. ) ;
#32834=EDGE_CURVE ( 'NONE', #12461, #17650, #3887, .T. ) ;
#32836=CARTESIAN_POINT ( 'NONE',  ( 17.99999999999999645, 0.000000000000000000, 0.000000000000000000 ) ) ;
#32839=ORIENTED_EDGE ( 'NONE', *, *, #33708, .T. ) ;
#32861=LINE ( 'NONE', #32436, #22475 ) ;
#32874=CARTESIAN_POINT ( 'NONE',  ( 0.000000000000000000, 0.000000000000000000, 0.000000000000000000 ) ) ;
#32875=ORIENTED_EDGE ( 'NONE', *, *, #32220, .T. ) ;
#32885=ADVANCED_FACE ( 'NONE', ( #10221 ), #2993, .T. ) ;
#32919=ORIENTED_EDGE ( 'NONE', *, *, #16974, .T. ) ;
#32921=AXIS2_PLACEMENT_3D ( 'NONE', #14898, #28837, #38624 ) ;
#32934=EDGE_CURVE ( 'NONE', #22441, #10216, #30402, .T. ) ;
#32940=DIRECTION ( 'NONE',  ( 1.000000000000000000, 0.000000000000000000, 0.000000000000000000 ) ) ;
#32947=CARTESIAN_POINT ( 'NONE',  ( 0.000000000000000000, 16.86122981692056655, -27.13802899033274940 ) ) ;
#32960=EDGE_CURVE ( 'NONE', #29952, #12461, #33875, .T. ) ;
#32978=FACE_OUTER_BOUND ( 'NONE', #41542, .T. ) ;
#32987=FACE_OUTER_BOUND ( 'NONE', #10136, .T. ) ;
#32988=LINE ( 'NONE', #25842, #19689 ) ;
#32999=ORIENTED_EDGE ( 'NONE', *, *, #1749, .F. ) ;
#33001=ORIENTED_EDGE ( 'NONE', *, *, #37137, .T. ) ;
#33014=ORIENTED_EDGE ( 'NONE', *, *, #14686, .F. ) ;
#33015=CARTESIAN_POINT ( 'NONE',  ( 17.99999999999999645, -5.919241748379815427, 31.39643714728454427 ) ) ;
#33026=CIRCLE ( 'NONE', #41399, 36.00000000000000000 ) ;
#33027=DIRECTION ( 'NONE',  ( -1.000000000000000000, -0.000000000000000000, -0.000000000000000000 ) ) ;
#33032=DIRECTION ( 'NONE',  ( 1.000000000000000000, -0.000000000000000000, -0.000000000000000000 ) ) ;
#33038=CARTESIAN_POINT ( 'NONE',  ( 0.000000000000000000, -31.80866420683992857, 2.997093558041182160 ) ) ;
#33039=CYLINDRICAL_SURFACE ( 'NONE', #39432, 13.60000000000000142 ) ;
#33049=FACE_OUTER_BOUND ( 'NONE', #38404, .T. ) ;
#33054=DIRECTION ( 'NONE',  ( -1.000000000000000000, -0.000000000000000000, -0.000000000000000000 ) ) ;
#33059=ORIENTED_EDGE ( 'NONE', *, *, #41352, .F. ) ;
#33085=ORIENTED_EDGE ( 'NONE', *, *, #42527, .F. ) ;
#33087=EDGE_CURVE ( 'NONE', #38633, #19127, #24647, .T. ) ;
#33094=VERTEX_POINT ( 'NONE', #24220 ) ;
#33104=FACE_OUTER_BOUND ( 'NONE', #5688, .T. ) ;
#33105=CARTESIAN_POINT ( 'NONE',  ( 17.99999999999999645, -21.48775762007842260, -23.64423737150161031 ) ) ;
#33120=VECTOR ( 'NONE', #37314, 1000.000000000000000 ) ;
#33128=LINE ( 'NONE', #6293, #37936 ) ;
#33140=EDGE_CURVE ( 'NONE', #11159, #1957, #7154, .T. ) ;
#33157=DIRECTION ( 'NONE',  ( 0.000000000000000000, 0.000000000000000000, 1.000000000000000000 ) ) ;
#33158=EDGE_CURVE ( 'NONE', #14447, #4027, #37049, .T. ) ;
#33160=AXIS2_PLACEMENT_3D ( 'NONE', #7435, #41013, #20797 ) ;
#33164=VERTEX_POINT ( 'NONE', #1904 ) ;
#33173=ORIENTED_EDGE ( 'NONE', *, *, #14321, .F. ) ;
#33178=ORIENTED_EDGE ( 'NONE', *, *, #22818, .F. ) ;
#33220=CARTESIAN_POINT ( 'NONE',  ( 17.99999999999999645, 22.66088087769180603, 21.87856208362564914 ) ) ;
#33232=DIRECTION ( 'NONE',  ( 0.000000000000000000, 0.000000000000000000, 1.000000000000000000 ) ) ;
#33234=LINE ( 'NONE', #13189, #19796 ) ;
#33246=EDGE_CURVE ( 'NONE', #9615, #40347, #27635, .T. ) ;
#33247=VERTEX_POINT ( 'NONE', #35493 ) ;
#33251=DIRECTION ( 'NONE',  ( 0.000000000000000000, 0.000000000000000000, -1.000000000000000000 ) ) ;
#33253=ORIENTED_EDGE ( 'NONE', *, *, #24111, .T. ) ;
#33256=ORIENTED_EDGE ( 'NONE', *, *, #5044, .T. ) ;
#33259=CIRCLE ( 'NONE', #4696, 13.60000000000000142 ) ;
#33268=VERTEX_POINT ( 'NONE', #25096 ) ;
#33271=EDGE_CURVE ( 'NONE', #15863, #18333, #15471, .T. ) ;
#33281=CARTESIAN_POINT ( 'NONE',  ( 0.000000000000000000, -24.70533337038204635, -26.18485254986720179 ) ) ;
#33284=ORIENTED_EDGE ( 'NONE', *, *, #36643, .T. ) ;
#33286=LINE ( 'NONE', #9726, #30057 ) ;
#33315=CIRCLE ( 'NONE', #1266, 13.59999999999999964 ) ;
#33320=VECTOR ( 'NONE', #19306, 1000.000000000000000 ) ;
#33334=DIRECTION ( 'NONE',  ( 0.000000000000000000, 0.000000000000000000, 1.000000000000000000 ) ) ;
#33377=EDGE_CURVE ( 'NONE', #10881, #42317, #10909, .T. ) ;
#33393=ORIENTED_EDGE ( 'NONE', *, *, #24596, .F. ) ;
#33397=DIRECTION ( 'NONE',  ( 0.000000000000000000, 0.000000000000000000, 1.000000000000000000 ) ) ;
#33400=DIRECTION ( 'NONE',  ( -1.000000000000000000, -0.000000000000000000, 0.000000000000000000 ) ) ;
#33417=DIRECTION ( 'NONE',  ( -1.000000000000000000, 0.000000000000000000, 0.000000000000000000 ) ) ;
#33436=ORIENTED_EDGE ( 'NONE', *, *, #37792, .T. ) ;
#33444=ORIENTED_EDGE ( 'NONE', *, *, #14062, .T. ) ;
#33454=AXIS2_PLACEMENT_3D ( 'NONE', #19726, #40761, #16445 ) ;
#33472=DIRECTION ( 'NONE',  ( -1.000000000000000000, 0.000000000000000000, 0.000000000000000000 ) ) ;
#33510=ADVANCED_FACE ( 'NONE', ( #761 ), #21118, .T. ) ;
#33511=CARTESIAN_POINT ( 'NONE',  ( 8.999999999999998224, 28.35267316522783432, 22.18391138608718549 ) ) ;
#33517=DIRECTION ( 'NONE',  ( 0.000000000000000000, 0.8951632913550603421, 0.4457383557765422499 ) ) ;
#33527=CIRCLE ( 'NONE', #30062, 13.60000000000000142 ) ;
#33528=ORIENTED_EDGE ( 'NONE', *, *, #39856, .F. ) ;
#33534=AXIS2_PLACEMENT_3D ( 'NONE', #27981, #37759, #41025 ) ;
#33537=CARTESIAN_POINT ( 'NONE',  ( 17.99999999999999645, -2.007101075700182591, 31.43498920425968279 ) ) ;
#33542=CARTESIAN_POINT ( 'NONE',  ( 17.99999999999999645, 0.000000000000000000, 0.000000000000000000 ) ) ;
#33546=FACE_OUTER_BOUND ( 'NONE', #14074, .T. ) ;
#33550=CARTESIAN_POINT ( 'NONE',  ( 17.99999999999999645, -11.49545354908957862, 29.80986809967256335 ) ) ;
#33556=FACE_OUTER_BOUND ( 'NONE', #7145, .T. ) ;
#33563=EDGE_CURVE ( 'NONE', #27630, #27814, #33718, .T. ) ;
#33574=LINE ( 'NONE', #17030, #27938 ) ;
#33579=ORIENTED_EDGE ( 'NONE', *, *, #21007, .T. ) ;
#33583=AXIS2_PLACEMENT_3D ( 'NONE', #1367, #41279, #11428 ) ;
#33593=DIRECTION ( 'NONE',  ( -1.000000000000000000, 0.000000000000000000, -0.000000000000000000 ) ) ;
#33594=CARTESIAN_POINT ( 'NONE',  ( 17.99999999999999645, 0.000000000000000000, 0.000000000000000000 ) ) ;
#33597=LINE ( 'NONE', #9825, #22953 ) ;
#33608=DIRECTION ( 'NONE',  ( 0.000000000000000000, 0.000000000000000000, 1.000000000000000000 ) ) ;
#33610=FACE_OUTER_BOUND ( 'NONE', #1896, .T. ) ;
#33616=DIRECTION ( 'NONE',  ( 0.000000000000000000, 0.000000000000000000, 1.000000000000000000 ) ) ;
#33619=EDGE_CURVE ( 'NONE', #26002, #20435, #2447, .T. ) ;
#33654=ORIENTED_EDGE ( 'NONE', *, *, #10484, .T. ) ;
#33690=VERTEX_POINT ( 'NONE', #24818 ) ;
#33692=ORIENTED_EDGE ( 'NONE', *, *, #19091, .F. ) ;
#33694=DIRECTION ( 'NONE',  ( -1.000000000000000000, 0.000000000000000000, 0.000000000000000000 ) ) ;
#33704=DIRECTION ( 'NONE',  ( 0.000000000000000000, 0.000000000000000000, 1.000000000000000000 ) ) ;
#33708=EDGE_CURVE ( 'NONE', #3331, #31747, #8835, .T. ) ;
#33710=VERTEX_POINT ( 'NONE', #25671 ) ;
#33715=VECTOR ( 'NONE', #25896, 1000.000000000000000 ) ;
#33716=DIRECTION ( 'NONE',  ( -1.000000000000000000, 0.000000000000000000, 0.000000000000000000 ) ) ;
#33718=LINE ( 'NONE', #33511, #26871 ) ;
#33730=ADVANCED_FACE ( 'NONE', ( #21971 ), #34585, .T. ) ;
#33742=CIRCLE ( 'NONE', #14978, 13.59999999999999964 ) ;
#33756=DIRECTION ( 'NONE',  ( 0.000000000000000000, -0.6736956436465479925, -0.7390089172206675272 ) ) ;
#33757=ORIENTED_EDGE ( 'NONE', *, *, #243, .T. ) ;
#33762=DIRECTION ( 'NONE',  ( -1.000000000000000000, 0.000000000000000000, -0.000000000000000000 ) ) ;
#33765=CARTESIAN_POINT ( 'NONE',  ( 17.99999999999999645, 0.000000000000000000, 0.000000000000000000 ) ) ;
#33777=DIRECTION ( 'NONE',  ( 1.000000000000000000, 0.000000000000000000, 0.000000000000000000 ) ) ;
#33792=ORIENTED_EDGE ( 'NONE', *, *, #6192, .F. ) ;
#33802=ORIENTED_EDGE ( 'NONE', *, *, #24719, .F. ) ;
#33807=EDGE_CURVE ( 'NONE', #26460, #16104, #42616, .T. ) ;
#33810=CYLINDRICAL_SURFACE ( 'NONE', #9640, 13.60000000000000142 ) ;
#33812=VECTOR ( 'NONE', #27587, 1000.000000000000000 ) ;
#33813=VERTEX_POINT ( 'NONE', #12766 ) ;
#33819=EDGE_CURVE ( 'NONE', #12201, #24796, #38721, .T. ) ;
#33821=CIRCLE ( 'NONE', #38672, 36.00000000000000000 ) ;
#33824=DIRECTION ( 'NONE',  ( 0.000000000000000000, 0.000000000000000000, 1.000000000000000000 ) ) ;
#33830=DIRECTION ( 'NONE',  ( 1.000000000000000000, 0.000000000000000000, 0.000000000000000000 ) ) ;
#33835=AXIS2_PLACEMENT_3D ( 'NONE', #40143, #10278, #7200 ) ;
#33868=AXIS2_PLACEMENT_3D ( 'NONE', #22917, #37025, #20276 ) ;
#33875=CIRCLE ( 'NONE', #7364, 13.59999999999999964 ) ;
#33896=ORIENTED_EDGE ( 'NONE', *, *, #16930, .F. ) ;
#33897=LINE ( 'NONE', #37155, #30537 ) ;
#33919=CARTESIAN_POINT ( 'NONE',  ( 0.000000000000000000, 22.66088087769180603, 21.87856208362564914 ) ) ;
#33930=DIRECTION ( 'NONE',  ( -1.000000000000000000, 0.000000000000000000, 0.000000000000000000 ) ) ;
#33931=CARTESIAN_POINT ( 'NONE',  ( 17.99999999999999645, 0.6168405712486720871, 35.99471499692226928 ) ) ;
#33937=CARTESIAN_POINT ( 'NONE',  ( 17.99999999999999645, 31.94619804602787738, -16.59639811537323340 ) ) ;
#33939=EDGE_LOOP ( 'NONE', ( #29765, #9404, #17617, #32414 ) ) ;
#33940=DIRECTION ( 'NONE',  ( 0.000000000000000000, 0.000000000000000000, -1.000000000000000000 ) ) ;
#33943=VECTOR ( 'NONE', #40652, 1000.000000000000000 ) ;
#33944=DIRECTION ( 'NONE',  ( 0.000000000000000000, 0.000000000000000000, 1.000000000000000000 ) ) ;
#33946=DIRECTION ( 'NONE',  ( 0.000000000000000000, 0.000000000000000000, 1.000000000000000000 ) ) ;
#33974=LINE ( 'NONE', #7572, #2423 ) ;
#33977=ORIENTED_EDGE ( 'NONE', *, *, #27583, .F. ) ;
#33986=ORIENTED_EDGE ( 'NONE', *, *, #5736, .T. ) ;
#33987=CARTESIAN_POINT ( 'NONE',  ( 0.000000000000000000, -31.48608500567871005, 0.9019157472703476230 ) ) ;
#33993=CARTESIAN_POINT ( 'NONE',  ( 17.99999999999999645, 30.78424799127077804, -6.672111855472861563 ) ) ;
#34013=CIRCLE ( 'NONE', #28472, 13.60000000000000142 ) ;
#34014=DIRECTION ( 'NONE',  ( -1.000000000000000000, 0.000000000000000000, 0.000000000000000000 ) ) ;
#34017=EDGE_LOOP ( 'NONE', ( #33014, #31315, #21044, #26332 ) ) ;
#34025=AXIS2_PLACEMENT_3D ( 'NONE', #8287, #31852, #1937 ) ;
#34046=LINE ( 'NONE', #31434, #12583 ) ;
#34057=AXIS2_PLACEMENT_3D ( 'NONE', #24421, #37674, #41151 ) ;
#34063=EDGE_LOOP ( 'NONE', ( #42574, #38078, #2661, #3186, #2079, #28319, #11468, #32999, #10338, #10440, #31981, #21338, #41585, #27505, #25805, #19293, #32919, #36218, #39765, #12058, #27623, #27615, #12820, #28072, #18701, #19833, #43177, #31223, #17768, #29616, #27291, #17837, #7147, #1662, #30211, #16684, #26351, #30855, #26262, #16901, #8347, #1349, #12348, #3109, #26732, #32634, #10249, #39971, #12335, #43161, #37569, #26698, #1301, #17953, #37369, #8171, #26696, #25339, #16337, #648, #26595, #11696, #21236, #28388, #12807, #31686, #3628, #36095, #2819, #18810, #723, #9287, #20724, #10214, #39649, #635, #34940, #13573, #19073, #8760, #455, #36501, #35147, #23790, #29232, #33896, #6163, #5271, #25099, #11432, #6358, #21927, #89, #9362, #37996, #38242, #37895, #16608, #36050, #9198, #31480, #27330, #31501, #27499, #22100, #15018, #2462, #16062, #8067, #4096, #35602, #4611, #27823, #23876, #27949, #29909, #1571, #7658, #32029, #5459, #16150, #7359, #1695, #26633, #26250, #14837, #26564, #27959, #23723, #32875, #16300, #42644, #24365, #15544, #23112, #14591, #9397, #12808, #27310, #14848, #33001 ) ) ;
#34082=DIRECTION ( 'NONE',  ( 0.000000000000000000, 0.000000000000000000, -1.000000000000000000 ) ) ;
#34083=DIRECTION ( 'NONE',  ( -1.000000000000000000, -0.000000000000000000, -0.000000000000000000 ) ) ;
#34087=VECTOR ( 'NONE', #29953, 1000.000000000000000 ) ;
#34091=DIRECTION ( 'NONE',  ( 0.000000000000000000, 0.000000000000000000, 1.000000000000000000 ) ) ;
#34093=CIRCLE ( 'NONE', #35459, 13.60000000000000320 ) ;
#34096=CARTESIAN_POINT ( 'NONE',  ( 17.99999999999999645, 13.22719389142019608, -28.58720592780581882 ) ) ;
#34099=ORIENTED_EDGE ( 'NONE', *, *, #32598, .T. ) ;
#34103=ORIENTED_EDGE ( 'NONE', *, *, #14006, .F. ) ;
#34106=DIRECTION ( 'NONE',  ( 1.000000000000000000, 0.000000000000000000, 0.000000000000000000 ) ) ;
#34107=EDGE_CURVE ( 'NONE', #4975, #27337, #19267, .T. ) ;
#34116=CARTESIAN_POINT ( 'NONE',  ( 0.000000000000000000, 24.70533337038223110, 26.18485254986702060 ) ) ;
#34120=ORIENTED_EDGE ( 'NONE', *, *, #10319, .F. ) ;
#34127=DIRECTION ( 'NONE',  ( -1.000000000000000000, 0.000000000000000000, 0.000000000000000000 ) ) ;
#34134=CYLINDRICAL_SURFACE ( 'NONE', #15020, 36.00000000000000000 ) ;
#34136=EDGE_CURVE ( 'NONE', #39574, #24001, #5283, .T. ) ;
#34138=CARTESIAN_POINT ( 'NONE',  ( 17.99999999999999645, 25.52601536738619714, -19.21447964122670626 ) ) ;
#34147=CARTESIAN_POINT ( 'NONE',  ( 17.99999999999999645, -28.35267316522800130, 22.18391138608698299 ) ) ;
#34152=ADVANCED_FACE ( 'NONE', ( #11219 ), #41931, .T. ) ;
#34157=DIRECTION ( 'NONE',  ( 0.000000000000000000, 0.000000000000000000, -1.000000000000000000 ) ) ;
#34159=AXIS2_PLACEMENT_3D ( 'NONE', #26826, #36846, #36404 ) ;
#34179=CYLINDRICAL_SURFACE ( 'NONE', #39688, 31.49899999999999878 ) ;
#34202=AXIS2_PLACEMENT_3D ( 'NONE', #9689, #2250, #42609 ) ;
#34206=VECTOR ( 'NONE', #14920, 1000.000000000000000 ) ;
#34208=VECTOR ( 'NONE', #22920, 1000.000000000000000 ) ;
#34216=LINE ( 'NONE', #6736, #19685 ) ;
#34235=CARTESIAN_POINT ( 'NONE',  ( 17.99999999999999645, 0.000000000000000000, 0.000000000000000000 ) ) ;
#34242=FACE_OUTER_BOUND ( 'NONE', #33939, .T. ) ;
#34245=EDGE_LOOP ( 'NONE', ( #31726, #40617, #35531, #36727, #21718, #36844, #3718, #5197, #27758, #3283, #22442, #8132, #9646, #15090, #18782, #14209, #33393, #41609, #4234, #21786, #2289, #16795, #2374, #23880, #30100, #19186, #36181, #19745, #31739, #39932, #39860, #395, #10330, #19009, #21202, #10806, #34381, #13772, #3296, #17256, #40737, #29259, #37536, #30267, #14309, #5424, #11349, #1322, #24713, #451, #11563, #7540, #8477, #33085, #38696, #8488, #1117, #31944, #29705, #32021, #22683, #25243, #1296, #18633, #35356, #22542, #851, #28101, #11546, #18817, #38674, #36484, #42694, #19548, #26370, #31215, #31761, #27154, #6986, #3339, #31128, #8232, #39138, #39589, #34991, #14253, #20220, #11478, #38101, #37439, #26, #32389, #22748, #12530, #23912, #25899, #11881, #20635, #1718, #29549, #31031, #15646, #33173, #34103, #25386, #13316, #18702, #39535, #18965, #28354, #33802, #14542, #10101, #16804, #22596, #15040, #19719, #37874, #42106, #35485, #12327, #15408, #7634, #6588, #18208, #35929, #42110, #9151, #22612, #2854, #24541, #27640, #41515, #471, #37675, #22560, #3766, #42350, #4800, #12736, #4155 ) ) ;
#34246=EDGE_CURVE ( 'NONE', #18842, #10311, #38752, .T. ) ;
#34250=FACE_OUTER_BOUND ( 'NONE', #13028, .T. ) ;
#34253=EDGE_LOOP ( 'NONE', ( #4524, #38177, #5346, #13230 ) ) ;
#34254=DIRECTION ( 'NONE',  ( -1.000000000000000000, -0.000000000000000000, 0.000000000000000000 ) ) ;
#34258=DIRECTION ( 'NONE',  ( -1.000000000000000000, -0.000000000000000000, 0.000000000000000000 ) ) ;
#34263=AXIS2_PLACEMENT_3D ( 'NONE', #39815, #35900, #15887 ) ;
#34273=CIRCLE ( 'NONE', #15505, 36.00000000000000000 ) ;
#34276=CARTESIAN_POINT ( 'NONE',  ( 0.000000000000000000, 19.69434969228107946, -24.58291258574028504 ) ) ;
#34280=DIRECTION ( 'NONE',  ( -1.000000000000000000, 0.000000000000000000, -0.000000000000000000 ) ) ;
#34300=CARTESIAN_POINT ( 'NONE',  ( 0.000000000000000000, 18.42432724429518487, -30.92804820215982531 ) ) ;
#34323=CARTESIAN_POINT ( 'NONE',  ( 17.99999999999999645, -14.84191762912296930, -27.78316904333141224 ) ) ;
#34334=ORIENTED_EDGE ( 'NONE', *, *, #6549, .F. ) ;
#34336=DIRECTION ( 'NONE',  ( 0.000000000000000000, 0.000000000000000000, -1.000000000000000000 ) ) ;
#34338=LINE ( 'NONE', #4435, #3033 ) ;
#34368=UNCERTAINTY_MEASURE_WITH_UNIT (LENGTH_MEASURE( 1.000000000000000082E-05 ), #18724, 'distance_accuracy_value', 'NONE');
#34381=ORIENTED_EDGE ( 'NONE', *, *, #28578, .F. ) ;
#34397=ORIENTED_EDGE ( 'NONE', *, *, #31288, .T. ) ;
#34419=ORIENTED_EDGE ( 'NONE', *, *, #3613, .T. ) ;
#34438=AXIS2_PLACEMENT_3D ( 'NONE', #3454, #30751, #40750 ) ;
#34448=LINE ( 'NONE', #5210, #9075 ) ;
#34450=VERTEX_POINT ( 'NONE', #19000 ) ;
#34473=LINE ( 'NONE', #4579, #17620 ) ;
#34490=FACE_OUTER_BOUND ( 'NONE', #9964, .T. ) ;
#34515=DIRECTION ( 'NONE',  ( 1.000000000000000000, -0.000000000000000000, 0.000000000000000000 ) ) ;
#34521=CIRCLE ( 'NONE', #15742, 13.59999999999999964 ) ;
#34530=FACE_OUTER_BOUND ( 'NONE', #11954, .T. ) ;
#34531=CARTESIAN_POINT ( 'NONE',  ( 0.000000000000000000, 35.78425302087538995, 3.935382540232923887 ) ) ;
#34538=DIRECTION ( 'NONE',  ( 0.000000000000000000, 0.000000000000000000, 1.000000000000000000 ) ) ;
#34542=EDGE_CURVE ( 'NONE', #34733, #33247, #17916, .T. ) ;
#34543=CARTESIAN_POINT ( 'NONE',  ( 0.000000000000000000, -9.484061862023704492, -30.03730300138991538 ) ) ;
#34545=ADVANCED_FACE ( 'NONE', ( #42488 ), #9332, .T. ) ;
#34555=AXIS2_PLACEMENT_3D ( 'NONE', #40047, #7121, #3406 ) ;
#34557=ORIENTED_EDGE ( 'NONE', *, *, #2655, .T. ) ;
#34562=COLOUR_RGB ( '', 0.40784314, 0.44705882, 0.49803922) ;
#34565=AXIS2_PLACEMENT_3D ( 'NONE', #39710, #24050, #40576 ) ;
#34566=CARTESIAN_POINT ( 'NONE',  ( -10.00000000000000000, 0.000000000000000000, 0.000000000000000000 ) ) ;
#34585=CYLINDRICAL_SURFACE ( 'NONE', #26164, 36.00000000000000000 ) ;
#34595=ADVANCED_FACE ( 'NONE', ( #12632 ), #39426, .T. ) ;
#34609=FACE_OUTER_BOUND ( 'NONE', #19963, .T. ) ;
#34621=AXIS2_PLACEMENT_3D ( 'NONE', #15387, #39301, #2024 ) ;
#34624=AXIS2_PLACEMENT_3D ( 'NONE', #11615, #8528, #14679 ) ;
#34631=AXIS2_PLACEMENT_3D ( 'NONE', #6643, #3946, #17332 ) ;
#34648=DIRECTION ( 'NONE',  ( -1.000000000000000000, -0.000000000000000000, -0.000000000000000000 ) ) ;
#34649=LINE ( 'NONE', #23632, #18520 ) ;
#34658=EDGE_CURVE ( 'NONE', #1973, #40378, #462, .T. ) ;
#34672=FACE_OUTER_BOUND ( 'NONE', #31436, .T. ) ;
#34674=EDGE_LOOP ( 'NONE', ( #731, #23384, #7592, #17723 ) ) ;
#34690=VERTEX_POINT ( 'NONE', #17654 ) ;
#34704=EDGE_CURVE ( 'NONE', #32609, #23378, #16997, .T. ) ;
#34710=CYLINDRICAL_SURFACE ( 'NONE', #16351, 13.60000000000000142 ) ;
#34716=EDGE_CURVE ( 'NONE', #28980, #17756, #26581, .T. ) ;
#34719=CIRCLE ( 'NONE', #14535, 31.49899999999999878 ) ;
#34733=VERTEX_POINT ( 'NONE', #6706 ) ;
#34749=CARTESIAN_POINT ( 'NONE',  ( 0.000000000000000000, 0.000000000000000000, 0.000000000000000000 ) ) ;
#34750=AXIS2_PLACEMENT_3D ( 'NONE', #20131, #36423, #419 ) ;
#34752=CIRCLE ( 'NONE', #593, 13.59999999999999964 ) ;
#34767=CARTESIAN_POINT ( 'NONE',  ( 0.000000000000000000, -18.42432724429495394, 30.92804820215996386 ) ) ;
#34774=VERTEX_POINT ( 'NONE', #41144 ) ;
#34780=EDGE_CURVE ( 'NONE', #15532, #23705, #28541, .T. ) ;
#34781=DIRECTION ( 'NONE',  ( -1.000000000000000000, 0.000000000000000000, 0.000000000000000000 ) ) ;
#34786=DIRECTION ( 'NONE',  ( 1.000000000000000000, -0.000000000000000000, 0.000000000000000000 ) ) ;
#34791=VERTEX_POINT ( 'NONE', #31362 ) ;
#34794=EDGE_CURVE ( 'NONE', #23705, #1507, #15132, .T. ) ;
#34795=ORIENTED_EDGE ( 'NONE', *, *, #22623, .F. ) ;
#34813=EDGE_CURVE ( 'NONE', #41650, #11761, #25272, .T. ) ;
#34829=EDGE_LOOP ( 'NONE', ( #2652, #32730, #13168, #90 ) ) ;
#34835=CARTESIAN_POINT ( 'NONE',  ( 0.000000000000000000, 0.000000000000000000, 0.000000000000000000 ) ) ;
#34837=DIRECTION ( 'NONE',  ( 1.000000000000000000, -0.000000000000000000, -0.000000000000000000 ) ) ;
#34858=LINE ( 'NONE', #31590, #17305 ) ;
#34863=AXIS2_PLACEMENT_3D ( 'NONE', #34235, #36255, #30970 ) ;
#34873=EDGE_CURVE ( 'NONE', #35008, #32609, #11626, .T. ) ;
#34886=CARTESIAN_POINT ( 'NONE',  ( 0.000000000000000000, 0.000000000000000000, 0.000000000000000000 ) ) ;
#34896=LINE ( 'NONE', #1508, #19693 ) ;
#34900=AXIS2_PLACEMENT_3D ( 'NONE', #24855, #38526, #17659 ) ;
#34940=ORIENTED_EDGE ( 'NONE', *, *, #36502, .T. ) ;
#34942=DIRECTION ( 'NONE',  ( -1.000000000000000000, 0.000000000000000000, 0.000000000000000000 ) ) ;
#34956=DIRECTION ( 'NONE',  ( -1.000000000000000000, -0.000000000000000000, -0.000000000000000000 ) ) ;
#34964=AXIS2_PLACEMENT_3D ( 'NONE', #23039, #26070, #3336 ) ;
#34967=CARTESIAN_POINT ( 'NONE',  ( 50.00005079999999680, 0.000000000000000000, 0.000000000000000000 ) ) ;
#34968=FACE_BOUND ( 'NONE', #26451, .T. ) ;
#34983=VERTEX_POINT ( 'NONE', #32206 ) ;
#34991=ORIENTED_EDGE ( 'NONE', *, *, #37683, .F. ) ;
#35002=ADVANCED_FACE ( 'NONE', ( #25703 ), #38953, .T. ) ;
#35006=VERTEX_POINT ( 'NONE', #9284 ) ;
#35008=VERTEX_POINT ( 'NONE', #26324 ) ;
#35040=VERTEX_POINT ( 'NONE', #42219 ) ;
#35046=CARTESIAN_POINT ( 'NONE',  ( 17.99999999999999645, -29.03409033315590904, 12.21509719675380623 ) ) ;
#35049=( GEOMETRIC_REPRESENTATION_CONTEXT ( 3 ) GLOBAL_UNCERTAINTY_ASSIGNED_CONTEXT ( ( #12029 ) ) GLOBAL_UNIT_ASSIGNED_CONTEXT ( ( #3755, #9480, #29561 ) ) REPRESENTATION_CONTEXT ( 'NONE', 'WORKASPACE' ) );
#35065=DIRECTION ( 'NONE',  ( -1.000000000000000000, 0.000000000000000000, 0.000000000000000000 ) ) ;
#35072=VECTOR ( 'NONE', #2811, 1000.000000000000000 ) ;
#35096=ORIENTED_EDGE ( 'NONE', *, *, #8182, .T. ) ;
#35116=DIRECTION ( 'NONE',  ( -1.000000000000000000, -0.000000000000000000, -0.000000000000000000 ) ) ;
#35132=CARTESIAN_POINT ( 'NONE',  ( 0.000000000000000000, -6.007673836297746206, -35.49518073030003507 ) ) ;
#35136=ADVANCED_FACE ( 'NONE', ( #33049 ), #3572, .T. ) ;
#35147=ORIENTED_EDGE ( 'NONE', *, *, #7064, .T. ) ;
#35149=VERTEX_POINT ( 'NONE', #17162 ) ;
#35154=CARTESIAN_POINT ( 'NONE',  ( 17.99999999999999645, 0.000000000000000000, 0.000000000000000000 ) ) ;
#35156=DIRECTION ( 'NONE',  ( -1.000000000000000000, -0.000000000000000000, -0.000000000000000000 ) ) ;
#35158=AXIS2_PLACEMENT_3D ( 'NONE', #6920, #27230, #6709 ) ;
#35171=AXIS2_PLACEMENT_3D ( 'NONE', #38281, #3039, #33608 ) ;
#35172=CARTESIAN_POINT ( 'NONE',  ( 17.99999999999999645, 0.000000000000000000, 0.000000000000000000 ) ) ;
#35180=DIRECTION ( 'NONE',  ( 0.000000000000000000, 0.9957341762950349118, -0.09226835946329871307 ) ) ;
#35182=VECTOR ( 'NONE', #30155, 1000.000000000000000 ) ;
#35183=DIRECTION ( 'NONE',  ( 0.000000000000000000, 0.000000000000000000, -1.000000000000000000 ) ) ;
#35186=EDGE_CURVE ( 'NONE', #34791, #10990, #40204, .T. ) ;
#35190=CIRCLE ( 'NONE', #310, 13.60000000000000142 ) ;
#35211=VERTEX_POINT ( 'NONE', #33281 ) ;
#35215=DIRECTION ( 'NONE',  ( -1.000000000000000000, 0.000000000000000000, 0.000000000000000000 ) ) ;
#35226=FACE_OUTER_BOUND ( 'NONE', #21297, .T. ) ;
#35231=LINE ( 'NONE', #12563, #17008 ) ;
#35253=VERTEX_POINT ( 'NONE', #37826 ) ;
#35261=ORIENTED_EDGE ( 'NONE', *, *, #7476, .T. ) ;
#35262=LINE ( 'NONE', #26327, #1468 ) ;
#35270=AXIS2_PLACEMENT_3D ( 'NONE', #13045, #2529, #6456 ) ;
#35276=CARTESIAN_POINT ( 'NONE',  ( 0.000000000000000000, -16.77727049691128869, 27.19001440037539297 ) ) ;
#35278=CYLINDRICAL_SURFACE ( 'NONE', #25919, 13.59999999999999964 ) ;
#35285=DIRECTION ( 'NONE',  ( 0.000000000000000000, 0.8951632913550604531, 0.4457383557765421944 ) ) ;
#35309=DIRECTION ( 'NONE',  ( -1.000000000000000000, -0.000000000000000000, -0.000000000000000000 ) ) ;
#35324=CARTESIAN_POINT ( 'NONE',  ( 0.000000000000000000, -12.42760411676013987, -33.78690065568439138 ) ) ;
#35329=ORIENTED_EDGE ( 'NONE', *, *, #30375, .T. ) ;
#35331=DIRECTION ( 'NONE',  ( -1.000000000000000000, -0.000000000000000000, 0.000000000000000000 ) ) ;
#35343=CARTESIAN_POINT ( 'NONE',  ( 17.99999999999999645, 16.77727049691110750, 27.19001440037552086 ) ) ;
#35356=ORIENTED_EDGE ( 'NONE', *, *, #686, .F. ) ;
#35362=CIRCLE ( 'NONE', #1224, 13.59999999999999964 ) ;
#35367=VERTEX_POINT ( 'NONE', #20883 ) ;
#35371=DIRECTION ( 'NONE',  ( 0.000000000000000000, 0.9957341762950348008, -0.09226835946329869920 ) ) ;
#35373=CIRCLE ( 'NONE', #31220, 31.49899999999999878 ) ;
#35380=ORIENTED_EDGE ( 'NONE', *, *, #4310, .F. ) ;
#35381=DIRECTION ( 'NONE',  ( 0.000000000000000000, 0.5264321628773507289, 0.8502171357296173237 ) ) ;
#35385=ORIENTED_EDGE ( 'NONE', *, *, #248, .F. ) ;
#35388=EDGE_CURVE ( 'NONE', #32556, #23084, #35362, .T. ) ;
#35390=DIRECTION ( 'NONE',  ( 0.000000000000000000, 0.000000000000000000, 1.000000000000000000 ) ) ;
#35391=ORIENTED_EDGE ( 'NONE', *, *, #19958, .T. ) ;
#35424=DIRECTION ( 'NONE',  ( 0.000000000000000000, 0.000000000000000000, 1.000000000000000000 ) ) ;
#35442=EDGE_CURVE ( 'NONE', #28874, #13089, #26323, .T. ) ;
#35458=ORIENTED_EDGE ( 'NONE', *, *, #7549, .F. ) ;
#35459=AXIS2_PLACEMENT_3D ( 'NONE', #8536, #25171, #35371 ) ;
#35469=ORIENTED_EDGE ( 'NONE', *, *, #6314, .T. ) ;
#35474=DIRECTION ( 'NONE',  ( -1.000000000000000000, -0.000000000000000000, 0.000000000000000000 ) ) ;
#35485=ORIENTED_EDGE ( 'NONE', *, *, #35589, .F. ) ;
#35493=CARTESIAN_POINT ( 'NONE',  ( 17.99999999999999645, -31.94619804602753277, -16.59639811537389775 ) ) ;
#35527=ORIENTED_EDGE ( 'NONE', *, *, #8443, .F. ) ;
#35531=ORIENTED_EDGE ( 'NONE', *, *, #3451, .F. ) ;
#35532=DIRECTION ( 'NONE',  ( 0.000000000000000000, 0.000000000000000000, 1.000000000000000000 ) ) ;
#35537=CYLINDRICAL_SURFACE ( 'NONE', #39470, 31.49899999999999878 ) ;
#35559=AXIS2_PLACEMENT_3D ( 'NONE', #22013, #14810, #18320 ) ;
#35566=AXIS2_PLACEMENT_3D ( 'NONE', #42057, #19424, #25950 ) ;
#35576=ORIENTED_EDGE ( 'NONE', *, *, #7549, .T. ) ;
#35589=EDGE_CURVE ( 'NONE', #27630, #12333, #13814, .T. ) ;
#35592=CYLINDRICAL_SURFACE ( 'NONE', #42212, 13.60000000000000142 ) ;
#35601=AXIS2_PLACEMENT_3D ( 'NONE', #30534, #13315, #13956 ) ;
#35602=ORIENTED_EDGE ( 'NONE', *, *, #29228, .T. ) ;
#35614=EDGE_CURVE ( 'NONE', #32794, #28703, #40924, .T. ) ;
#35621=ORIENTED_EDGE ( 'NONE', *, *, #12156, .T. ) ;
#35633=CARTESIAN_POINT ( 'NONE',  ( 17.99999999999999645, -16.86122981692037825, 27.13802899033285954 ) ) ;
#35638=ORIENTED_EDGE ( 'NONE', *, *, #4379, .F. ) ;
#35647=DIRECTION ( 'NONE',  ( 1.000000000000000000, -0.000000000000000000, -0.000000000000000000 ) ) ;
#35650=VERTEX_POINT ( 'NONE', #10318 ) ;
#35651=AXIS2_PLACEMENT_3D ( 'NONE', #7433, #33830, #27095 ) ;
#35665=EDGE_CURVE ( 'NONE', #12333, #12218, #22896, .T. ) ;
#35678=EDGE_CURVE ( 'NONE', #38810, #15150, #16898, .T. ) ;
#35679=DIRECTION ( 'NONE',  ( -1.000000000000000000, 0.000000000000000000, 0.000000000000000000 ) ) ;
#35680=ORIENTED_EDGE ( 'NONE', *, *, #16440, .T. ) ;
#35697=EDGE_CURVE ( 'NONE', #12125, #1957, #43004, .T. ) ;
#35713=CARTESIAN_POINT ( 'NONE',  ( 0.000000000000000000, -18.42432724429453827, -30.92804820216021611 ) ) ;
#35723=CARTESIAN_POINT ( 'NONE',  ( 9.000000000000000000, 34.78944633786291973, -9.257128253673258200 ) ) ;
#35738=CARTESIAN_POINT ( 'NONE',  ( 17.99999999999999645, 5.822172717930716779, -31.41458249383134671 ) ) ;
#35750=CARTESIAN_POINT ( 'NONE',  ( 17.99999999999999645, -18.25486108452643208, 25.66996392254267079 ) ) ;
#35771=DIRECTION ( 'NONE',  ( 0.000000000000000000, 0.000000000000000000, 1.000000000000000000 ) ) ;
#35772=LINE ( 'NONE', #29276, #24293 ) ;
#35778=AXIS2_PLACEMENT_3D ( 'NONE', #16507, #34127, #17380 ) ;
#35784=CYLINDRICAL_SURFACE ( 'NONE', #37260, 13.59999999999999964 ) ;
#35798=VECTOR ( 'NONE', #1328, 1000.000000000000000 ) ;
#35803=ORIENTED_EDGE ( 'NONE', *, *, #24492, .F. ) ;
#35806=AXIS2_PLACEMENT_3D ( 'NONE', #18811, #29024, #32270 ) ;
#35823=CARTESIAN_POINT ( 'NONE',  ( 17.99999999999999645, 9.484061862024356415, -30.03730300138970932 ) ) ;
#35838=VERTEX_POINT ( 'NONE', #10746 ) ;
#35843=AXIS2_PLACEMENT_3D ( 'NONE', #6934, #20291, #27243 ) ;
#35844=ORIENTED_EDGE ( 'NONE', *, *, #24339, .F. ) ;
#35877=EDGE_CURVE ( 'NONE', #10311, #35149, #35772, .T. ) ;
#35900=DIRECTION ( 'NONE',  ( 1.000000000000000000, 0.000000000000000000, 0.000000000000000000 ) ) ;
#35923=AXIS2_PLACEMENT_3D ( 'NONE', #26229, #6558, #19067 ) ;
#35929=ORIENTED_EDGE ( 'NONE', *, *, #6908, .F. ) ;
#35936=CARTESIAN_POINT ( 'NONE',  ( 17.99999999999999645, 25.46650492921924425, -19.29328419707757547 ) ) ;
#35954=EDGE_LOOP ( 'NONE', ( #7176, #18396, #7265, #3522 ) ) ;
#35955=CARTESIAN_POINT ( 'NONE',  ( 0.000000000000000000, 23.87611429743662939, 20.54551452399628531 ) ) ;
#35962=CARTESIAN_POINT ( 'NONE',  ( 17.99999999999999645, -21.56073507908662634, 23.57770962728557151 ) ) ;
#35988=CARTESIAN_POINT ( 'NONE',  ( 17.99999999999999645, 7.749090474611513457, 30.53094492177216068 ) ) ;
#36003=CIRCLE ( 'NONE', #38784, 13.59999999999999787 ) ;
#36021=CYLINDRICAL_SURFACE ( 'NONE', #17598, 13.60000000000000142 ) ;
#36032=AXIS2_PLACEMENT_3D ( 'NONE', #40449, #20655, #29814 ) ;
#36033=ORIENTED_EDGE ( 'NONE', *, *, #20915, .T. ) ;
#36039=CIRCLE ( 'NONE', #7498, 31.49899999999999878 ) ;
#36044=FACE_OUTER_BOUND ( 'NONE', #2571, .T. ) ;
#36050=ORIENTED_EDGE ( 'NONE', *, *, #4701, .T. ) ;
#36055=DIRECTION ( 'NONE',  ( 0.000000000000000000, -0.3612416661871405976, -0.9324722294043605864 ) ) ;
#36058=DIRECTION ( 'NONE',  ( 0.000000000000000000, 0.000000000000000000, 1.000000000000000000 ) ) ;
#36060=DIRECTION ( 'NONE',  ( -1.000000000000000000, -0.000000000000000000, 0.000000000000000000 ) ) ;
#36061=EDGE_LOOP ( 'NONE', ( #38668, #36614, #32109, #36900 ) ) ;
#36073=VECTOR ( 'NONE', #31134, 1000.000000000000000 ) ;
#36074=DIRECTION ( 'NONE',  ( 0.000000000000000000, 0.000000000000000000, 1.000000000000000000 ) ) ;
#36087=CARTESIAN_POINT ( 'NONE',  ( 17.99999999999999645, -28.35267316522768155, -22.18391138608739155 ) ) ;
#36092=ORIENTED_EDGE ( 'NONE', *, *, #2558, .F. ) ;
#36095=ORIENTED_EDGE ( 'NONE', *, *, #35186, .T. ) ;
#36096=CARTESIAN_POINT ( 'NONE',  ( 0.000000000000000000, -31.80866420683989304, -2.997093558041628025 ) ) ;
#36108=ADVANCED_FACE ( 'NONE', ( #26852 ), #6536, .T. ) ;
#36110=CARTESIAN_POINT ( 'NONE',  ( 18.00000000000000355, 1.836970198721029589E-15, -15.00000000000000000 ) ) ;
#36111=EDGE_CURVE ( 'NONE', #990, #26550, #1939, .T. ) ;
#36140=EDGE_CURVE ( 'NONE', #26427, #16104, #41718, .T. ) ;
#36151=EDGE_LOOP ( 'NONE', ( #42033, #3789, #18683, #682 ) ) ;
#36159=EDGE_CURVE ( 'NONE', #23236, #9115, #33597, .T. ) ;
#36162=DIRECTION ( 'NONE',  ( -1.000000000000000000, 0.000000000000000000, 0.000000000000000000 ) ) ;
#36164=FACE_OUTER_BOUND ( 'NONE', #799, .T. ) ;
#36181=ORIENTED_EDGE ( 'NONE', *, *, #24496, .F. ) ;
#36195=CARTESIAN_POINT ( 'NONE',  ( 0.000000000000000000, 31.94619804602787738, -16.59639811537323340 ) ) ;
#36218=ORIENTED_EDGE ( 'NONE', *, *, #38470, .T. ) ;
#36228=DIRECTION ( 'NONE',  ( 0.000000000000000000, 0.000000000000000000, 1.000000000000000000 ) ) ;
#36231=FACE_OUTER_BOUND ( 'NONE', #26807, .T. ) ;
#36232=LINE ( 'NONE', #26017, #20764 ) ;
#36240=AXIS2_PLACEMENT_3D ( 'NONE', #38178, #11361, #30991 ) ;
#36249=DIRECTION ( 'NONE',  ( -1.000000000000000000, -0.000000000000000000, -0.000000000000000000 ) ) ;
#36255=DIRECTION ( 'NONE',  ( -1.000000000000000000, -0.000000000000000000, -0.000000000000000000 ) ) ;
#36263=DIRECTION ( 'NONE',  ( 0.000000000000000000, 0.9957341762950341346, 0.09226835946330566585 ) ) ;
#36268=VECTOR ( 'NONE', #25248, 1000.000000000000000 ) ;
#36271=AXIS2_PLACEMENT_3D ( 'NONE', #5602, #1674, #8657 ) ;
#36300=CYLINDRICAL_SURFACE ( 'NONE', #22994, 31.49899999999999878 ) ;
#36304=CIRCLE ( 'NONE', #32157, 36.00000000000000000 ) ;
#36310=CARTESIAN_POINT ( 'NONE',  ( 17.99999999999999645, 0.000000000000000000, 0.000000000000000000 ) ) ;
#36332=DIRECTION ( 'NONE',  ( 0.000000000000000000, 0.000000000000000000, 1.000000000000000000 ) ) ;
#36339=VECTOR ( 'NONE', #2821, 1000.000000000000000 ) ;
#36344=ADVANCED_FACE ( 'NONE', ( #20995 ), #1298, .T. ) ;
#36345=AXIS2_PLACEMENT_3D ( 'NONE', #17309, #20352, #40793 ) ;
#36347=CARTESIAN_POINT ( 'NONE',  ( 17.99999999999999645, 14.84191762912354839, -27.78316904333109960 ) ) ;
#36349=EDGE_CURVE ( 'NONE', #31530, #27814, #27799, .T. ) ;
#36366=AXIS2_PLACEMENT_3D ( 'NONE', #13173, #26680, #9437 ) ;
#36374=DIRECTION ( 'NONE',  ( 0.000000000000000000, 0.000000000000000000, -1.000000000000000000 ) ) ;
#36380=CYLINDRICAL_SURFACE ( 'NONE', #9469, 31.49899999999999878 ) ;
#36404=DIRECTION ( 'NONE',  ( 0.000000000000000000, 0.000000000000000000, 1.000000000000000000 ) ) ;
#36422=CYLINDRICAL_SURFACE ( 'NONE', #29399, 13.59999999999999787 ) ;
#36423=DIRECTION ( 'NONE',  ( -1.000000000000000000, 0.000000000000000000, 0.000000000000000000 ) ) ;
#36442=ADVANCED_FACE ( 'NONE', ( #29385 ), #16521, .T. ) ;
#36456=CARTESIAN_POINT ( 'NONE',  ( -10.00000000000000000, 0.000000000000000000, 0.000000000000000000 ) ) ;
#36465=DIRECTION ( 'NONE',  ( 1.000000000000000000, 0.000000000000000000, -0.000000000000000000 ) ) ;
#36470=DIRECTION ( 'NONE',  ( -1.000000000000000000, -0.000000000000000000, 0.000000000000000000 ) ) ;
#36476=ORIENTED_EDGE ( 'NONE', *, *, #36643, .F. ) ;
#36477=DIRECTION ( 'NONE',  ( -1.000000000000000000, -0.000000000000000000, -0.000000000000000000 ) ) ;
#36481=AXIS2_PLACEMENT_3D ( 'NONE', #34886, #1933, #37719 ) ;
#36484=ORIENTED_EDGE ( 'NONE', *, *, #16437, .F. ) ;
#36500=CARTESIAN_POINT ( 'NONE',  ( 0.000000000000000000, 0.000000000000000000, 0.000000000000000000 ) ) ;
#36501=ORIENTED_EDGE ( 'NONE', *, *, #19034, .F. ) ;
#36502=EDGE_CURVE ( 'NONE', #3853, #38171, #11820, .T. ) ;
#36514=EDGE_CURVE ( 'NONE', #3796, #27725, #6206, .T. ) ;
#36519=CYLINDRICAL_SURFACE ( 'NONE', #378, 13.60000000000000142 ) ;
#36520=ORIENTED_EDGE ( 'NONE', *, *, #26578, .T. ) ;
#36527=ADVANCED_FACE ( 'NONE', ( #7532 ), #3788, .T. ) ;
#36539=CARTESIAN_POINT ( 'NONE',  ( 17.99999999999999645, -18.25486108452643208, 25.66996392254267079 ) ) ;
#36540=ORIENTED_EDGE ( 'NONE', *, *, #24339, .T. ) ;
#36544=DIRECTION ( 'NONE',  ( -1.000000000000000000, 0.000000000000000000, 0.000000000000000000 ) ) ;
#36552=CIRCLE ( 'NONE', #27527, 13.60000000000000320 ) ;
#36564=ORIENTED_EDGE ( 'NONE', *, *, #11378, .F. ) ;
#36584=CARTESIAN_POINT ( 'NONE',  ( 17.99999999999999645, 2.007101075699966763, 31.43498920425970411 ) ) ;
#36586=FACE_OUTER_BOUND ( 'NONE', #3261, .T. ) ;
#36592=VERTEX_POINT ( 'NONE', #33931 ) ;
#36599=AXIS2_PLACEMENT_3D ( 'NONE', #12831, #38199, #6055 ) ;
#36611=DIRECTION ( 'NONE',  ( 0.000000000000000000, -0.6736956436465478815, -0.7390089172206675272 ) ) ;
#36612=ADVANCED_FACE ( 'NONE', ( #20233 ), #23715, .T. ) ;
#36614=ORIENTED_EDGE ( 'NONE', *, *, #35678, .F. ) ;
#36624=ORIENTED_EDGE ( 'NONE', *, *, #6788, .F. ) ;
#36641=EDGE_CURVE ( 'NONE', #3331, #38633, #18107, .T. ) ;
#36643=EDGE_CURVE ( 'NONE', #27712, #27725, #7957, .T. ) ;
#36645=CARTESIAN_POINT ( 'NONE',  ( 17.99999999999999645, -31.80866420683992857, 2.997093558041182160 ) ) ;
#36647=DIRECTION ( 'NONE',  ( -1.000000000000000000, 0.000000000000000000, -0.000000000000000000 ) ) ;
#36664=CARTESIAN_POINT ( 'NONE',  ( 8.999999999999998224, -24.70533337038204635, -26.18485254986720179 ) ) ;
#36671=ORIENTED_EDGE ( 'NONE', *, *, #19066, .T. ) ;
#36680=ORIENTED_EDGE ( 'NONE', *, *, #13407, .T. ) ;
#36705=EDGE_LOOP ( 'NONE', ( #4320, #31270, #1721, #42600 ) ) ;
#36713=EDGE_LOOP ( 'NONE', ( #21640, #42031, #33792, #29491 ) ) ;
#36715=EDGE_CURVE ( 'NONE', #35838, #31678, #28551, .T. ) ;
#36727=ORIENTED_EDGE ( 'NONE', *, *, #30085, .F. ) ;
#36739=AXIS2_PLACEMENT_3D ( 'NONE', #9946, #23295, #38973 ) ;
#36742=CARTESIAN_POINT ( 'NONE',  ( 17.99999999999999645, 5.822172717930716779, -31.41458249383134671 ) ) ;
#36754=VERTEX_POINT ( 'NONE', #11046 ) ;
#36758=CARTESIAN_POINT ( 'NONE',  ( 0.000000000000000000, 0.000000000000000000, 0.000000000000000000 ) ) ;
#36800=DIRECTION ( 'NONE',  ( 0.000000000000000000, 0.7980172272802408262, -0.6026346363792547400 ) ) ;
#36801=AXIS2_PLACEMENT_3D ( 'NONE', #16738, #26742, #39164 ) ;
#36815=CYLINDRICAL_SURFACE ( 'NONE', #7011, 13.59999999999999964 ) ;
#36837=VERTEX_POINT ( 'NONE', #12544 ) ;
#36844=ORIENTED_EDGE ( 'NONE', *, *, #4922, .F. ) ;
#36846=DIRECTION ( 'NONE',  ( -1.000000000000000000, -0.000000000000000000, 0.000000000000000000 ) ) ;
#36857=CIRCLE ( 'NONE', #5507, 31.49900000000000588 ) ;
#36858=CARTESIAN_POINT ( 'NONE',  ( 17.99999999999999645, 31.81777574834305966, -2.898764365605425830 ) ) ;
#36869=DIRECTION ( 'NONE',  ( 0.000000000000000000, 0.5264321628773568351, -0.8502171357296134380 ) ) ;
#36872=DIRECTION ( 'NONE',  ( -1.000000000000000000, -0.000000000000000000, 0.000000000000000000 ) ) ;
#36881=VECTOR ( 'NONE', #33930, 1000.000000000000000 ) ;
#36882=CARTESIAN_POINT ( 'NONE',  ( 0.000000000000000000, 0.000000000000000000, 0.000000000000000000 ) ) ;
#36883=EDGE_CURVE ( 'NONE', #4444, #24289, #6238, .T. ) ;
#36888=DIRECTION ( 'NONE',  ( 0.000000000000000000, -0.7980172272802448230, 0.6026346363792494110 ) ) ;
#36900=ORIENTED_EDGE ( 'NONE', *, *, #16811, .T. ) ;
#36904=AXIS2_PLACEMENT_3D ( 'NONE', #18766, #32025, #23294 ) ;
#36912=VERTEX_POINT ( 'NONE', #20840 ) ;
#36934=CARTESIAN_POINT ( 'NONE',  ( -10.00000000000000000, 0.000000000000000000, 0.000000000000000000 ) ) ;
#36945=ORIENTED_EDGE ( 'NONE', *, *, #33619, .T. ) ;
#36957=ORIENTED_EDGE ( 'NONE', *, *, #11710, .F. ) ;
#36966=DIRECTION ( 'NONE',  ( -1.000000000000000000, -0.000000000000000000, -0.000000000000000000 ) ) ;
#36973=EDGE_LOOP ( 'NONE', ( #8535, #21856, #16006, #29927 ) ) ;
#36978=DIRECTION ( 'NONE',  ( 0.000000000000000000, 0.000000000000000000, 1.000000000000000000 ) ) ;
#36983=AXIS2_PLACEMENT_3D ( 'NONE', #19712, #33417, #9853 ) ;
#36985=ORIENTED_EDGE ( 'NONE', *, *, #36349, .F. ) ;
#36991=PRODUCT_DEFINITION_CONTEXT ( 'detailed design', #25675, 'design' ) ;
#37003=DIRECTION ( 'NONE',  ( 0.000000000000000000, 0.000000000000000000, 1.000000000000000000 ) ) ;
#37007=AXIS2_PLACEMENT_3D ( 'NONE', #16737, #19788, #4016 ) ;
#37012=AXIS2_PLACEMENT_3D ( 'NONE', #18818, #33777, #37051 ) ;
#37024=DIRECTION ( 'NONE',  ( 0.000000000000000000, 0.000000000000000000, 1.000000000000000000 ) ) ;
#37025=DIRECTION ( 'NONE',  ( -1.000000000000000000, 0.000000000000000000, 0.000000000000000000 ) ) ;
#37029=CARTESIAN_POINT ( 'NONE',  ( 17.99999999999999645, -7.749090474611287860, -30.53094492177221397 ) ) ;
#37032=VECTOR ( 'NONE', #37147, 1000.000000000000000 ) ;
#37039=EDGE_LOOP ( 'NONE', ( #20728, #420, #28024, #16422 ) ) ;
#37044=CIRCLE ( 'NONE', #7078, 13.59999999999999787 ) ;
#37048=DIRECTION ( 'NONE',  ( -1.000000000000000000, 0.000000000000000000, 0.000000000000000000 ) ) ;
#37049=LINE ( 'NONE', #20512, #15140 ) ;
#37051=DIRECTION ( 'NONE',  ( 0.000000000000000000, 0.000000000000000000, -1.000000000000000000 ) ) ;
#37059=CARTESIAN_POINT ( 'NONE',  ( 17.99999999999999645, 34.78944633786291973, -9.257128253673256424 ) ) ;
#37068=CIRCLE ( 'NONE', #13429, 13.59999999999999787 ) ;
#37086=CARTESIAN_POINT ( 'NONE',  ( 17.99999999999999645, -16.77727049691090500, -27.19001440037564166 ) ) ;
#37092=AXIS2_PLACEMENT_3D ( 'NONE', #24729, #37986, #18841 ) ;
#37094=ORIENTED_EDGE ( 'NONE', *, *, #21503, .T. ) ;
#37112=CYLINDRICAL_SURFACE ( 'NONE', #987, 13.59999999999999964 ) ;
#37137=EDGE_CURVE ( 'NONE', #35367, #11424, #29245, .T. ) ;
#37143=VERTEX_POINT ( 'NONE', #34096 ) ;
#37144=ADVANCED_FACE ( 'NONE', ( #4182 ), #30833, .T. ) ;
#37147=DIRECTION ( 'NONE',  ( -1.000000000000000000, 0.000000000000000000, 0.000000000000000000 ) ) ;
#37148=VERTEX_POINT ( 'NONE', #4853 ) ;
#37155=CARTESIAN_POINT ( 'NONE',  ( 9.000000000000000000, -32.49609705003715732, 15.49205204337262920 ) ) ;
#37167=EDGE_CURVE ( 'NONE', #20374, #3430, #28219, .T. ) ;
#37169=( NAMED_UNIT ( * ) SI_UNIT ( $, .STERADIAN. ) SOLID_ANGLE_UNIT ( ) );
#37180=ORIENTED_EDGE ( 'NONE', *, *, #26445, .T. ) ;
#37185=VERTEX_POINT ( 'NONE', #8342 ) ;
#37206=VERTEX_POINT ( 'NONE', #22333 ) ;
#37210=CIRCLE ( 'NONE', #7938, 13.59999999999999964 ) ;
#37222=CARTESIAN_POINT ( 'NONE',  ( 8.999999999999998224, -0.6168405712489253290, 35.99471499692226217 ) ) ;
#37231=CARTESIAN_POINT ( 'NONE',  ( 0.000000000000000000, 0.000000000000000000, 0.000000000000000000 ) ) ;
#37235=FACE_OUTER_BOUND ( 'NONE', #42484, .T. ) ;
#37245=EDGE_LOOP ( 'NONE', ( #30466, #10721, #35458, #27324 ) ) ;
#37253=VECTOR ( 'NONE', #7059, 1000.000000000000000 ) ;
#37258=CARTESIAN_POINT ( 'NONE',  ( 0.000000000000000000, -7.220349212960190499, -35.26849241522671718 ) ) ;
#37260=AXIS2_PLACEMENT_3D ( 'NONE', #27850, #24377, #37631 ) ;
#37266=ORIENTED_EDGE ( 'NONE', *, *, #14062, .F. ) ;
#37281=CARTESIAN_POINT ( 'NONE',  ( 0.000000000000000000, -13.57797752207901532, -33.34124362422488730 ) ) ;
#37302=EDGE_CURVE ( 'NONE', #2224, #15863, #40386, .T. ) ;
#37314=DIRECTION ( 'NONE',  ( -1.000000000000000000, -0.000000000000000000, 0.000000000000000000 ) ) ;
#37317=CYLINDRICAL_SURFACE ( 'NONE', #33160, 13.59999999999999787 ) ;
#37369=ORIENTED_EDGE ( 'NONE', *, *, #10110, .T. ) ;
#37370=ADVANCED_FACE ( 'NONE', ( #23826 ), #13353, .T. ) ;
#37373=VERTEX_POINT ( 'NONE', #3480 ) ;
#37399=DIRECTION ( 'NONE',  ( -1.000000000000000000, 0.000000000000000000, 0.000000000000000000 ) ) ;
#37403=ORIENTED_EDGE ( 'NONE', *, *, #31759, .F. ) ;
#37409=DIRECTION ( 'NONE',  ( 0.000000000000000000, 0.000000000000000000, 1.000000000000000000 ) ) ;
#37424=AXIS2_PLACEMENT_3D ( 'NONE', #7079, #33694, #948 ) ;
#37439=ORIENTED_EDGE ( 'NONE', *, *, #41368, .F. ) ;
#37451=CIRCLE ( 'NONE', #24998, 13.59999999999999787 ) ;
#37467=CARTESIAN_POINT ( 'NONE',  ( 17.99999999999999645, 0.000000000000000000, 0.000000000000000000 ) ) ;
#37484=EDGE_LOOP ( 'NONE', ( #31013, #30284, #41452, #6236 ) ) ;
#37489=ORIENTED_EDGE ( 'NONE', *, *, #34780, .T. ) ;
#37500=ADVANCED_FACE ( 'NONE', ( #641 ), #27295, .T. ) ;
#37502=EDGE_LOOP ( 'NONE', ( #5090, #370, #16989, #32445 ) ) ;
#37508=CARTESIAN_POINT ( 'NONE',  ( 0.000000000000000000, 0.000000000000000000, 0.000000000000000000 ) ) ;
#37512=CARTESIAN_POINT ( 'NONE',  ( 17.99999999999999645, -29.68570942776464960, -10.53307442156965656 ) ) ;
#37523=DIRECTION ( 'NONE',  ( 0.000000000000000000, 0.000000000000000000, 1.000000000000000000 ) ) ;
#37531=CARTESIAN_POINT ( 'NONE',  ( 17.99999999999999645, -25.52601536738579213, -19.21447964122724272 ) ) ;
#37535=CARTESIAN_POINT ( 'NONE',  ( 0.000000000000000000, 25.52601536738619714, -19.21447964122670626 ) ) ;
#37536=ORIENTED_EDGE ( 'NONE', *, *, #24790, .F. ) ;
#37539=AXIS2_PLACEMENT_3D ( 'NONE', #37833, #35215, #31320 ) ;
#37544=CARTESIAN_POINT ( 'NONE',  ( 0.000000000000000000, 0.000000000000000000, 0.000000000000000000 ) ) ;
#37550=EDGE_CURVE ( 'NONE', #42747, #11747, #22977, .T. ) ;
#37568=EDGE_CURVE ( 'NONE', #35149, #1962, #42507, .T. ) ;
#37569=ORIENTED_EDGE ( 'NONE', *, *, #14686, .T. ) ;
#37583=EDGE_CURVE ( 'NONE', #3236, #27591, #34046, .T. ) ;
#37598=CARTESIAN_POINT ( 'NONE',  ( 0.000000000000000000, -21.48775762007876367, 23.64423737150130478 ) ) ;
#37608=ADVANCED_FACE ( 'NONE', ( #41214 ), #24925, .T. ) ;
#37613=LINE ( 'NONE', #20651, #6067 ) ;
#37616=ORIENTED_EDGE ( 'NONE', *, *, #26997, .T. ) ;
#37628=DIRECTION ( 'NONE',  ( 1.000000000000000000, 0.000000000000000000, 0.000000000000000000 ) ) ;
#37631=DIRECTION ( 'NONE',  ( 0.000000000000000000, 0.000000000000000000, 1.000000000000000000 ) ) ;
#37667=CARTESIAN_POINT ( 'NONE',  ( 17.99999999999999645, 0.000000000000000000, 0.000000000000000000 ) ) ;
#37674=DIRECTION ( 'NONE',  ( -1.000000000000000000, -0.000000000000000000, 0.000000000000000000 ) ) ;
#37675=ORIENTED_EDGE ( 'NONE', *, *, #14629, .F. ) ;
#37676=AXIS2_PLACEMENT_3D ( 'NONE', #8038, #34014, #18133 ) ;
#37677=CYLINDRICAL_SURFACE ( 'NONE', #29727, 36.00000000000000000 ) ;
#37682=VECTOR ( 'NONE', #32807, 1000.000000000000000 ) ;
#37683=EDGE_CURVE ( 'NONE', #8515, #21935, #22355, .T. ) ;
#37696=CIRCLE ( 'NONE', #35601, 13.59999999999999964 ) ;
#37700=DIRECTION ( 'NONE',  ( 0.000000000000000000, -0.9957341762950355779, 0.09226835946329130234 ) ) ;
#37703=ADVANCED_FACE ( 'NONE', ( #7638 ), #7854, .T. ) ;
#37712=AXIS2_PLACEMENT_3D ( 'NONE', #15560, #28855, #33397 ) ;
#37719=DIRECTION ( 'NONE',  ( 0.000000000000000000, 0.000000000000000000, 1.000000000000000000 ) ) ;
#37752=DIRECTION ( 'NONE',  ( 0.000000000000000000, 0.000000000000000000, 1.000000000000000000 ) ) ;
#37756=ORIENTED_EDGE ( 'NONE', *, *, #11650, .F. ) ;
#37759=DIRECTION ( 'NONE',  ( -1.000000000000000000, 0.000000000000000000, 0.000000000000000000 ) ) ;
#37774=FACE_OUTER_BOUND ( 'NONE', #16844, .T. ) ;
#37780=CARTESIAN_POINT ( 'NONE',  ( 0.000000000000000000, 31.94619804602764290, 16.59639811537368814 ) ) ;
#37792=EDGE_CURVE ( 'NONE', #5751, #42039, #38811, .T. ) ;
#37793=EDGE_CURVE ( 'NONE', #20704, #28489, #20265, .T. ) ;
#37799=DIRECTION ( 'NONE',  ( 0.000000000000000000, 0.000000000000000000, 1.000000000000000000 ) ) ;
#37800=FACE_OUTER_BOUND ( 'NONE', #20469, .T. ) ;
#37801=DIRECTION ( 'NONE',  ( -1.000000000000000000, -0.000000000000000000, -0.000000000000000000 ) ) ;
#37804=AXIS2_PLACEMENT_3D ( 'NONE', #10228, #13748, #27052 ) ;
#37826=CARTESIAN_POINT ( 'NONE',  ( 0.000000000000000000, 32.49609705003704363, 15.49205204337285657 ) ) ;
#37832=ORIENTED_EDGE ( 'NONE', *, *, #14006, .T. ) ;
#37833=CARTESIAN_POINT ( 'NONE',  ( 17.99999999999999645, 5.822172717930266472, 31.41458249383143198 ) ) ;
#37834=ORIENTED_EDGE ( 'NONE', *, *, #36514, .F. ) ;
#37836=CARTESIAN_POINT ( 'NONE',  ( 0.000000000000000000, 0.6168405712486755288, 35.99471499692226928 ) ) ;
#37840=DIRECTION ( 'NONE',  ( -1.000000000000000000, 0.000000000000000000, 0.000000000000000000 ) ) ;
#37845=CARTESIAN_POINT ( 'NONE',  ( 17.99999999999999645, 30.71634675606053833, 8.790889055186667633 ) ) ;
#37873=DIRECTION ( 'NONE',  ( 0.000000000000000000, 0.9618256431728199329, -0.2736629900720800590 ) ) ;
#37874=ORIENTED_EDGE ( 'NONE', *, *, #21615, .F. ) ;
#37875=CIRCLE ( 'NONE', #7226, 13.59999999999999787 ) ;
#37876=DIRECTION ( 'NONE',  ( -1.000000000000000000, 0.000000000000000000, -0.000000000000000000 ) ) ;
#37891=CARTESIAN_POINT ( 'NONE',  ( 17.99999999999999645, 18.25486108452625089, 25.66996392254279868 ) ) ;
#37895=ORIENTED_EDGE ( 'NONE', *, *, #39060, .T. ) ;
#37896=LINE ( 'NONE', #32224, #294 ) ;
#37897=ORIENTED_EDGE ( 'NONE', *, *, #36641, .T. ) ;
#37916=FACE_OUTER_BOUND ( 'NONE', #17220, .T. ) ;
#37925=AXIS2_PLACEMENT_3D ( 'NONE', #33542, #23759, #33756 ) ;
#37927=EDGE_CURVE ( 'NONE', #23084, #42317, #33128, .T. ) ;
#37930=EDGE_CURVE ( 'NONE', #25212, #606, #24442, .T. ) ;
#37936=VECTOR ( 'NONE', #42937, 1000.000000000000000 ) ;
#37952=DIRECTION ( 'NONE',  ( 0.000000000000000000, -0.9957341762950334685, -0.09226835946331299332 ) ) ;
#37960=AXIS2_PLACEMENT_3D ( 'NONE', #24136, #17387, #738 ) ;
#37980=VECTOR ( 'NONE', #6480, 1000.000000000000000 ) ;
#37986=DIRECTION ( 'NONE',  ( -1.000000000000000000, 0.000000000000000000, 0.000000000000000000 ) ) ;
#37991=CARTESIAN_POINT ( 'NONE',  ( 17.99999999999999645, -0.6168405712489235526, 35.99471499692226928 ) ) ;
#37996=ORIENTED_EDGE ( 'NONE', *, *, #19396, .T. ) ;
#38000=ORIENTED_EDGE ( 'NONE', *, *, #23595, .T. ) ;
#38006=CIRCLE ( 'NONE', #33835, 13.60000000000000142 ) ;
#38007=DIRECTION ( 'NONE',  ( 0.000000000000000000, 0.7980172272802363853, 0.6026346363792605132 ) ) ;
#38011=EDGE_CURVE ( 'NONE', #606, #41289, #639, .T. ) ;
#38017=CARTESIAN_POINT ( 'NONE',  ( 18.00000000000000355, 0.000000000000000000, 0.000000000000000000 ) ) ;
#38024=AXIS2_PLACEMENT_3D ( 'NONE', #35154, #5274, #18642 ) ;
#38043=VECTOR ( 'NONE', #14610, 1000.000000000000000 ) ;
#38044=AXIS2_PLACEMENT_3D ( 'NONE', #19018, #22500, #15946 ) ;
#38049=DIRECTION ( 'NONE',  ( 1.000000000000000000, 0.000000000000000000, 0.000000000000000000 ) ) ;
#38060=VECTOR ( 'NONE', #14430, 1000.000000000000000 ) ;
#38062=DIRECTION ( 'NONE',  ( 0.000000000000000000, -0.1837495178165569620, -0.9829730996839042279 ) ) ;
#38073=DIRECTION ( 'NONE',  ( 1.000000000000000000, 0.000000000000000000, 0.000000000000000000 ) ) ;
#38078=ORIENTED_EDGE ( 'NONE', *, *, #10436, .T. ) ;
#38080=VECTOR ( 'NONE', #40816, 1000.000000000000000 ) ;
#38101=ORIENTED_EDGE ( 'NONE', *, *, #21468, .F. ) ;
#38103=DIRECTION ( 'NONE',  ( -1.000000000000000000, -0.000000000000000000, -0.000000000000000000 ) ) ;
#38106=VERTEX_POINT ( 'NONE', #4519 ) ;
#38116=ADVANCED_FACE ( 'NONE', ( #3858 ), #4754, .T. ) ;
#38127=CARTESIAN_POINT ( 'NONE',  ( 0.000000000000000000, 23.79363200506992015, -27.01597816121622486 ) ) ;
#38136=DIRECTION ( 'NONE',  ( 0.000000000000000000, 0.000000000000000000, 1.000000000000000000 ) ) ;
#38140=ORIENTED_EDGE ( 'NONE', *, *, #9121, .F. ) ;
#38155=AXIS2_PLACEMENT_3D ( 'NONE', #38542, #15469, #31382 ) ;
#38159=ORIENTED_EDGE ( 'NONE', *, *, #33140, .F. ) ;
#38171=VERTEX_POINT ( 'NONE', #37258 ) ;
#38173=VERTEX_POINT ( 'NONE', #38127 ) ;
#38177=ORIENTED_EDGE ( 'NONE', *, *, #15690, .T. ) ;
#38178=CARTESIAN_POINT ( 'NONE',  ( 17.99999999999999645, 0.000000000000000000, 0.000000000000000000 ) ) ;
#38187=VERTEX_POINT ( 'NONE', #30941 ) ;
#38188=DIRECTION ( 'NONE',  ( -1.000000000000000000, 0.000000000000000000, 0.000000000000000000 ) ) ;
#38190=CARTESIAN_POINT ( 'NONE',  ( 17.99999999999999645, 27.24480646643629811, -15.80846360676556372 ) ) ;
#38191=DIRECTION ( 'NONE',  ( -1.000000000000000000, 0.000000000000000000, 0.000000000000000000 ) ) ;
#38194=CARTESIAN_POINT ( 'NONE',  ( 17.99999999999999645, 16.86122981692056655, -27.13802899033274940 ) ) ;
#38199=DIRECTION ( 'NONE',  ( -1.000000000000000000, -0.000000000000000000, 0.000000000000000000 ) ) ;
#38208=DIRECTION ( 'NONE',  ( -1.000000000000000000, 0.000000000000000000, 0.000000000000000000 ) ) ;
#38214=DIRECTION ( 'NONE',  ( -1.000000000000000000, -0.000000000000000000, 0.000000000000000000 ) ) ;
#38217=ADVANCED_FACE ( 'NONE', ( #40955 ), #8250, .T. ) ;
#38219=FACE_OUTER_BOUND ( 'NONE', #32567, .T. ) ;
#38229=AXIS2_PLACEMENT_3D ( 'NONE', #33765, #16184, #23612 ) ;
#38231=ORIENTED_EDGE ( 'NONE', *, *, #36111, .T. ) ;
#38242=ORIENTED_EDGE ( 'NONE', *, *, #16705, .T. ) ;
#38250=ADVANCED_FACE ( 'NONE', ( #28345 ), #5608, .T. ) ;
#38266=DIRECTION ( 'NONE',  ( 0.000000000000000000, 0.000000000000000000, 1.000000000000000000 ) ) ;
#38271=ORIENTED_EDGE ( 'NONE', *, *, #5736, .F. ) ;
#38274=ORIENTED_EDGE ( 'NONE', *, *, #34813, .T. ) ;
#38281=CARTESIAN_POINT ( 'NONE',  ( 17.99999999999999645, -25.52601536738605859, 19.21447964122688390 ) ) ;
#38304=DIRECTION ( 'NONE',  ( 0.000000000000000000, -0.8951632913550571224, -0.4457383557765488002 ) ) ;
#38317=AXIS2_PLACEMENT_3D ( 'NONE', #11202, #14916, #4399 ) ;
#38319=ORIENTED_EDGE ( 'NONE', *, *, #2222, .T. ) ;
#38322=CARTESIAN_POINT ( 'NONE',  ( 8.999999999999998224, -31.94619804602753277, -16.59639811537390131 ) ) ;
#38340=EDGE_CURVE ( 'NONE', #5647, #8178, #6946, .T. ) ;
#38361=VERTEX_POINT ( 'NONE', #2734 ) ;
#38374=CIRCLE ( 'NONE', #30734, 31.49899999999999878 ) ;
#38387=DIRECTION ( 'NONE',  ( 0.000000000000000000, 0.000000000000000000, 1.000000000000000000 ) ) ;
#38396=ORIENTED_EDGE ( 'NONE', *, *, #29294, .F. ) ;
#38404=EDGE_LOOP ( 'NONE', ( #35576, #40529, #37266, #20626 ) ) ;
#38409=VERTEX_POINT ( 'NONE', #39613 ) ;
#38426=ORIENTED_EDGE ( 'NONE', *, *, #33708, .F. ) ;
#38427=AXIS2_PLACEMENT_3D ( 'NONE', #8556, #24757, #2003 ) ;
#38428=ORIENTED_EDGE ( 'NONE', *, *, #4138, .F. ) ;
#38432=EDGE_LOOP ( 'NONE', ( #7600, #13191, #3208, #29698 ) ) ;
#38433=CARTESIAN_POINT ( 'NONE',  ( 17.99999999999999645, 29.03409033315581667, 12.21509719675401051 ) ) ;
#38470=EDGE_CURVE ( 'NONE', #20449, #20287, #9043, .T. ) ;
#38478=ADVANCED_BREP_SHAPE_REPRESENTATION ( '', ( #13741, #13552 ), #32277 ) ;
#38479=ORIENTED_EDGE ( 'NONE', *, *, #34813, .F. ) ;
#38500=CARTESIAN_POINT ( 'NONE',  ( 0.000000000000000000, 27.24480646643607074, 15.80846360676594564 ) ) ;
#38502=EDGE_CURVE ( 'NONE', #11159, #38585, #12552, .T. ) ;
#38504=DIRECTION ( 'NONE',  ( -1.000000000000000000, -0.000000000000000000, -0.000000000000000000 ) ) ;
#38519=CARTESIAN_POINT ( 'NONE',  ( 0.000000000000000000, -11.58753559615464290, -29.77419532459275331 ) ) ;
#38526=DIRECTION ( 'NONE',  ( -1.000000000000000000, 0.000000000000000000, 0.000000000000000000 ) ) ;
#38534=CYLINDRICAL_SURFACE ( 'NONE', #35559, 13.60000000000000142 ) ;
#38542=CARTESIAN_POINT ( 'NONE',  ( 17.99999999999999645, 0.000000000000000000, 0.000000000000000000 ) ) ;
#38552=EDGE_CURVE ( 'NONE', #23356, #10153, #25218, .T. ) ;
#38566=CARTESIAN_POINT ( 'NONE',  ( 0.000000000000000000, 30.78424799127077094, -6.672111855472859787 ) ) ;
#38567=AXIS2_PLACEMENT_3D ( 'NONE', #32767, #41940, #35183 ) ;
#38582=CARTESIAN_POINT ( 'NONE',  ( 0.000000000000000000, -2.007101075699733173, -31.43498920425971832 ) ) ;
#38585=VERTEX_POINT ( 'NONE', #28486 ) ;
#38593=CARTESIAN_POINT ( 'NONE',  ( 17.99999999999999645, -30.71634675606047793, -8.790889055186887902 ) ) ;
#38605=CIRCLE ( 'NONE', #6552, 13.59999999999999964 ) ;
#38606=EDGE_CURVE ( 'NONE', #17796, #10741, #25135, .T. ) ;
#38612=CARTESIAN_POINT ( 'NONE',  ( 0.000000000000000000, -28.57802095670076881, -14.28532136906702732 ) ) ;
#38617=AXIS2_PLACEMENT_3D ( 'NONE', #38194, #14887, #27763 ) ;
#38624=DIRECTION ( 'NONE',  ( 0.000000000000000000, 0.000000000000000000, 1.000000000000000000 ) ) ;
#38626=CIRCLE ( 'NONE', #17789, 13.59999999999999964 ) ;
#38630=CYLINDRICAL_SURFACE ( 'NONE', #29912, 36.00000000000000000 ) ;
#38633=VERTEX_POINT ( 'NONE', #39948 ) ;
#38647=CARTESIAN_POINT ( 'NONE',  ( 17.99999999999999645, 0.000000000000000000, 0.000000000000000000 ) ) ;
#38657=EDGE_CURVE ( 'NONE', #23539, #33268, #11135, .T. ) ;
#38659=CIRCLE ( 'NONE', #15716, 13.59999999999999964 ) ;
#38668=ORIENTED_EDGE ( 'NONE', *, *, #15076, .F. ) ;
#38672=AXIS2_PLACEMENT_3D ( 'NONE', #20179, #40181, #13184 ) ;
#38674=ORIENTED_EDGE ( 'NONE', *, *, #13459, .F. ) ;
#38679=DIRECTION ( 'NONE',  ( 0.000000000000000000, 0.000000000000000000, 1.000000000000000000 ) ) ;
#38687=EDGE_CURVE ( 'NONE', #24756, #6694, #40690, .T. ) ;
#38695=AXIS2_PLACEMENT_3D ( 'NONE', #40379, #34280, #31015 ) ;
#38696=ORIENTED_EDGE ( 'NONE', *, *, #25007, .F. ) ;
#38697=AXIS2_PLACEMENT_3D ( 'NONE', #38519, #31793, #8641 ) ;
#38707=EDGE_LOOP ( 'NONE', ( #17390, #19942, #14852, #7581 ) ) ;
#38721=CIRCLE ( 'NONE', #29680, 31.49899999999999878 ) ;
#38733=VECTOR ( 'NONE', #14007, 1000.000000000000000 ) ;
#38734=DIRECTION ( 'NONE',  ( -1.000000000000000000, -0.000000000000000000, -0.000000000000000000 ) ) ;
#38735=ADVANCED_FACE ( 'NONE', ( #23011 ), #30764, .T. ) ;
#38745=DIRECTION ( 'NONE',  ( 0.000000000000000000, -0.3612416661871405421, -0.9324722294043605864 ) ) ;
#38752=CIRCLE ( 'NONE', #41521, 36.00000000000000000 ) ;
#38762=DIRECTION ( 'NONE',  ( -1.000000000000000000, 0.000000000000000000, 0.000000000000000000 ) ) ;
#38767=EDGE_LOOP ( 'NONE', ( #33579, #23406, #2358, #27702 ) ) ;
#38784=AXIS2_PLACEMENT_3D ( 'NONE', #24350, #27825, #31300 ) ;
#38810=VERTEX_POINT ( 'NONE', #33220 ) ;
#38811=LINE ( 'NONE', #19015, #39021 ) ;
#38817=AXIS2_PLACEMENT_3D ( 'NONE', #27326, #11183, #14464 ) ;
#38852=CARTESIAN_POINT ( 'NONE',  ( 0.000000000000000000, 0.000000000000000000, 0.000000000000000000 ) ) ;
#38866=DIRECTION ( 'NONE',  ( 0.000000000000000000, 0.000000000000000000, 1.000000000000000000 ) ) ;
#38884=EDGE_CURVE ( 'NONE', #12837, #29515, #5002, .T. ) ;
#38886=AXIS2_PLACEMENT_3D ( 'NONE', #26053, #9452, #27 ) ;
#38899=DIRECTION ( 'NONE',  ( -1.000000000000000000, 0.000000000000000000, 0.000000000000000000 ) ) ;
#38907=CIRCLE ( 'NONE', #24328, 13.59999999999999964 ) ;
#38938=ORIENTED_EDGE ( 'NONE', *, *, #4487, .F. ) ;
#38944=CARTESIAN_POINT ( 'NONE',  ( 17.99999999999999645, 25.46650492921896713, 19.29328419707794495 ) ) ;
#38953=CYLINDRICAL_SURFACE ( 'NONE', #42946, 13.60000000000000142 ) ;
#38967=ORIENTED_EDGE ( 'NONE', *, *, #38470, .F. ) ;
#38973=DIRECTION ( 'NONE',  ( 0.000000000000000000, 0.000000000000000000, -1.000000000000000000 ) ) ;
#38975=CARTESIAN_POINT ( 'NONE',  ( 17.99999999999999645, 0.000000000000000000, 0.000000000000000000 ) ) ;
#38977=CARTESIAN_POINT ( 'NONE',  ( 0.000000000000000000, 16.77727049691149475, -27.19001440037526862 ) ) ;
#39001=FACE_OUTER_BOUND ( 'NONE', #22668, .T. ) ;
#39013=ORIENTED_EDGE ( 'NONE', *, *, #23934, .T. ) ;
#39019=CIRCLE ( 'NONE', #6294, 13.60000000000000142 ) ;
#39021=VECTOR ( 'NONE', #25342, 1000.000000000000000 ) ;
#39045=AXIS2_PLACEMENT_3D ( 'NONE', #15825, #22600, #31973 ) ;
#39047=CARTESIAN_POINT ( 'NONE',  ( 0.000000000000000000, -16.86122981692000167, -27.13802899033310112 ) ) ;
#39049=CIRCLE ( 'NONE', #13312, 13.59999999999999964 ) ;
#39055=DIRECTION ( 'NONE',  ( 0.000000000000000000, 0.000000000000000000, -1.000000000000000000 ) ) ;
#39056=ORIENTED_EDGE ( 'NONE', *, *, #19227, .T. ) ;
#39060=EDGE_CURVE ( 'NONE', #25006, #33094, #14017, .T. ) ;
#39062=DIRECTION ( 'NONE',  ( 0.000000000000000000, 0.3612416661871538093, -0.9324722294043554793 ) ) ;
#39070=CYLINDRICAL_SURFACE ( 'NONE', #2418, 13.59999999999999964 ) ;
#39072=CYLINDRICAL_SURFACE ( 'NONE', #17584, 36.00000000000000000 ) ;
#39078=DIRECTION ( 'NONE',  ( -1.000000000000000000, 0.000000000000000000, 0.000000000000000000 ) ) ;
#39086=ADVANCED_FACE ( 'NONE', ( #11523 ), #38534, .T. ) ;
#39089=ORIENTED_EDGE ( 'NONE', *, *, #8496, .T. ) ;
#39105=DIRECTION ( 'NONE',  ( 0.000000000000000000, 0.000000000000000000, 1.000000000000000000 ) ) ;
#39114=EDGE_CURVE ( 'NONE', #10741, #10211, #41607, .T. ) ;
#39128=DIRECTION ( 'NONE',  ( -1.000000000000000000, 0.000000000000000000, 0.000000000000000000 ) ) ;
#39138=ORIENTED_EDGE ( 'NONE', *, *, #31466, .F. ) ;
#39164=DIRECTION ( 'NONE',  ( 0.000000000000000000, 0.000000000000000000, 1.000000000000000000 ) ) ;
#39168=CIRCLE ( 'NONE', #37092, 31.49899999999999878 ) ;
#39174=ORIENTED_EDGE ( 'NONE', *, *, #19091, .T. ) ;
#39177=DIRECTION ( 'NONE',  ( -1.000000000000000000, 0.000000000000000000, 0.000000000000000000 ) ) ;
#39202=CIRCLE ( 'NONE', #25318, 36.00000000000000000 ) ;
#39218=EDGE_CURVE ( 'NONE', #14987, #8291, #20988, .T. ) ;
#39228=ORIENTED_EDGE ( 'NONE', *, *, #3084, .F. ) ;
#39235=DIRECTION ( 'NONE',  ( 0.000000000000000000, 0.000000000000000000, 1.000000000000000000 ) ) ;
#39242=VERTEX_POINT ( 'NONE', #36539 ) ;
#39244=AXIS2_PLACEMENT_3D ( 'NONE', #29788, #24502, #37752 ) ;
#39246=FACE_OUTER_BOUND ( 'NONE', #31106, .T. ) ;
#39253=CARTESIAN_POINT ( 'NONE',  ( -10.00000000000000000, 0.000000000000000000, 0.000000000000000000 ) ) ;
#39256=ORIENTED_EDGE ( 'NONE', *, *, #3271, .F. ) ;
#39257=DIRECTION ( 'NONE',  ( -1.000000000000000000, -0.000000000000000000, -0.000000000000000000 ) ) ;
#39259=ORIENTED_EDGE ( 'NONE', *, *, #6523, .F. ) ;
#39263=ORIENTED_EDGE ( 'NONE', *, *, #6907, .F. ) ;
#39277=FACE_OUTER_BOUND ( 'NONE', #21620, .T. ) ;
#39278=CARTESIAN_POINT ( 'NONE',  ( 17.99999999999999645, -0.04937522221101428577, -31.94951095880159286 ) ) ;
#39301=DIRECTION ( 'NONE',  ( -1.000000000000000000, 0.000000000000000000, 0.000000000000000000 ) ) ;
#39303=CARTESIAN_POINT ( 'NONE',  ( 17.99999999999999645, 7.749090474611513457, 30.53094492177216068 ) ) ;
#39312=DIRECTION ( 'NONE',  ( -1.000000000000000000, -0.000000000000000000, -0.000000000000000000 ) ) ;
#39317=DIRECTION ( 'NONE',  ( -1.000000000000000000, 0.000000000000000000, 0.000000000000000000 ) ) ;
#39333=AXIS2_PLACEMENT_3D ( 'NONE', #29722, #40369, #33616 ) ;
#39342=AXIS2_PLACEMENT_3D ( 'NONE', #6651, #26529, #40451 ) ;
#39347=EDGE_CURVE ( 'NONE', #16681, #42378, #4025, .T. ) ;
#39350=VERTEX_POINT ( 'NONE', #33937 ) ;
#39351=EDGE_CURVE ( 'NONE', #26484, #38810, #21710, .T. ) ;
#39354=DIRECTION ( 'NONE',  ( 0.000000000000000000, 0.000000000000000000, -1.000000000000000000 ) ) ;
#39361=CIRCLE ( 'NONE', #7295, 13.60000000000000142 ) ;
#39379=VERTEX_POINT ( 'NONE', #34147 ) ;
#39386=VERTEX_POINT ( 'NONE', #40669 ) ;
#39409=AXIS2_PLACEMENT_3D ( 'NONE', #4381, #2918, #42637 ) ;
#39410=EDGE_CURVE ( 'NONE', #5566, #10311, #16834, .T. ) ;
#39412=CIRCLE ( 'NONE', #1805, 13.59999999999999787 ) ;
#39424=CARTESIAN_POINT ( 'NONE',  ( 17.99999999999999645, -31.11570115861491814, -4.898994019976963266 ) ) ;
#39426=CYLINDRICAL_SURFACE ( 'NONE', #33868, 13.60000000000000142 ) ;
#39432=AXIS2_PLACEMENT_3D ( 'NONE', #36742, #40436, #39996 ) ;
#39434=CYLINDRICAL_SURFACE ( 'NONE', #39583, 36.00000000000000000 ) ;
#39439=CARTESIAN_POINT ( 'NONE',  ( 0.000000000000000000, 13.57797752207923381, 33.34124362422479493 ) ) ;
#39461=SHAPE_DEFINITION_REPRESENTATION ( #20401, #40225 ) ;
#39470=AXIS2_PLACEMENT_3D ( 'NONE', #5018, #35331, #38387 ) ;
#39472=DIRECTION ( 'NONE',  ( -1.000000000000000000, 0.000000000000000000, 0.000000000000000000 ) ) ;
#39473=EDGE_CURVE ( 'NONE', #7715, #26178, #16133, .T. ) ;
#39485=ORIENTED_EDGE ( 'NONE', *, *, #16440, .F. ) ;
#39488=AXIS2_PLACEMENT_3D ( 'NONE', #21034, #14896, #11616 ) ;
#39512=CARTESIAN_POINT ( 'NONE',  ( 17.99999999999999645, 12.42760411676086996, -33.78690065568411427 ) ) ;
#39535=ORIENTED_EDGE ( 'NONE', *, *, #16347, .F. ) ;
#39537=DIRECTION ( 'NONE',  ( -1.000000000000000000, 0.000000000000000000, -0.000000000000000000 ) ) ;
#39539=DIRECTION ( 'NONE',  ( 0.000000000000000000, 0.1837495178165706178, -0.9829730996839017854 ) ) ;
#39552=CARTESIAN_POINT ( 'NONE',  ( 17.99999999999999645, -32.49609705003715732, 15.49205204337262565 ) ) ;
#39574=VERTEX_POINT ( 'NONE', #11475 ) ;
#39583=AXIS2_PLACEMENT_3D ( 'NONE', #16794, #13291, #29879 ) ;
#39588=DIRECTION ( 'NONE',  ( 0.000000000000000000, 0.000000000000000000, 1.000000000000000000 ) ) ;
#39589=ORIENTED_EDGE ( 'NONE', *, *, #24667, .F. ) ;
#39610=CYLINDRICAL_SURFACE ( 'NONE', #30333, 31.49899999999999878 ) ;
#39613=CARTESIAN_POINT ( 'NONE',  ( 0.000000000000000000, 29.09613215194512748, -21.19941258140292106 ) ) ;
#39620=ORIENTED_EDGE ( 'NONE', *, *, #12156, .F. ) ;
#39624=CARTESIAN_POINT ( 'NONE',  ( -10.00000000000000000, 0.000000000000000000, 0.000000000000000000 ) ) ;
#39627=EDGE_CURVE ( 'NONE', #26154, #19383, #23129, .T. ) ;
#39631=VERTEX_POINT ( 'NONE', #25869 ) ;
#39642=ORIENTED_EDGE ( 'NONE', *, *, #19396, .F. ) ;
#39646=AXIS2_PLACEMENT_3D ( 'NONE', #27784, #27333, #34082 ) ;
#39649=ORIENTED_EDGE ( 'NONE', *, *, #14600, .T. ) ;
#39652=EDGE_CURVE ( 'NONE', #27819, #33813, #31448, .T. ) ;
#39657=EDGE_CURVE ( 'NONE', #22441, #27845, #3100, .T. ) ;
#39662=CYLINDRICAL_SURFACE ( 'NONE', #19319, 31.49899999999999878 ) ;
#39668=VERTEX_POINT ( 'NONE', #5758 ) ;
#39688=AXIS2_PLACEMENT_3D ( 'NONE', #30272, #4275, #14350 ) ;
#39690=AXIS2_PLACEMENT_3D ( 'NONE', #6984, #20341, #33824 ) ;
#39694=EDGE_CURVE ( 'NONE', #33164, #13228, #28655, .T. ) ;
#39699=EDGE_CURVE ( 'NONE', #39242, #6807, #39752, .T. ) ;
#39710=CARTESIAN_POINT ( 'NONE',  ( 0.000000000000000000, -11.58753559615507100, 29.77419532459258278 ) ) ;
#39724=AXIS2_PLACEMENT_3D ( 'NONE', #21212, #34254, #4349 ) ;
#39744=DIRECTION ( 'NONE',  ( -1.000000000000000000, -0.000000000000000000, -0.000000000000000000 ) ) ;
#39748=CYLINDRICAL_SURFACE ( 'NONE', #38886, 13.59999999999999964 ) ;
#39752=CIRCLE ( 'NONE', #21021, 13.59999999999999964 ) ;
#39756=CIRCLE ( 'NONE', #14020, 15.00000000000000000 ) ;
#39765=ORIENTED_EDGE ( 'NONE', *, *, #11710, .T. ) ;
#39785=EDGE_CURVE ( 'NONE', #30670, #35008, #3976, .T. ) ;
#39815=CARTESIAN_POINT ( 'NONE',  ( 0.000000000000000000, 25.46650492921924425, -19.29328419707757547 ) ) ;
#39817=DIRECTION ( 'NONE',  ( 0.000000000000000000, 0.7980172272802408262, -0.6026346363792547400 ) ) ;
#39837=ADVANCED_FACE ( 'NONE', ( #26704 ), #16914, .T. ) ;
#39856=EDGE_CURVE ( 'NONE', #4224, #22493, #6836, .T. ) ;
#39860=ORIENTED_EDGE ( 'NONE', *, *, #5364, .F. ) ;
#39863=ORIENTED_EDGE ( 'NONE', *, *, #8240, .T. ) ;
#39883=CARTESIAN_POINT ( 'NONE',  ( 17.99999999999999645, -13.57797752207947006, 33.34124362422470256 ) ) ;
#39896=CYLINDRICAL_SURFACE ( 'NONE', #43008, 31.49899999999999878 ) ;
#39901=ORIENTED_EDGE ( 'NONE', *, *, #6907, .T. ) ;
#39904=CARTESIAN_POINT ( 'NONE',  ( 0.000000000000000000, -31.80866420683992857, 16.59709355804118402 ) ) ;
#39908=ORIENTED_EDGE ( 'NONE', *, *, #7476, .F. ) ;
#39912=AXIS2_PLACEMENT_3D ( 'NONE', #18079, #21572, #14995 ) ;
#39916=ORIENTED_EDGE ( 'NONE', *, *, #7410, .F. ) ;
#39924=DIRECTION ( 'NONE',  ( -1.000000000000000000, -0.000000000000000000, -0.000000000000000000 ) ) ;
#39926=AXIS2_PLACEMENT_3D ( 'NONE', #31880, #38191, #1967 ) ;
#39932=ORIENTED_EDGE ( 'NONE', *, *, #21061, .F. ) ;
#39948=CARTESIAN_POINT ( 'NONE',  ( 17.99999999999999645, -7.220349212960696761, 35.26849241522662481 ) ) ;
#39954=EDGE_CURVE ( 'NONE', #4807, #7922, #15464, .T. ) ;
#39956=CARTESIAN_POINT ( 'NONE',  ( 17.99999999999999645, 22.66088087769180603, 21.87856208362564914 ) ) ;
#39960=CARTESIAN_POINT ( 'NONE',  ( 17.99999999999999645, -28.62203781743013664, 14.19692359621445199 ) ) ;
#39968=ORIENTED_EDGE ( 'NONE', *, *, #41605, .T. ) ;
#39971=ORIENTED_EDGE ( 'NONE', *, *, #33377, .T. ) ;
#39979=ORIENTED_EDGE ( 'NONE', *, *, #21615, .T. ) ;
#39983=SHAPE_REPRESENTATION_RELATIONSHIP ( 'NONE' , 'NONE' ,  #40225, #38478 ) ;
#39992=DIRECTION ( 'NONE',  ( 0.000000000000000000, 0.000000000000000000, 1.000000000000000000 ) ) ;
#39996=DIRECTION ( 'NONE',  ( 0.000000000000000000, 0.000000000000000000, 1.000000000000000000 ) ) ;
#40012=VECTOR ( 'NONE', #32653, 1000.000000000000000 ) ;
#40030=CARTESIAN_POINT ( 'NONE',  ( 17.99999999999999645, -6.007673836297749759, -35.49518073030004217 ) ) ;
#40038=DIRECTION ( 'NONE',  ( -1.000000000000000000, 0.000000000000000000, 0.000000000000000000 ) ) ;
#40041=ADVANCED_FACE ( 'NONE', ( #42351 ), #39072, .T. ) ;
#40047=CARTESIAN_POINT ( 'NONE',  ( 0.000000000000000000, -5.919241748379376666, -31.39643714728462953 ) ) ;
#40051=CARTESIAN_POINT ( 'NONE',  ( 17.99999999999999645, -22.66088087769164972, -21.87856208362581256 ) ) ;
#40062=VERTEX_POINT ( 'NONE', #25392 ) ;
#40084=AXIS2_PLACEMENT_3D ( 'NONE', #36858, #22161, #12098 ) ;
#40095=ORIENTED_EDGE ( 'NONE', *, *, #13272, .F. ) ;
#40108=EDGE_CURVE ( 'NONE', #42317, #26674, #32155, .T. ) ;
#40114=AXIS2_PLACEMENT_3D ( 'NONE', #40791, #10948, #36888 ) ;
#40115=ORIENTED_EDGE ( 'NONE', *, *, #40677, .F. ) ;
#40124=ORIENTED_EDGE ( 'NONE', *, *, #40432, .T. ) ;
#40127=ORIENTED_EDGE ( 'NONE', *, *, #11703, .T. ) ;
#40131=DIRECTION ( 'NONE',  ( -1.000000000000000000, -0.000000000000000000, -0.000000000000000000 ) ) ;
#40138=EDGE_CURVE ( 'NONE', #15922, #4444, #12696, .T. ) ;
#40143=CARTESIAN_POINT ( 'NONE',  ( 0.000000000000000000, -21.48775762007842260, -23.64423737150161031 ) ) ;
#40149=CARTESIAN_POINT ( 'NONE',  ( 17.99999999999999645, -26.29521155129861398, 17.34211205339337880 ) ) ;
#40160=DIRECTION ( 'NONE',  ( -1.000000000000000000, -0.000000000000000000, -0.000000000000000000 ) ) ;
#40170=CIRCLE ( 'NONE', #34621, 13.59999999999999964 ) ;
#40175=DIRECTION ( 'NONE',  ( 0.000000000000000000, 0.000000000000000000, 1.000000000000000000 ) ) ;
#40181=DIRECTION ( 'NONE',  ( -1.000000000000000000, -0.000000000000000000, -0.000000000000000000 ) ) ;
#40185=ORIENTED_EDGE ( 'NONE', *, *, #33377, .F. ) ;
#40204=CIRCLE ( 'NONE', #36032, 13.59999999999999787 ) ;
#40205=CARTESIAN_POINT ( 'NONE',  ( 9.000000000000000000, 18.42432724429473012, 30.92804820216009176 ) ) ;
#40225=SHAPE_REPRESENTATION ( 'spur gear_iso_ISO - Spur gear 2M 34T 20PA 18FW ---S34A75H50L30.0N', ( #13552 ), #32277 ) ;
#40230=DIRECTION ( 'NONE',  ( 0.000000000000000000, -0.9618256431728159361, -0.2736629900720938813 ) ) ;
#40232=CARTESIAN_POINT ( 'NONE',  ( -10.00000000000000000, 0.000000000000000000, 0.000000000000000000 ) ) ;
#40240=DIRECTION ( 'NONE',  ( 0.000000000000000000, 0.000000000000000000, 1.000000000000000000 ) ) ;
#40245=DIRECTION ( 'NONE',  ( -1.000000000000000000, -0.000000000000000000, 0.000000000000000000 ) ) ;
#40249=AXIS2_PLACEMENT_3D ( 'NONE', #33594, #13553, #23173 ) ;
#40250=EDGE_CURVE ( 'NONE', #1826, #35253, #2194, .T. ) ;
#40271=CIRCLE ( 'NONE', #42362, 13.59999999999999787 ) ;
#40273=ORIENTED_EDGE ( 'NONE', *, *, #23694, .T. ) ;
#40276=ORIENTED_EDGE ( 'NONE', *, *, #33807, .F. ) ;
#40285=VERTEX_POINT ( 'NONE', #3921 ) ;
#40288=DIRECTION ( 'NONE',  ( 1.000000000000000000, -0.000000000000000000, -0.000000000000000000 ) ) ;
#40347=VERTEX_POINT ( 'NONE', #1314 ) ;
#40349=ORIENTED_EDGE ( 'NONE', *, *, #33087, .T. ) ;
#40354=DIRECTION ( 'NONE',  ( 0.000000000000000000, 0.000000000000000000, 1.000000000000000000 ) ) ;
#40360=DIRECTION ( 'NONE',  ( 0.000000000000000000, 0.5264321628773568351, -0.8502171357296134380 ) ) ;
#40363=ORIENTED_EDGE ( 'NONE', *, *, #38884, .F. ) ;
#40368=CARTESIAN_POINT ( 'NONE',  ( 0.000000000000000000, 0.000000000000000000, 0.000000000000000000 ) ) ;
#40369=DIRECTION ( 'NONE',  ( -1.000000000000000000, -0.000000000000000000, 0.000000000000000000 ) ) ;
#40378=VERTEX_POINT ( 'NONE', #14872 ) ;
#40379=CARTESIAN_POINT ( 'NONE',  ( 17.99999999999999645, 25.52601536738619714, -19.21447964122670626 ) ) ;
#40386=CIRCLE ( 'NONE', #7670, 13.59999999999999964 ) ;
#40388=ADVANCED_FACE ( 'NONE', ( #30787 ), #11817, .T. ) ;
#40390=ORIENTED_EDGE ( 'NONE', *, *, #37568, .T. ) ;
#40396=CARTESIAN_POINT ( 'NONE',  ( 17.99999999999999645, 16.86122981692017930, 27.13802899033298388 ) ) ;
#40404=ORIENTED_EDGE ( 'NONE', *, *, #38606, .T. ) ;
#40432=EDGE_CURVE ( 'NONE', #28925, #34983, #34473, .T. ) ;
#40436=DIRECTION ( 'NONE',  ( -1.000000000000000000, -0.000000000000000000, 0.000000000000000000 ) ) ;
#40445=VECTOR ( 'NONE', #17616, 1000.000000000000000 ) ;
#40449=CARTESIAN_POINT ( 'NONE',  ( 0.000000000000000000, -5.822172717930031993, -31.41458249383147106 ) ) ;
#40451=DIRECTION ( 'NONE',  ( 0.000000000000000000, 0.000000000000000000, 1.000000000000000000 ) ) ;
#40456=DIRECTION ( 'NONE',  ( -1.000000000000000000, 0.000000000000000000, 0.000000000000000000 ) ) ;
#40457=CIRCLE ( 'NONE', #16115, 13.60000000000000320 ) ;
#40458=CARTESIAN_POINT ( 'NONE',  ( 0.000000000000000000, 0.000000000000000000, 0.000000000000000000 ) ) ;
#40465=CARTESIAN_POINT ( 'NONE',  ( 17.99999999999999645, -31.11570115861498920, 4.898994019976531611 ) ) ;
#40467=EDGE_CURVE ( 'NONE', #33268, #18842, #33527, .T. ) ;
#40497=LINE ( 'NONE', #1658, #41573 ) ;
#40513=ORIENTED_EDGE ( 'NONE', *, *, #11378, .T. ) ;
#40524=DIRECTION ( 'NONE',  ( -1.000000000000000000, -0.000000000000000000, 0.000000000000000000 ) ) ;
#40529=ORIENTED_EDGE ( 'NONE', *, *, #5658, .F. ) ;
#40531=LINE ( 'NONE', #27704, #2131 ) ;
#40557=DIRECTION ( 'NONE',  ( -1.000000000000000000, 0.000000000000000000, -0.000000000000000000 ) ) ;
#40576=DIRECTION ( 'NONE',  ( 0.000000000000000000, 0.6736956436465532105, 0.7390089172206627532 ) ) ;
#40616=CIRCLE ( 'NONE', #22586, 36.00000000000000000 ) ;
#40617=ORIENTED_EDGE ( 'NONE', *, *, #35614, .F. ) ;
#40622=EDGE_CURVE ( 'NONE', #37185, #1059, #29346, .T. ) ;
#40642=SURFACE_STYLE_FILL_AREA ( #27379 ) ;
#40652=DIRECTION ( 'NONE',  ( -1.000000000000000000, 0.000000000000000000, 0.000000000000000000 ) ) ;
#40669=CARTESIAN_POINT ( 'NONE',  ( 0.000000000000000000, -35.78425302087536863, -3.935382540233168580 ) ) ;
#40674=EDGE_CURVE ( 'NONE', #28703, #19537, #37696, .T. ) ;
#40677=EDGE_CURVE ( 'NONE', #11747, #17756, #40457, .T. ) ;
#40690=CIRCLE ( 'NONE', #34863, 36.00000000000000000 ) ;
#40696=LINE ( 'NONE', #37222, #36073 ) ;
#40720=ORIENTED_EDGE ( 'NONE', *, *, #23698, .F. ) ;
#40723=VERTEX_POINT ( 'NONE', #6732 ) ;
#40737=ORIENTED_EDGE ( 'NONE', *, *, #37568, .F. ) ;
#40750=DIRECTION ( 'NONE',  ( 0.000000000000000000, 0.9618256431728179345, 0.2736629900720866648 ) ) ;
#40751=VECTOR ( 'NONE', #35679, 1000.000000000000000 ) ;
#40761=DIRECTION ( 'NONE',  ( -1.000000000000000000, 0.000000000000000000, 0.000000000000000000 ) ) ;
#40765=LINE ( 'NONE', #20984, #17499 ) ;
#40782=ORIENTED_EDGE ( 'NONE', *, *, #551, .F. ) ;
#40785=VERTEX_POINT ( 'NONE', #14822 ) ;
#40786=LINE ( 'NONE', #10705, #27536 ) ;
#40791=CARTESIAN_POINT ( 'NONE',  ( 17.99999999999999645, -28.57802095670076881, -14.28532136906702732 ) ) ;
#40793=DIRECTION ( 'NONE',  ( 0.000000000000000000, 0.000000000000000000, 1.000000000000000000 ) ) ;
#40794=VECTOR ( 'NONE', #8450, 1000.000000000000000 ) ;
#40812=CARTESIAN_POINT ( 'NONE',  ( 0.000000000000000000, -28.35267316522767445, -22.18391138608739155 ) ) ;
#40816=DIRECTION ( 'NONE',  ( -1.000000000000000000, -0.000000000000000000, 0.000000000000000000 ) ) ;
#40830=CARTESIAN_POINT ( 'NONE',  ( 17.99999999999999645, 16.77727049691149475, -27.19001440037526862 ) ) ;
#40835=ORIENTED_EDGE ( 'NONE', *, *, #20845, .T. ) ;
#40843=CIRCLE ( 'NONE', #29020, 36.00000000000000000 ) ;
#40844=EDGE_CURVE ( 'NONE', #30103, #12063, #15447, .T. ) ;
#40847=CIRCLE ( 'NONE', #10179, 13.59999999999999964 ) ;
#40858=LINE ( 'NONE', #11014, #37253 ) ;
#40862=ORIENTED_EDGE ( 'NONE', *, *, #32934, .T. ) ;
#40880=CIRCLE ( 'NONE', #1868, 31.49900000000000588 ) ;
#40896=CIRCLE ( 'NONE', #32564, 13.59999999999999964 ) ;
#40912=LINE ( 'NONE', #17633, #31057 ) ;
#40917=ORIENTED_EDGE ( 'NONE', *, *, #27368, .T. ) ;
#40923=CARTESIAN_POINT ( 'NONE',  ( 0.000000000000000000, 0.000000000000000000, 0.000000000000000000 ) ) ;
#40924=CIRCLE ( 'NONE', #15206, 31.49899999999999523 ) ;
#40932=CIRCLE ( 'NONE', #15909, 31.49900000000000233 ) ;
#40940=DIRECTION ( 'NONE',  ( 0.000000000000000000, 0.000000000000000000, 1.000000000000000000 ) ) ;
#40946=FACE_OUTER_BOUND ( 'NONE', #14488, .T. ) ;
#40948=CARTESIAN_POINT ( 'NONE',  ( 17.99999999999999645, -31.81777574834303124, -2.898764365605651427 ) ) ;
#40955=FACE_OUTER_BOUND ( 'NONE', #7109, .T. ) ;
#40983=CARTESIAN_POINT ( 'NONE',  ( 0.000000000000000000, -6.007673836298252468, 35.49518073029994980 ) ) ;
#40989=VERTEX_POINT ( 'NONE', #16048 ) ;
#40998=ORIENTED_EDGE ( 'NONE', *, *, #34542, .T. ) ;
#41002=CYLINDRICAL_SURFACE ( 'NONE', #20783, 13.59999999999999964 ) ;
#41004=CARTESIAN_POINT ( 'NONE',  ( 17.99999999999999645, 28.57802095670106723, -14.28532136906642691 ) ) ;
#41007=CARTESIAN_POINT ( 'NONE',  ( 17.99999999999999645, -0.6168405712484049674, -35.99471499692227638 ) ) ;
#41013=DIRECTION ( 'NONE',  ( -1.000000000000000000, 0.000000000000000000, 0.000000000000000000 ) ) ;
#41018=ORIENTED_EDGE ( 'NONE', *, *, #12405, .T. ) ;
#41020=DIRECTION ( 'NONE',  ( 1.000000000000000000, 0.000000000000000000, -0.000000000000000000 ) ) ;
#41025=DIRECTION ( 'NONE',  ( 0.000000000000000000, -0.1837495178165775567, 0.9829730996839004531 ) ) ;
#41027=DIRECTION ( 'NONE',  ( -1.000000000000000000, -0.000000000000000000, -0.000000000000000000 ) ) ;
#41049=EDGE_CURVE ( 'NONE', #38810, #12162, #2177, .T. ) ;
#41056=CARTESIAN_POINT ( 'NONE',  ( 17.99999999999999645, 14.84191762912354839, -27.78316904333109960 ) ) ;
#41066=ORIENTED_EDGE ( 'NONE', *, *, #7399, .T. ) ;
#41071=CARTESIAN_POINT ( 'NONE',  ( 17.99999999999999645, -30.78424799127063238, -6.672111855473501940 ) ) ;
#41074=DIRECTION ( 'NONE',  ( 1.000000000000000000, 0.000000000000000000, 0.000000000000000000 ) ) ;
#41086=ORIENTED_EDGE ( 'NONE', *, *, #39657, .T. ) ;
#41107=CARTESIAN_POINT ( 'NONE',  ( 0.000000000000000000, 11.49545354908936545, 29.80986809967263085 ) ) ;
#41111=CARTESIAN_POINT ( 'NONE',  ( 17.99999999999999645, 23.87611429743691360, -20.54551452399595135 ) ) ;
#41116=ORIENTED_EDGE ( 'NONE', *, *, #16008, .T. ) ;
#41137=CARTESIAN_POINT ( 'NONE',  ( 17.99999999999999645, 31.11570115861495367, 4.898994019976747438 ) ) ;
#41143=CARTESIAN_POINT ( 'NONE',  ( -10.00000000000000000, 0.000000000000000000, 0.000000000000000000 ) ) ;
#41144=CARTESIAN_POINT ( 'NONE',  ( 17.99999999999999645, 31.48608500567870294, -0.9019157472705674472 ) ) ;
#41149=EDGE_CURVE ( 'NONE', #12162, #27630, #37044, .T. ) ;
#41151=DIRECTION ( 'NONE',  ( 0.000000000000000000, 0.000000000000000000, 1.000000000000000000 ) ) ;
#41169=VERTEX_POINT ( 'NONE', #13630 ) ;
#41173=ADVANCED_FACE ( 'NONE', ( #30639 ), #3749, .T. ) ;
#41185=ORIENTED_EDGE ( 'NONE', *, *, #36159, .T. ) ;
#41191=CARTESIAN_POINT ( 'NONE',  ( 17.99999999999999645, -11.58753559615464290, -29.77419532459275331 ) ) ;
#41199=CARTESIAN_POINT ( 'NONE',  ( 0.000000000000000000, 26.29521155129848964, 17.34211205339357065 ) ) ;
#41200=EDGE_CURVE ( 'NONE', #16458, #12461, #26925, .T. ) ;
#41211=ORIENTED_EDGE ( 'NONE', *, *, #19770, .T. ) ;
#41214=FACE_OUTER_BOUND ( 'NONE', #2093, .T. ) ;
#41222=AXIS2_PLACEMENT_3D ( 'NONE', #28173, #21012, #41441 ) ;
#41255=ORIENTED_EDGE ( 'NONE', *, *, #10436, .F. ) ;
#41260=ADVANCED_FACE ( 'NONE', ( #21280 ), #18229, .T. ) ;
#41271=ORIENTED_EDGE ( 'NONE', *, *, #16347, .T. ) ;
#41279=DIRECTION ( 'NONE',  ( -1.000000000000000000, 0.000000000000000000, 0.000000000000000000 ) ) ;
#41282=EDGE_CURVE ( 'NONE', #13944, #38187, #5711, .T. ) ;
#41289=VERTEX_POINT ( 'NONE', #14929 ) ;
#41307=DIRECTION ( 'NONE',  ( 0.000000000000000000, 0.000000000000000000, -1.000000000000000000 ) ) ;
#41317=EDGE_LOOP ( 'NONE', ( #27267, #19849, #29640, #22677 ) ) ;
#41330=ADVANCED_FACE ( 'NONE', ( #34530 ), #18018, .F. ) ;
#41335=VERTEX_POINT ( 'NONE', #31924 ) ;
#41352=EDGE_CURVE ( 'NONE', #33690, #27845, #809, .T. ) ;
#41357=ORIENTED_EDGE ( 'NONE', *, *, #39657, .F. ) ;
#41358=AXIS2_PLACEMENT_3D ( 'NONE', #25254, #5989, #28728 ) ;
#41360=DIRECTION ( 'NONE',  ( -1.000000000000000000, -0.000000000000000000, 0.000000000000000000 ) ) ;
#41368=EDGE_CURVE ( 'NONE', #24289, #42039, #30799, .T. ) ;
#41375=CARTESIAN_POINT ( 'NONE',  ( 8.999999999999998224, 24.70533337038223110, 26.18485254986702060 ) ) ;
#41382=DIRECTION ( 'NONE',  ( -1.000000000000000000, 0.000000000000000000, 0.000000000000000000 ) ) ;
#41389=AXIS2_PLACEMENT_3D ( 'NONE', #26666, #16664, #24060 ) ;
#41391=CIRCLE ( 'NONE', #29583, 36.00000000000000000 ) ;
#41399=AXIS2_PLACEMENT_3D ( 'NONE', #41876, #35116, #8298 ) ;
#41410=ORIENTED_EDGE ( 'NONE', *, *, #38340, .F. ) ;
#41412=DIRECTION ( 'NONE',  ( 0.000000000000000000, 0.1837495178165638177, 0.9829730996839030066 ) ) ;
#41413=CARTESIAN_POINT ( 'NONE',  ( 17.99999999999999645, -21.48775762007876367, 23.64423737150130478 ) ) ;
#41419=ORIENTED_EDGE ( 'NONE', *, *, #319, .F. ) ;
#41426=CARTESIAN_POINT ( 'NONE',  ( 0.000000000000000000, 30.71634675606053833, 8.790889055186667633 ) ) ;
#41431=DIRECTION ( 'NONE',  ( -1.000000000000000000, -0.000000000000000000, 0.000000000000000000 ) ) ;
#41441=DIRECTION ( 'NONE',  ( 0.000000000000000000, 0.000000000000000000, 1.000000000000000000 ) ) ;
#41452=ORIENTED_EDGE ( 'NONE', *, *, #8317, .F. ) ;
#41468=AXIS2_PLACEMENT_3D ( 'NONE', #27376, #33472, #3556 ) ;
#41473=VERTEX_POINT ( 'NONE', #26016 ) ;
#41475=ADVANCED_FACE ( 'NONE', ( #36231 ), #36021, .T. ) ;
#41486=CARTESIAN_POINT ( 'NONE',  ( 8.999999999999998224, 12.42760411676086996, -33.78690065568411427 ) ) ;
#41488=ORIENTED_EDGE ( 'NONE', *, *, #41368, .T. ) ;
#41492=DIRECTION ( 'NONE',  ( 0.000000000000000000, -0.8951632913550570114, -0.4457383557765488558 ) ) ;
#41493=ORIENTED_EDGE ( 'NONE', *, *, #20420, .F. ) ;
#41504=DIRECTION ( 'NONE',  ( 0.000000000000000000, 0.000000000000000000, 1.000000000000000000 ) ) ;
#41512=DIRECTION ( 'NONE',  ( -1.000000000000000000, 0.000000000000000000, 0.000000000000000000 ) ) ;
#41514=DIRECTION ( 'NONE',  ( -1.000000000000000000, 0.000000000000000000, -0.000000000000000000 ) ) ;
#41515=ORIENTED_EDGE ( 'NONE', *, *, #7199, .F. ) ;
#41521=AXIS2_PLACEMENT_3D ( 'NONE', #8354, #37801, #41728 ) ;
#41539=AXIS2_PLACEMENT_3D ( 'NONE', #42353, #39078, #32549 ) ;
#41540=DIRECTION ( 'NONE',  ( 0.000000000000000000, 0.000000000000000000, 1.000000000000000000 ) ) ;
#41542=EDGE_LOOP ( 'NONE', ( #2311, #16323, #5235, #26976 ) ) ;
#41545=ADVANCED_FACE ( 'NONE', ( #4146 ), #10285, .T. ) ;
#41546=CIRCLE ( 'NONE', #27650, 13.59999999999999964 ) ;
#41567=( NAMED_UNIT ( * ) PLANE_ANGLE_UNIT ( ) SI_UNIT ( $, .RADIAN. ) );
#41572=CARTESIAN_POINT ( 'NONE',  ( 17.99999999999999645, -19.69434969228090893, 24.58291258574042004 ) ) ;
#41573=VECTOR ( 'NONE', #15245, 1000.000000000000000 ) ;
#41585=ORIENTED_EDGE ( 'NONE', *, *, #15910, .T. ) ;
#41596=EDGE_CURVE ( 'NONE', #27814, #28643, #41927, .T. ) ;
#41605=EDGE_CURVE ( 'NONE', #23084, #39350, #34273, .T. ) ;
#41607=LINE ( 'NONE', #37891, #732 ) ;
#41609=ORIENTED_EDGE ( 'NONE', *, *, #11123, .F. ) ;
#41614=CARTESIAN_POINT ( 'NONE',  ( 17.99999999999999645, 0.000000000000000000, 0.000000000000000000 ) ) ;
#41615=AXIS2_PLACEMENT_3D ( 'NONE', #28235, #31495, #1368 ) ;
#41619=ORIENTED_EDGE ( 'NONE', *, *, #27583, .T. ) ;
#41622=CARTESIAN_POINT ( 'NONE',  ( 0.000000000000000000, 29.68570942776472066, 10.53307442156944873 ) ) ;
#41627=DIRECTION ( 'NONE',  ( 0.000000000000000000, 0.000000000000000000, 1.000000000000000000 ) ) ;
#41636=AXIS2_PLACEMENT_3D ( 'NONE', #14960, #42161, #35424 ) ;
#41641=AXIS2_PLACEMENT_3D ( 'NONE', #4972, #25503, #28119 ) ;
#41650=VERTEX_POINT ( 'NONE', #3490 ) ;
#41652=DIRECTION ( 'NONE',  ( -1.000000000000000000, 0.000000000000000000, 0.000000000000000000 ) ) ;
#41659=EDGE_CURVE ( 'NONE', #35211, #33710, #23402, .T. ) ;
#41660=CIRCLE ( 'NONE', #9614, 13.60000000000000320 ) ;
#41703=DIRECTION ( 'NONE',  ( -1.000000000000000000, 0.000000000000000000, -0.000000000000000000 ) ) ;
#41709=CARTESIAN_POINT ( 'NONE',  ( 0.000000000000000000, 0.000000000000000000, 0.000000000000000000 ) ) ;
#41718=CIRCLE ( 'NONE', #38229, 36.00000000000000000 ) ;
#41727=DIRECTION ( 'NONE',  ( -1.000000000000000000, 0.000000000000000000, 0.000000000000000000 ) ) ;
#41728=DIRECTION ( 'NONE',  ( 0.000000000000000000, 0.000000000000000000, 1.000000000000000000 ) ) ;
#41742=CARTESIAN_POINT ( 'NONE',  ( 17.99999999999999645, 19.47322409167269086, 30.27859877001407085 ) ) ;
#41745=AXIS2_PLACEMENT_3D ( 'NONE', #24142, #40456, #17393 ) ;
#41749=CARTESIAN_POINT ( 'NONE',  ( 17.99999999999999645, 5.919241748379588053, 31.39643714728458690 ) ) ;
#41762=ADVANCED_FACE ( 'NONE', ( #1087 ), #31648, .T. ) ;
#41773=VERTEX_POINT ( 'NONE', #18608 ) ;
#41775=AXIS2_PLACEMENT_3D ( 'NONE', #43101, #13254, #39817 ) ;
#41801=VECTOR ( 'NONE', #3071, 1000.000000000000000 ) ;
#41804=CARTESIAN_POINT ( 'NONE',  ( 0.000000000000000000, 23.87611429743691360, -20.54551452399595135 ) ) ;
#41806=DIRECTION ( 'NONE',  ( 0.000000000000000000, -0.5264321628773627193, 0.8502171357296098853 ) ) ;
#41825=AXIS2_PLACEMENT_3D ( 'NONE', #11824, #21665, #39235 ) ;
#41829=CARTESIAN_POINT ( 'NONE',  ( 17.99999999999999645, -13.22719389141998825, 28.58720592780592185 ) ) ;
#41834=AXIS2_PLACEMENT_3D ( 'NONE', #11257, #25240, #28507 ) ;
#41852=CARTESIAN_POINT ( 'NONE',  ( 17.99999999999999645, -30.71634675606060227, 8.790889055186445589 ) ) ;
#41862=AXIS2_PLACEMENT_3D ( 'NONE', #42180, #9249, #36074 ) ;
#41863=AXIS2_PLACEMENT_3D ( 'NONE', #34749, #34956, #17776 ) ;
#41865=FACE_OUTER_BOUND ( 'NONE', #14107, .T. ) ;
#41872=DIRECTION ( 'NONE',  ( 0.000000000000000000, -0.9957341762950354669, 0.09226835946329131621 ) ) ;
#41876=CARTESIAN_POINT ( 'NONE',  ( 0.000000000000000000, 0.000000000000000000, 0.000000000000000000 ) ) ;
#41899=CARTESIAN_POINT ( 'NONE',  ( 17.99999999999999645, -19.47322409167248480, -30.27859877001420230 ) ) ;
#41912=DIRECTION ( 'NONE',  ( 0.000000000000000000, 0.000000000000000000, -1.000000000000000000 ) ) ;
#41923=CARTESIAN_POINT ( 'NONE',  ( 17.99999999999999645, -28.57802095670097131, 14.28532136906662586 ) ) ;
#41924=ORIENTED_EDGE ( 'NONE', *, *, #1053, .T. ) ;
#41927=CIRCLE ( 'NONE', #23165, 36.00000000000000000 ) ;
#41931=CYLINDRICAL_SURFACE ( 'NONE', #20642, 13.60000000000000142 ) ;
#41932=CARTESIAN_POINT ( 'NONE',  ( 0.000000000000000000, -30.71634675606047793, -8.790889055186887902 ) ) ;
#41940=DIRECTION ( 'NONE',  ( 1.000000000000000000, 0.000000000000000000, 0.000000000000000000 ) ) ;
#41965=ORIENTED_EDGE ( 'NONE', *, *, #19582, .T. ) ;
#41974=DIRECTION ( 'NONE',  ( 0.000000000000000000, 0.000000000000000000, 1.000000000000000000 ) ) ;
#41989=FACE_OUTER_BOUND ( 'NONE', #13266, .T. ) ;
#41993=ORIENTED_EDGE ( 'NONE', *, *, #9169, .F. ) ;
#42004=ORIENTED_EDGE ( 'NONE', *, *, #564, .F. ) ;
#42005=DIRECTION ( 'NONE',  ( -1.000000000000000000, -0.000000000000000000, 0.000000000000000000 ) ) ;
#42010=DIRECTION ( 'NONE',  ( -1.000000000000000000, -0.000000000000000000, 0.000000000000000000 ) ) ;
#42011=CARTESIAN_POINT ( 'NONE',  ( 0.000000000000000000, 29.68570942776486987, -10.53307442156903662 ) ) ;
#42031=ORIENTED_EDGE ( 'NONE', *, *, #26374, .T. ) ;
#42033=ORIENTED_EDGE ( 'NONE', *, *, #2021, .T. ) ;
#42039=VERTEX_POINT ( 'NONE', #16823 ) ;
#42041=DIRECTION ( 'NONE',  ( -1.000000000000000000, -0.000000000000000000, 0.000000000000000000 ) ) ;
#42057=CARTESIAN_POINT ( 'NONE',  ( 17.99999999999999645, 0.000000000000000000, 0.000000000000000000 ) ) ;
#42059=ORIENTED_EDGE ( 'NONE', *, *, #25429, .F. ) ;
#42074=DIRECTION ( 'NONE',  ( -1.000000000000000000, -0.000000000000000000, 0.000000000000000000 ) ) ;
#42081=AXIS2_PLACEMENT_3D ( 'NONE', #12023, #5233, #18815 ) ;
#42106=ORIENTED_EDGE ( 'NONE', *, *, #35665, .F. ) ;
#42110=ORIENTED_EDGE ( 'NONE', *, *, #38606, .F. ) ;
#42117=ORIENTED_EDGE ( 'NONE', *, *, #39785, .T. ) ;
#42127=VECTOR ( 'NONE', #18238, 1000.000000000000000 ) ;
#42145=CIRCLE ( 'NONE', #17134, 36.00000000000000000 ) ;
#42161=DIRECTION ( 'NONE',  ( -1.000000000000000000, -0.000000000000000000, -0.000000000000000000 ) ) ;
#42180=CARTESIAN_POINT ( 'NONE',  ( 17.99999999999999645, 0.000000000000000000, 0.000000000000000000 ) ) ;
#42187=EDGE_CURVE ( 'NONE', #40723, #23356, #39202, .T. ) ;
#42195=DIRECTION ( 'NONE',  ( 0.000000000000000000, 0.000000000000000000, 1.000000000000000000 ) ) ;
#42198=EDGE_LOOP ( 'NONE', ( #13695, #14437, #34099, #29984 ) ) ;
#42202=CARTESIAN_POINT ( 'NONE',  ( 17.99999999999999645, 18.25486108452660972, -25.66996392254254644 ) ) ;
#42207=EDGE_CURVE ( 'NONE', #23236, #2013, #27405, .T. ) ;
#42212=AXIS2_PLACEMENT_3D ( 'NONE', #12502, #9638, #19491 ) ;
#42213=CARTESIAN_POINT ( 'NONE',  ( 0.000000000000000000, -23.87611429743677505, 20.54551452399611478 ) ) ;
#42219=CARTESIAN_POINT ( 'NONE',  ( 0.000000000000000000, 6.007673836298521586, -35.49518073029990717 ) ) ;
#42230=AXIS2_PLACEMENT_3D ( 'NONE', #32685, #36162, #23121 ) ;
#42244=ADVANCED_FACE ( 'NONE', ( #28130 ), #4534, .T. ) ;
#42270=AXIS2_PLACEMENT_3D ( 'NONE', #26197, #39472, #20482 ) ;
#42274=CARTESIAN_POINT ( 'NONE',  ( 17.99999999999999645, 30.74337109795208178, 8.695908345466650147 ) ) ;
#42287=ORIENTED_EDGE ( 'NONE', *, *, #32241, .T. ) ;
#42304=AXIS2_PLACEMENT_3D ( 'NONE', #37231, #28946, #12578 ) ;
#42309=CARTESIAN_POINT ( 'NONE',  ( 17.99999999999999645, 0.000000000000000000, 0.000000000000000000 ) ) ;
#42317=VERTEX_POINT ( 'NONE', #21178 ) ;
#42337=AXIS2_PLACEMENT_3D ( 'NONE', #38852, #2187, #5898 ) ;
#42340=DIRECTION ( 'NONE',  ( -1.000000000000000000, 0.000000000000000000, -0.000000000000000000 ) ) ;
#42350=ORIENTED_EDGE ( 'NONE', *, *, #39694, .F. ) ;
#42351=FACE_OUTER_BOUND ( 'NONE', #365, .T. ) ;
#42353=CARTESIAN_POINT ( 'NONE',  ( 17.99999999999999645, -31.81777574834308098, 2.898764365605205562 ) ) ;
#42362=AXIS2_PLACEMENT_3D ( 'NONE', #11727, #25065, #38304 ) ;
#42368=DIRECTION ( 'NONE',  ( -1.000000000000000000, 0.000000000000000000, 0.000000000000000000 ) ) ;
#42378=VERTEX_POINT ( 'NONE', #32668 ) ;
#42381=CARTESIAN_POINT ( 'NONE',  ( 0.000000000000000000, -2.007101075700183035, 31.43498920425968990 ) ) ;
#42385=DIRECTION ( 'NONE',  ( -1.000000000000000000, 0.000000000000000000, 0.000000000000000000 ) ) ;
#42392=DIRECTION ( 'NONE',  ( 0.000000000000000000, 0.000000000000000000, -1.000000000000000000 ) ) ;
#42394=VERTEX_POINT ( 'NONE', #16110 ) ;
#42399=EDGE_LOOP ( 'NONE', ( #26719, #40115, #12104, #5548 ) ) ;
#42406=CARTESIAN_POINT ( 'NONE',  ( 0.000000000000000000, 0.000000000000000000, 0.000000000000000000 ) ) ;
#42418=VECTOR ( 'NONE', #31746, 1000.000000000000000 ) ;
#42427=CARTESIAN_POINT ( 'NONE',  ( 17.99999999999999645, 13.22719389141978930, 28.58720592780601066 ) ) ;
#42433=EDGE_CURVE ( 'NONE', #27860, #38361, #23966, .T. ) ;
#42439=DIRECTION ( 'NONE',  ( 0.000000000000000000, 0.000000000000000000, 1.000000000000000000 ) ) ;
#42442=LINE ( 'NONE', #2290, #26562 ) ;
#42456=CARTESIAN_POINT ( 'NONE',  ( 17.99999999999999645, 0.000000000000000000, 0.000000000000000000 ) ) ;
#42483=ADVANCED_FACE ( 'NONE', ( #20047 ), #19606, .T. ) ;
#42484=EDGE_LOOP ( 'NONE', ( #763, #39620, #17299, #32839 ) ) ;
#42488=FACE_OUTER_BOUND ( 'NONE', #25846, .T. ) ;
#42497=LINE ( 'NONE', #2773, #23868 ) ;
#42507=CIRCLE ( 'NONE', #11184, 13.59999999999999964 ) ;
#42523=ORIENTED_EDGE ( 'NONE', *, *, #42207, .T. ) ;
#42527=EDGE_CURVE ( 'NONE', #42394, #33710, #19084, .T. ) ;
#42571=EDGE_LOOP ( 'NONE', ( #11856, #41924, #41993, #31860 ) ) ;
#42574=ORIENTED_EDGE ( 'NONE', *, *, #20, .T. ) ;
#42578=EDGE_CURVE ( 'NONE', #2232, #10112, #30888, .T. ) ;
#42579=CIRCLE ( 'NONE', #33534, 31.49899999999999878 ) ;
#42581=ORIENTED_EDGE ( 'NONE', *, *, #326, .T. ) ;
#42590=CARTESIAN_POINT ( 'NONE',  ( 17.99999999999999645, 28.57802095670086828, 14.28532136906683370 ) ) ;
#42597=CYLINDRICAL_SURFACE ( 'NONE', #18745, 13.59999999999999964 ) ;
#42600=ORIENTED_EDGE ( 'NONE', *, *, #5000, .T. ) ;
#42608=VERTEX_POINT ( 'NONE', #41572 ) ;
#42609=DIRECTION ( 'NONE',  ( 0.000000000000000000, 0.9957341762950349118, -0.09226835946329871307 ) ) ;
#42610=PRODUCT ( 'spur gear_iso_ISO - Spur gear 2M 34T 20PA 18FW ---S34A75H50L30.0N', 'spur gear_iso_ISO - Spur gear 2M 34T 20PA 18FW ---S34A75H50L30.0N', '', ( #42724 ) ) ;
#42611=ADVANCED_FACE ( 'NONE', ( #11723 ), #31126, .T. ) ;
#42616=LINE ( 'NONE', #32388, #26903 ) ;
#42632=CARTESIAN_POINT ( 'NONE',  ( 17.99999999999999645, 3.803237743092368284, -31.26855263151010789 ) ) ;
#42637=DIRECTION ( 'NONE',  ( 0.000000000000000000, 0.6736956436465532105, 0.7390089172206627532 ) ) ;
#42644=ORIENTED_EDGE ( 'NONE', *, *, #16008, .F. ) ;
#42652=EDGE_CURVE ( 'NONE', #30185, #26654, #3021, .T. ) ;
#42659=ORIENTED_EDGE ( 'NONE', *, *, #32346, .T. ) ;
#42677=ORIENTED_EDGE ( 'NONE', *, *, #12106, .T. ) ;
#42694=ORIENTED_EDGE ( 'NONE', *, *, #15690, .F. ) ;
#42702=CIRCLE ( 'NONE', #26727, 13.59999999999999787 ) ;
#42711=DIRECTION ( 'NONE',  ( -1.000000000000000000, 0.000000000000000000, -0.000000000000000000 ) ) ;
#42724=PRODUCT_CONTEXT ( 'NONE', #2979, 'mechanical' ) ;
#42732=ADVANCED_FACE ( 'NONE', ( #41989 ), #1864, .T. ) ;
#42734=FACE_OUTER_BOUND ( 'NONE', #4575, .T. ) ;
#42739=VERTEX_POINT ( 'NONE', #12139 ) ;
#42747=VERTEX_POINT ( 'NONE', #28931 ) ;
#42763=AXIS2_PLACEMENT_3D ( 'NONE', #19002, #19625, #25324 ) ;
#42767=DIRECTION ( 'NONE',  ( -1.000000000000000000, 0.000000000000000000, 0.000000000000000000 ) ) ;
#42795=LINE ( 'NONE', #22576, #30141 ) ;
#42800=ORIENTED_EDGE ( 'NONE', *, *, #23857, .T. ) ;
#42821=EDGE_CURVE ( 'NONE', #43048, #41169, #5834, .T. ) ;
#42831=SURFACE_STYLE_FILL_AREA ( #3342 ) ;
#42837=LINE ( 'NONE', #5776, #9508 ) ;
#42876=EDGE_LOOP ( 'NONE', ( #9977, #27663, #17166, #23305 ) ) ;
#42888=DIRECTION ( 'NONE',  ( 0.000000000000000000, 0.000000000000000000, 1.000000000000000000 ) ) ;
#42892=LINE ( 'NONE', #36347, #12936 ) ;
#42900=CIRCLE ( 'NONE', #13013, 13.60000000000000320 ) ;
#42936=EDGE_LOOP ( 'NONE', ( #15941, #7505, #38938, #6292 ) ) ;
#42937=DIRECTION ( 'NONE',  ( -1.000000000000000000, 0.000000000000000000, -0.000000000000000000 ) ) ;
#42941=CARTESIAN_POINT ( 'NONE',  ( 0.000000000000000000, 25.46650492921896713, 19.29328419707794495 ) ) ;
#42946=AXIS2_PLACEMENT_3D ( 'NONE', #22861, #9723, #42439 ) ;
#42958=EDGE_CURVE ( 'NONE', #17989, #20730, #37875, .T. ) ;
#42979=CIRCLE ( 'NONE', #502, 36.00000000000000000 ) ;
#42980=ORIENTED_EDGE ( 'NONE', *, *, #9121, .T. ) ;
#42986=CIRCLE ( 'NONE', #18689, 13.59999999999999787 ) ;
#42989=ORIENTED_EDGE ( 'NONE', *, *, #7898, .T. ) ;
#42998=ORIENTED_EDGE ( 'NONE', *, *, #21007, .F. ) ;
#43004=CIRCLE ( 'NONE', #20776, 13.59999999999999964 ) ;
#43008=AXIS2_PLACEMENT_3D ( 'NONE', #13332, #16173, #33157 ) ;
#43012=AXIS2_PLACEMENT_3D ( 'NONE', #41932, #15158, #15784 ) ;
#43014=ORIENTED_EDGE ( 'NONE', *, *, #37167, .F. ) ;
#43047=DIRECTION ( 'NONE',  ( 0.000000000000000000, -0.6736956436465636466, 0.7390089172206532053 ) ) ;
#43048=VERTEX_POINT ( 'NONE', #31883 ) ;
#43051=EDGE_CURVE ( 'NONE', #6792, #3236, #41391, .T. ) ;
#43058=DIRECTION ( 'NONE',  ( -1.000000000000000000, -0.000000000000000000, -0.000000000000000000 ) ) ;
#43066=ADVANCED_FACE ( 'NONE', ( #25152 ), #14454, .T. ) ;
#43101=CARTESIAN_POINT ( 'NONE',  ( 0.000000000000000000, 28.57802095670086828, 14.28532136906683370 ) ) ;
#43110=ORIENTED_EDGE ( 'NONE', *, *, #15778, .T. ) ;
#43111=CIRCLE ( 'NONE', #39646, 13.59999999999999964 ) ;
#43112=CARTESIAN_POINT ( 'NONE',  ( 17.99999999999999645, -13.57797752207901532, -33.34124362422488730 ) ) ;
#43119=CARTESIAN_POINT ( 'NONE',  ( 0.000000000000000000, 9.484061862024356415, -30.03730300138970932 ) ) ;
#43124=VERTEX_POINT ( 'NONE', #31240 ) ;
#43132=CYLINDRICAL_SURFACE ( 'NONE', #31710, 13.59999999999999964 ) ;
#43133=ADVANCED_FACE ( 'NONE', ( #21462 ), #34710, .T. ) ;
#43151=DIRECTION ( 'NONE',  ( 0.000000000000000000, 0.000000000000000000, 1.000000000000000000 ) ) ;
#43161=ORIENTED_EDGE ( 'NONE', *, *, #6928, .F. ) ;
#43177=ORIENTED_EDGE ( 'NONE', *, *, #564, .T. ) ;
ENDSEC;
END-ISO-10303-21;
